ISO-10303-21;
HEADER;
FILE_DESCRIPTION (('STEP AP214'),
    '1' );
FILE_NAME ('small gear_ISO - Spur gear 2M 40T 20PA 10FW ---S40A75H50L20.0N.step',
    '2026-10-08T09:53:37',
    ( '' ),
    ( '' ),
    'SwSTEP 2.0',
    'SolidWorks 2026',
    '' );
FILE_SCHEMA (( 'AUTOMOTIVE_DESIGN' ));
ENDSEC;

DATA;
#4=DIRECTION ( 'NONE',  ( -1.000000000000000000, -0.000000000000000000, -0.000000000000000000 ) ) ;
#5=CARTESIAN_POINT ( 'NONE',  ( 10.00000000000000000, 21.53537804866126137, -30.80686688396986028 ) ) ;
#8=DIRECTION ( 'NONE',  ( -1.000000000000000000, 0.000000000000000000, 0.000000000000000000 ) ) ;
#17=DIRECTION ( 'NONE',  ( 0.000000000000000000, 0.8910065241883656784, 0.4539904997395510788 ) ) ;
#25=AXIS2_PLACEMENT_3D ( 'NONE', #2057, #18922, #40477 ) ;
#33=CIRCLE ( 'NONE', #8406, 42.00000000000000000 ) ;
#39=EDGE_CURVE ( 'NONE', #49169, #37092, #23562, .T. ) ;
#65=CIRCLE ( 'NONE', #33475, 42.00000000000000000 ) ;
#68=CIRCLE ( 'NONE', #60030, 16.00000000000000000 ) ;
#93=AXIS2_PLACEMENT_3D ( 'NONE', #19631, #69384, #17880 ) ;
#114=ORIENTED_EDGE ( 'NONE', *, *, #19664, .T. ) ;
#121=AXIS2_PLACEMENT_3D ( 'NONE', #14908, #31452, #37108 ) ;
#128=EDGE_LOOP ( 'NONE', ( #64642, #36236, #46742, #60430 ) ) ;
#137=ORIENTED_EDGE ( 'NONE', *, *, #39556, .T. ) ;
#141=ORIENTED_EDGE ( 'NONE', *, *, #29114, .F. ) ;
#142=CARTESIAN_POINT ( 'NONE',  ( 10.00000000000000000, 22.74946021919175720, -29.81001611430984255 ) ) ;
#161=DIRECTION ( 'NONE',  ( 0.000000000000000000, 0.000000000000000000, 1.000000000000000000 ) ) ;
#180=AXIS2_PLACEMENT_3D ( 'NONE', #34076, #10405, #33316 ) ;
#184=CARTESIAN_POINT ( 'NONE',  ( 5.000000000000000000, -38.55633173626998911, -16.65560815589452304 ) ) ;
#189=DIRECTION ( 'NONE',  ( -1.000000000000000000, -0.000000000000000000, 0.000000000000000000 ) ) ;
#215=EDGE_CURVE ( 'NONE', #47891, #8216, #22873, .T. ) ;
#249=DIRECTION ( 'NONE',  ( -1.000000000000000000, 0.000000000000000000, -0.000000000000000000 ) ) ;
#254=ORIENTED_EDGE ( 'NONE', *, *, #39026, .T. ) ;
#294=LINE ( 'NONE', #17534, #41829 ) ;
#304=DIRECTION ( 'NONE',  ( 0.000000000000000000, -0.8090169943749531134, 0.5877852522924654766 ) ) ;
#305=VERTEX_POINT ( 'NONE', #60978 ) ;
#308=FACE_OUTER_BOUND ( 'NONE', #16262, .T. ) ;
#318=CYLINDRICAL_SURFACE ( 'NONE', #22478, 37.49900000000000233 ) ;
#323=CYLINDRICAL_SURFACE ( 'NONE', #57366, 37.49900000000000233 ) ;
#334=DIRECTION ( 'NONE',  ( 0.000000000000000000, 0.000000000000000000, 1.000000000000000000 ) ) ;
#364=ORIENTED_EDGE ( 'NONE', *, *, #34297, .F. ) ;
#388=EDGE_CURVE ( 'NONE', #19251, #12587, #32396, .T. ) ;
#394=CARTESIAN_POINT ( 'NONE',  ( 0.000000000000000000, -35.95386929396264009, 10.96151621346475658 ) ) ;
#399=AXIS2_PLACEMENT_3D ( 'NONE', #19459, #47664, #13453 ) ;
#404=EDGE_CURVE ( 'NONE', #15647, #17733, #32964, .T. ) ;
#420=VERTEX_POINT ( 'NONE', #38424 ) ;
#439=ORIENTED_EDGE ( 'NONE', *, *, #48970, .F. ) ;
#441=AXIS2_PLACEMENT_3D ( 'NONE', #21998, #44945, #63995 ) ;
#456=DIRECTION ( 'NONE',  ( -1.000000000000000000, 0.000000000000000000, -0.000000000000000000 ) ) ;
#457=EDGE_CURVE ( 'NONE', #24962, #18771, #8940, .T. ) ;
#462=DIRECTION ( 'NONE',  ( -1.000000000000000000, -0.000000000000000000, -0.000000000000000000 ) ) ;
#463=CARTESIAN_POINT ( 'NONE',  ( 0.000000000000000000, -16.23288003029521320, 33.80338159004277543 ) ) ;
#467=DIRECTION ( 'NONE',  ( -1.000000000000000000, 0.000000000000000000, 0.000000000000000000 ) ) ;
#468=DIRECTION ( 'NONE',  ( -1.000000000000000000, 0.000000000000000000, -0.000000000000000000 ) ) ;
#486=DIRECTION ( 'NONE',  ( 0.000000000000000000, 0.000000000000000000, 1.000000000000000000 ) ) ;
#497=ORIENTED_EDGE ( 'NONE', *, *, #18676, .T. ) ;
#511=CARTESIAN_POINT ( 'NONE',  ( 10.00000000000000000, -0.8828120875903202602, 37.48860685352291000 ) ) ;
#516=ORIENTED_EDGE ( 'NONE', *, *, #53833, .T. ) ;
#536=CARTESIAN_POINT ( 'NONE',  ( 10.00000000000000000, 29.81001611431041098, -22.74946021919100403 ) ) ;
#540=LINE ( 'NONE', #23438, #24033 ) ;
#550=CARTESIAN_POINT ( 'NONE',  ( -10.00000000000000000, 0.000000000000000000, 0.000000000000000000 ) ) ;
#557=DIRECTION ( 'NONE',  ( 0.000000000000000000, 0.000000000000000000, 1.000000000000000000 ) ) ;
#574=DIRECTION ( 'NONE',  ( -1.000000000000000000, -0.000000000000000000, 0.000000000000000000 ) ) ;
#600=ORIENTED_EDGE ( 'NONE', *, *, #27391, .T. ) ;
#604=CARTESIAN_POINT ( 'NONE',  ( 10.00000000000000000, 26.08949754953024325, 27.05870788708241648 ) ) ;
#606=CYLINDRICAL_SURFACE ( 'NONE', #23467, 16.00000000000000000 ) ;
#607=AXIS2_PLACEMENT_3D ( 'NONE', #43704, #71876, #9106 ) ;
#608=CARTESIAN_POINT ( 'NONE',  ( 10.00000000000000000, 17.80606268964540462, 33.00180498840053644 ) ) ;
#614=AXIS2_PLACEMENT_3D ( 'NONE', #15545, #73036, #49383 ) ;
#633=VERTEX_POINT ( 'NONE', #13543 ) ;
#640=ADVANCED_FACE ( 'NONE', ( #6800 ), #18087, .T. ) ;
#646=DIRECTION ( 'NONE',  ( -1.000000000000000000, 0.000000000000000000, 0.000000000000000000 ) ) ;
#653=EDGE_CURVE ( 'NONE', #39661, #53810, #37773, .T. ) ;
#663=AXIS2_PLACEMENT_3D ( 'NONE', #26223, #37524, #31862 ) ;
#667=EDGE_CURVE ( 'NONE', #38085, #21754, #59390, .T. ) ;
#694=CARTESIAN_POINT ( 'NONE',  ( 0.000000000000000000, 0.000000000000000000, 0.000000000000000000 ) ) ;
#708=CARTESIAN_POINT ( 'NONE',  ( 10.00000000000000000, -10.74501242461258244, -35.92658777277521409 ) ) ;
#713=ORIENTED_EDGE ( 'NONE', *, *, #55662, .F. ) ;
#723=EDGE_CURVE ( 'NONE', #44034, #16018, #25617, .T. ) ;
#729=VERTEX_POINT ( 'NONE', #41025 ) ;
#736=CIRCLE ( 'NONE', #30667, 16.00000000000000355 ) ;
#737=EDGE_CURVE ( 'NONE', #34884, #37666, #67655, .T. ) ;
#772=VECTOR ( 'NONE', #57930, 1000.000000000000000 ) ;
#778=ORIENTED_EDGE ( 'NONE', *, *, #49916, .F. ) ;
#783=ORIENTED_EDGE ( 'NONE', *, *, #47685, .F. ) ;
#790=ORIENTED_EDGE ( 'NONE', *, *, #1567, .F. ) ;
#800=AXIS2_PLACEMENT_3D ( 'NONE', #26996, #3729, #16474 ) ;
#814=ORIENTED_EDGE ( 'NONE', *, *, #38959, .F. ) ;
#824=FACE_OUTER_BOUND ( 'NONE', #34255, .T. ) ;
#841=CARTESIAN_POINT ( 'NONE',  ( 10.00000000000000000, -37.58145647212455032, 0.6853352020789044152 ) ) ;
#858=AXIS2_PLACEMENT_3D ( 'NONE', #17609, #45833, #68755 ) ;
#863=DIRECTION ( 'NONE',  ( -1.000000000000000000, -0.000000000000000000, 0.000000000000000000 ) ) ;
#867=CIRCLE ( 'NONE', #42855, 42.00000000000000000 ) ;
#882=ORIENTED_EDGE ( 'NONE', *, *, #12481, .F. ) ;
#890=FACE_OUTER_BOUND ( 'NONE', #46338, .T. ) ;
#958=DIRECTION ( 'NONE',  ( -1.000000000000000000, -0.000000000000000000, 0.000000000000000000 ) ) ;
#979=CARTESIAN_POINT ( 'NONE',  ( 10.00000000000000000, -16.45098606841102651, -33.79645857604531045 ) ) ;
#983=FACE_OUTER_BOUND ( 'NONE', #73941, .T. ) ;
#1000=CARTESIAN_POINT ( 'NONE',  ( 0.000000000000000000, 16.95692799528845640, -1.176623242955009039E-14 ) ) ;
#1003=ORIENTED_EDGE ( 'NONE', *, *, #34297, .T. ) ;
#1004=CIRCLE ( 'NONE', #67001, 42.00000000000000000 ) ;
#1007=ADVANCED_FACE ( 'NONE', ( #69142 ), #17626, .T. ) ;
#1015=DIRECTION ( 'NONE',  ( -1.000000000000000000, 0.000000000000000000, -0.000000000000000000 ) ) ;
#1037=EDGE_CURVE ( 'NONE', #26528, #55462, #37286, .T. ) ;
#1045=AXIS2_PLACEMENT_3D ( 'NONE', #37846, #37482, #72037 ) ;
#1050=CIRCLE ( 'NONE', #17802, 42.00000000000000000 ) ;
#1057=DIRECTION ( 'NONE',  ( 1.000000000000000000, 0.000000000000000000, 0.000000000000000000 ) ) ;
#1060=EDGE_CURVE ( 'NONE', #59771, #48642, #39457, .T. ) ;
#1083=DIRECTION ( 'NONE',  ( -1.000000000000000000, -0.000000000000000000, 0.000000000000000000 ) ) ;
#1093=VERTEX_POINT ( 'NONE', #17993 ) ;
#1104=DIRECTION ( 'NONE',  ( 0.000000000000000000, 0.000000000000000000, 1.000000000000000000 ) ) ;
#1118=CARTESIAN_POINT ( 'NONE',  ( 4.999999999999999112, -2.663952781846440576, 41.91543099594817789 ) ) ;
#1134=DIRECTION ( 'NONE',  ( 0.000000000000000000, 0.000000000000000000, 1.000000000000000000 ) ) ;
#1144=EDGE_CURVE ( 'NONE', #34884, #21495, #31203, .T. ) ;
#1153=ORIENTED_EDGE ( 'NONE', *, *, #63592, .T. ) ;
#1163=CIRCLE ( 'NONE', #17913, 42.00000000000000000 ) ;
#1164=EDGE_LOOP ( 'NONE', ( #66927, #73159, #62142, #19064 ) ) ;
#1166=VERTEX_POINT ( 'NONE', #7082 ) ;
#1186=CARTESIAN_POINT ( 'NONE',  ( -10.00000000000000000, 0.000000000000000000, 0.000000000000000000 ) ) ;
#1202=DIRECTION ( 'NONE',  ( -1.000000000000000000, 0.000000000000000000, 0.000000000000000000 ) ) ;
#1204=CIRCLE ( 'NONE', #3594, 16.00000000000000000 ) ;
#1210=ORIENTED_EDGE ( 'NONE', *, *, #37944, .T. ) ;
#1225=DIRECTION ( 'NONE',  ( 0.000000000000000000, 0.000000000000000000, 1.000000000000000000 ) ) ;
#1229=ADVANCED_FACE ( 'NONE', ( #7820 ), #30737, .T. ) ;
#1261=EDGE_LOOP ( 'NONE', ( #9691, #58194, #22600, #52420 ) ) ;
#1264=AXIS2_PLACEMENT_3D ( 'NONE', #61042, #50496, #16287 ) ;
#1314=ADVANCED_FACE ( 'NONE', ( #54791 ), #3687, .T. ) ;
#1330=EDGE_CURVE ( 'NONE', #9413, #14702, #54034, .T. ) ;
#1341=EDGE_CURVE ( 'NONE', #59461, #44099, #3318, .T. ) ;
#1352=CYLINDRICAL_SURFACE ( 'NONE', #10629, 16.00000000000000000 ) ;
#1392=CARTESIAN_POINT ( 'NONE',  ( 10.00000000000000000, 0.000000000000000000, 0.000000000000000000 ) ) ;
#1409=AXIS2_PLACEMENT_3D ( 'NONE', #53674, #19086, #35631 ) ;
#1412=ORIENTED_EDGE ( 'NONE', *, *, #5219, .F. ) ;
#1423=AXIS2_PLACEMENT_3D ( 'NONE', #13367, #36300, #7735 ) ;
#1427=DIRECTION ( 'NONE',  ( 0.000000000000000000, 0.000000000000000000, 1.000000000000000000 ) ) ;
#1432=DIRECTION ( 'NONE',  ( 1.000000000000000000, 0.000000000000000000, 0.000000000000000000 ) ) ;
#1433=EDGE_CURVE ( 'NONE', #64991, #31095, #60059, .T. ) ;
#1473=ORIENTED_EDGE ( 'NONE', *, *, #45783, .F. ) ;
#1494=CARTESIAN_POINT ( 'NONE',  ( 10.00000000000000000, 0.8828120875905820508, -37.48860685352290290 ) ) ;
#1498=DIRECTION ( 'NONE',  ( 0.000000000000000000, 0.8910065241883688980, -0.4539904997395445840 ) ) ;
#1509=ADVANCED_FACE ( 'NONE', ( #64059 ), #36208, .T. ) ;
#1534=ORIENTED_EDGE ( 'NONE', *, *, #56706, .T. ) ;
#1535=VERTEX_POINT ( 'NONE', #2781 ) ;
#1564=CIRCLE ( 'NONE', #68777, 37.49900000000000233 ) ;
#1567=EDGE_CURVE ( 'NONE', #47714, #31828, #41285, .T. ) ;
#1581=CARTESIAN_POINT ( 'NONE',  ( 10.00000000000000000, -6.736453364083292428, -36.88895765772640800 ) ) ;
#1584=CARTESIAN_POINT ( 'NONE',  ( 10.00000000000000000, 33.80338159004283938, 16.23288003029508886 ) ) ;
#1585=EDGE_CURVE ( 'NONE', #57628, #18829, #8754, .T. ) ;
#1587=CARTESIAN_POINT ( 'NONE',  ( 10.00000000000000000, -35.47612816024506088, -22.48208911017539435 ) ) ;
#1611=VERTEX_POINT ( 'NONE', #59524 ) ;
#1614=VERTEX_POINT ( 'NONE', #42238 ) ;
#1624=VERTEX_POINT ( 'NONE', #42596 ) ;
#1663=AXIS2_PLACEMENT_3D ( 'NONE', #53590, #13727, #36664 ) ;
#1668=CARTESIAN_POINT ( 'NONE',  ( 10.00000000000000000, -22.64427369931191336, 30.00120703465197280 ) ) ;
#1716=LINE ( 'NONE', #13684, #11133 ) ;
#1719=DIRECTION ( 'NONE',  ( 0.000000000000000000, -0.9876883405951361050, -0.1564344650402419989 ) ) ;
#1739=CIRCLE ( 'NONE', #12468, 16.00000000000000000 ) ;
#1745=DIRECTION ( 'NONE',  ( -1.000000000000000000, -0.000000000000000000, 0.000000000000000000 ) ) ;
#1788=AXIS2_PLACEMENT_3D ( 'NONE', #24828, #48138, #59416 ) ;
#1791=CIRCLE ( 'NONE', #11346, 15.99999999999999645 ) ;
#1799=ORIENTED_EDGE ( 'NONE', *, *, #67467, .T. ) ;
#1804=EDGE_CURVE ( 'NONE', #48805, #70509, #59712, .T. ) ;
#1836=VECTOR ( 'NONE', #32453, 1000.000000000000000 ) ;
#1864=CARTESIAN_POINT ( 'NONE',  ( 0.000000000000000000, -16.65560815589383381, -38.55633173627028754 ) ) ;
#1867=DIRECTION ( 'NONE',  ( -1.000000000000000000, 0.000000000000000000, -0.000000000000000000 ) ) ;
#1926=DIRECTION ( 'NONE',  ( -1.000000000000000000, -0.000000000000000000, 0.000000000000000000 ) ) ;
#1930=DIRECTION ( 'NONE',  ( 0.000000000000000000, 0.4539904997395414754, 0.8910065241883706744 ) ) ;
#1942=DIRECTION ( 'NONE',  ( 0.000000000000000000, 0.000000000000000000, 1.000000000000000000 ) ) ;
#1945=CARTESIAN_POINT ( 'NONE',  ( 0.000000000000000000, 0.000000000000000000, 0.000000000000000000 ) ) ;
#1947=DIRECTION ( 'NONE',  ( -1.000000000000000000, -0.000000000000000000, -0.000000000000000000 ) ) ;
#1951=AXIS2_PLACEMENT_3D ( 'NONE', #58393, #74203, #557 ) ;
#2020=AXIS2_PLACEMENT_3D ( 'NONE', #21412, #62039, #10146 ) ;
#2041=DIRECTION ( 'NONE',  ( 0.000000000000000000, 0.000000000000000000, 1.000000000000000000 ) ) ;
#2042=AXIS2_PLACEMENT_3D ( 'NONE', #16207, #62085, #56819 ) ;
#2057=CARTESIAN_POINT ( 'NONE',  ( 10.00000000000000000, 0.000000000000000000, 0.000000000000000000 ) ) ;
#2058=LINE ( 'NONE', #46780, #39113 ) ;
#2059=VERTEX_POINT ( 'NONE', #1584 ) ;
#2070=ORIENTED_EDGE ( 'NONE', *, *, #1144, .T. ) ;
#2072=AXIS2_PLACEMENT_3D ( 'NONE', #41054, #53068, #59448 ) ;
#2081=DIRECTION ( 'NONE',  ( 0.000000000000000000, -1.000000000000000000, -1.040834085586084257E-14 ) ) ;
#2097=CIRCLE ( 'NONE', #858, 16.00000000000000000 ) ;
#2112=CIRCLE ( 'NONE', #74075, 15.99999999999999822 ) ;
#2114=DIRECTION ( 'NONE',  ( 0.000000000000000000, 0.000000000000000000, 1.000000000000000000 ) ) ;
#2137=DIRECTION ( 'NONE',  ( -1.000000000000000000, 0.000000000000000000, 0.000000000000000000 ) ) ;
#2146=CIRCLE ( 'NONE', #66983, 37.49900000000000944 ) ;
#2149=DIRECTION ( 'NONE',  ( 0.000000000000000000, -0.3090169943749349057, -0.9510565162951577500 ) ) ;
#2155=DIRECTION ( 'NONE',  ( 0.000000000000000000, 1.000000000000000000, -9.787530781167598712E-16 ) ) ;
#2162=EDGE_CURVE ( 'NONE', #51113, #46234, #14576, .T. ) ;
#2177=VECTOR ( 'NONE', #62193, 1000.000000000000000 ) ;
#2185=AXIS2_PLACEMENT_3D ( 'NONE', #10980, #22631, #73372 ) ;
#2192=DIRECTION ( 'NONE',  ( 0.000000000000000000, 0.9510565162951521989, 0.3090169943749517256 ) ) ;
#2212=CYLINDRICAL_SURFACE ( 'NONE', #9342, 42.00000000000000000 ) ;
#2248=EDGE_LOOP ( 'NONE', ( #12656, #52522, #7149, #49721 ) ) ;
#2256=DIRECTION ( 'NONE',  ( -1.000000000000000000, 0.000000000000000000, 0.000000000000000000 ) ) ;
#2257=CIRCLE ( 'NONE', #29837, 37.49900000000000233 ) ;
#2267=DIRECTION ( 'NONE',  ( 0.000000000000000000, -0.8090169943749402348, -0.5877852522924830181 ) ) ;
#2268=VERTEX_POINT ( 'NONE', #11986 ) ;
#2283=VECTOR ( 'NONE', #21810, 1000.000000000000000 ) ;
#2299=DIRECTION ( 'NONE',  ( -1.000000000000000000, 0.000000000000000000, 0.000000000000000000 ) ) ;
#2307=DIRECTION ( 'NONE',  ( 0.000000000000000000, 0.5877852522924742473, -0.8090169943749465631 ) ) ;
#2320=VECTOR ( 'NONE', #60550, 1000.000000000000000 ) ;
#2324=ORIENTED_EDGE ( 'NONE', *, *, #13247, .F. ) ;
#2344=EDGE_LOOP ( 'NONE', ( #61508, #36126, #11112, #46149 ) ) ;
#2349=ORIENTED_EDGE ( 'NONE', *, *, #47198, .F. ) ;
#2350=ORIENTED_EDGE ( 'NONE', *, *, #71718, .F. ) ;
#2352=ORIENTED_EDGE ( 'NONE', *, *, #68826, .T. ) ;
#2355=EDGE_CURVE ( 'NONE', #16458, #40253, #71665, .T. ) ;
#2363=ORIENTED_EDGE ( 'NONE', *, *, #5707, .F. ) ;
#2388=DIRECTION ( 'NONE',  ( 0.000000000000000000, 0.000000000000000000, 1.000000000000000000 ) ) ;
#2390=CIRCLE ( 'NONE', #53976, 16.00000000000000000 ) ;
#2395=CIRCLE ( 'NONE', #28739, 16.00000000000000000 ) ;
#2399=VECTOR ( 'NONE', #8785, 1000.000000000000000 ) ;
#2411=DIRECTION ( 'NONE',  ( -1.000000000000000000, -0.000000000000000000, -0.000000000000000000 ) ) ;
#2420=AXIS2_PLACEMENT_3D ( 'NONE', #41593, #25422, #42709 ) ;
#2432=FACE_OUTER_BOUND ( 'NONE', #29237, .T. ) ;
#2438=EDGE_CURVE ( 'NONE', #49630, #38085, #24023, .T. ) ;
#2459=DIRECTION ( 'NONE',  ( -1.000000000000000000, 0.000000000000000000, -0.000000000000000000 ) ) ;
#2526=ORIENTED_EDGE ( 'NONE', *, *, #56990, .F. ) ;
#2543=DIRECTION ( 'NONE',  ( 0.000000000000000000, 0.000000000000000000, 1.000000000000000000 ) ) ;
#2546=ORIENTED_EDGE ( 'NONE', *, *, #16968, .T. ) ;
#2549=ORIENTED_EDGE ( 'NONE', *, *, #36224, .F. ) ;
#2573=ORIENTED_EDGE ( 'NONE', *, *, #28192, .T. ) ;
#2575=CARTESIAN_POINT ( 'NONE',  ( 0.000000000000000000, 0.000000000000000000, 0.000000000000000000 ) ) ;
#2578=ORIENTED_EDGE ( 'NONE', *, *, #34614, .T. ) ;
#2581=VERTEX_POINT ( 'NONE', #32601 ) ;
#2593=CARTESIAN_POINT ( 'NONE',  ( 0.000000000000000000, 0.000000000000000000, 0.000000000000000000 ) ) ;
#2598=DIRECTION ( 'NONE',  ( 0.000000000000000000, 0.000000000000000000, 1.000000000000000000 ) ) ;
#2620=VERTEX_POINT ( 'NONE', #66824 ) ;
#2640=VECTOR ( 'NONE', #25446, 1000.000000000000000 ) ;
#2646=ORIENTED_EDGE ( 'NONE', *, *, #28659, .T. ) ;
#2649=ORIENTED_EDGE ( 'NONE', *, *, #67729, .T. ) ;
#2674=DIRECTION ( 'NONE',  ( -1.000000000000000000, 0.000000000000000000, 0.000000000000000000 ) ) ;
#2680=FACE_OUTER_BOUND ( 'NONE', #5977, .T. ) ;
#2698=VECTOR ( 'NONE', #10737, 1000.000000000000000 ) ;
#2700=DIRECTION ( 'NONE',  ( 0.000000000000000000, 0.000000000000000000, 1.000000000000000000 ) ) ;
#2704=CARTESIAN_POINT ( 'NONE',  ( 10.00000000000000000, 0.000000000000000000, 0.000000000000000000 ) ) ;
#2718=ORIENTED_EDGE ( 'NONE', *, *, #19405, .F. ) ;
#2736=AXIS2_PLACEMENT_3D ( 'NONE', #604, #34398, #11468 ) ;
#2738=ORIENTED_EDGE ( 'NONE', *, *, #40000, .T. ) ;
#2761=DIRECTION ( 'NONE',  ( 0.000000000000000000, -0.3090169943749349057, -0.9510565162951576390 ) ) ;
#2781=CARTESIAN_POINT ( 'NONE',  ( 10.00000000000000000, -35.38097989696503021, -12.42422080174676147 ) ) ;
#2783=EDGE_CURVE ( 'NONE', #20472, #61501, #4829, .T. ) ;
#2821=LINE ( 'NONE', #26077, #61572 ) ;
#2825=CARTESIAN_POINT ( 'NONE',  ( 10.00000000000000000, -10.96151621346461447, -35.95386929396268272 ) ) ;
#2826=CARTESIAN_POINT ( 'NONE',  ( 10.00000000000000000, -37.01155633439053361, -6.555932627142825986 ) ) ;
#2839=CARTESIAN_POINT ( 'NONE',  ( 0.000000000000000000, 37.48860685352291000, 0.8828120875901893649 ) ) ;
#2853=EDGE_CURVE ( 'NONE', #60113, #31095, #1004, .T. ) ;
#2874=CARTESIAN_POINT ( 'NONE',  ( 0.000000000000000000, 0.000000000000000000, 0.000000000000000000 ) ) ;
#2886=PLANE ( 'NONE',  #28775 ) ;
#2892=CARTESIAN_POINT ( 'NONE',  ( -3.308722450212110699E-21, 16.95692799528845995, 2.500000000000000000 ) ) ;
#2897=EDGE_CURVE ( 'NONE', #13869, #2268, #63387, .T. ) ;
#2914=ORIENTED_EDGE ( 'NONE', *, *, #45284, .F. ) ;
#2933=EDGE_CURVE ( 'NONE', #58686, #41070, #14135, .T. ) ;
#2942=EDGE_CURVE ( 'NONE', #52264, #37092, #28870, .T. ) ;
#2945=DIRECTION ( 'NONE',  ( 0.000000000000000000, -0.7071067811865389130, -0.7071067811865563435 ) ) ;
#2948=CYLINDRICAL_SURFACE ( 'NONE', #18202, 16.00000000000000000 ) ;
#2951=CARTESIAN_POINT ( 'NONE',  ( 10.00000000000000000, 15.48615015657582283, 39.04073710021349797 ) ) ;
#2960=AXIS2_PLACEMENT_3D ( 'NONE', #15954, #56181, #74209 ) ;
#2965=CIRCLE ( 'NONE', #28157, 42.00000000000000000 ) ;
#2970=AXIS2_PLACEMENT_3D ( 'NONE', #7042, #29969, #47639 ) ;
#2975=CARTESIAN_POINT ( 'NONE',  ( 0.000000000000000000, -6.555932627142676772, 37.01155633439056203 ) ) ;
#3007=EDGE_LOOP ( 'NONE', ( #3845, #52907, #63616, #71587 ) ) ;
#3016=EDGE_CURVE ( 'NONE', #48031, #70536, #36961, .T. ) ;
#3026=LINE ( 'NONE', #19898, #60294 ) ;
#3046=AXIS2_PLACEMENT_3D ( 'NONE', #8883, #8523, #25436 ) ;
#3061=CARTESIAN_POINT ( 'NONE',  ( 0.000000000000000000, 0.000000000000000000, 0.000000000000000000 ) ) ;
#3075=ADVANCED_FACE ( 'NONE', ( #59291 ), #7784, .T. ) ;
#3077=ORIENTED_EDGE ( 'NONE', *, *, #17757, .F. ) ;
#3084=DIRECTION ( 'NONE',  ( -1.000000000000000000, 0.000000000000000000, 0.000000000000000000 ) ) ;
#3087=EDGE_CURVE ( 'NONE', #19149, #56343, #52163, .T. ) ;
#3104=VERTEX_POINT ( 'NONE', #708 ) ;
#3121=CARTESIAN_POINT ( 'NONE',  ( 10.00000000000000000, -33.00180498840035170, -17.80606268964575278 ) ) ;
#3132=CARTESIAN_POINT ( 'NONE',  ( 0.000000000000000000, -37.01155633439063308, 6.555932627142289526 ) ) ;
#3146=DIRECTION ( 'NONE',  ( 0.000000000000000000, 0.000000000000000000, 1.000000000000000000 ) ) ;
#3159=ADVANCED_FACE ( 'NONE', ( #6678 ), #52528, .T. ) ;
#3167=VERTEX_POINT ( 'NONE', #12676 ) ;
#3174=CARTESIAN_POINT ( 'NONE',  ( 5.000000000000000000, -15.48615015657555993, -39.04073710021360455 ) ) ;
#3185=DIRECTION ( 'NONE',  ( 1.000000000000000000, -0.000000000000000000, -0.000000000000000000 ) ) ;
#3193=ADVANCED_FACE ( 'NONE', ( #25073 ), #72408, .T. ) ;
#3194=ORIENTED_EDGE ( 'NONE', *, *, #57075, .T. ) ;
#3209=CLOSED_SHELL ( 'NONE', ( #57203, #31036, #20088, #28833, #54894, #49126, #28029, #28766, #34130, #28070, #26735, #5093, #10361, #1314, #15329, #69939, #39757, #67651, #38725, #66344, #58630, #67974, #5871, #34646, #53935, #15977, #72459, #48983, #48808, #1509, #1229, #10961, #55057, #45402, #28792, #8383, #13223, #27732, #22656, #11603, #12155, #69842, #9923, #19792, #43645, #43497, #34918, #13086, #59323, #3075, #30479, #70400, #55004, #8997, #17002, #48617, #31552, #37795, #31221, #73056, #44118, #8487, #72637, #25954, #54931, #57492, #4868, #39139, #17323, #54320, #33477, #37552, #57875, #71129, #45958, #33810, #36988, #38884, #55455, #32575, #11870, #64124, #3193, #39458, #68778, #59976, #39116, #5385, #36936, #16895, #48040, #28760, #6559, #43113, #64786, #11704, #20603, #53300, #50223, #39582, #18254, #61298, #64041, #7399, #27915, #25603, #37438, #24431, #24115, #54898, #19929, #30535, #20534, #1007, #50604, #30656, #21228, #18391, #27564, #66804, #13799, #36325, #39120, #12156, #5998, #14452, #34425, #4456, #21969, #71548, #30441, #9937, #57400, #32843, #6874, #58909, #38559, #8844, #27650, #71267, #3159, #11771, #28261, #18653, #44166, #41118, #61530, #14606, #22687, #65133, #36503, #18074, #47696, #60215, #33068, #11241, #34617, #40472, #74064, #62990, #19518, #23118, #8432, #16182, #640, #4532, #50256, #69252, #49760, #27514, #44918, #20862, #64105 ) ) ;
#3225=CARTESIAN_POINT ( 'NONE',  ( 0.000000000000000000, 40.68715046381927891, 10.41901085202092858 ) ) ;
#3227=CIRCLE ( 'NONE', #30751, 16.00000000000000000 ) ;
#3244=EDGE_CURVE ( 'NONE', #56046, #13831, #62250, .T. ) ;
#3277=EDGE_CURVE ( 'NONE', #8216, #44755, #45467, .T. ) ;
#3293=DIRECTION ( 'NONE',  ( 0.000000000000000000, -0.5877852522924802425, 0.8090169943749422332 ) ) ;
#3302=ORIENTED_EDGE ( 'NONE', *, *, #8745, .T. ) ;
#3318=LINE ( 'NONE', #48409, #55252 ) ;
#3325=VECTOR ( 'NONE', #22983, 1000.000000000000000 ) ;
#3327=EDGE_CURVE ( 'NONE', #52875, #6755, #27398, .T. ) ;
#3331=LINE ( 'NONE', #42787, #3611 ) ;
#3334=DIRECTION ( 'NONE',  ( 1.000000000000000000, 0.000000000000000000, 0.000000000000000000 ) ) ;
#3342=DIRECTION ( 'NONE',  ( 0.000000000000000000, 0.8090169943749447867, 0.5877852522924769119 ) ) ;
#3370=CARTESIAN_POINT ( 'NONE',  ( 0.000000000000000000, -41.91543099594819921, 2.663952781846001816 ) ) ;
#3379=DIRECTION ( 'NONE',  ( 0.000000000000000000, 0.9876883405951382144, -0.1564344650402276493 ) ) ;
#3392=CARTESIAN_POINT ( 'NONE',  ( 10.00000000000000000, 27.05870788708231700, 26.08949754953034272 ) ) ;
#3393=CIRCLE ( 'NONE', #35763, 42.00000000000000000 ) ;
#3399=CIRCLE ( 'NONE', #18982, 37.49900000000000233 ) ;
#3417=VECTOR ( 'NONE', #56473, 1000.000000000000000 ) ;
#3436=AXIS2_PLACEMENT_3D ( 'NONE', #73311, #3084, #21823 ) ;
#3439=AXIS2_PLACEMENT_3D ( 'NONE', #55501, #14153, #61149 ) ;
#3441=AXIS2_PLACEMENT_3D ( 'NONE', #58800, #70422, #64445 ) ;
#3474=DIRECTION ( 'NONE',  ( 1.000000000000000000, -0.000000000000000000, -0.000000000000000000 ) ) ;
#3477=ORIENTED_EDGE ( 'NONE', *, *, #11438, .T. ) ;
#3492=CARTESIAN_POINT ( 'NONE',  ( 0.000000000000000000, 12.26510123303259725, 35.53030884539089840 ) ) ;
#3508=CYLINDRICAL_SURFACE ( 'NONE', #41890, 16.00000000000000000 ) ;
#3514=EDGE_CURVE ( 'NONE', #12638, #64991, #4384, .T. ) ;
#3523=AXIS2_PLACEMENT_3D ( 'NONE', #3775, #72529, #21033 ) ;
#3535=EDGE_LOOP ( 'NONE', ( #35759, #37357, #71112, #37446 ) ) ;
#3556=CIRCLE ( 'NONE', #29919, 16.00000000000000711 ) ;
#3570=DIRECTION ( 'NONE',  ( -1.000000000000000000, -0.000000000000000000, -0.000000000000000000 ) ) ;
#3576=CYLINDRICAL_SURFACE ( 'NONE', #66928, 12.50000000000000000 ) ;
#3594=AXIS2_PLACEMENT_3D ( 'NONE', #45396, #32971, #39006 ) ;
#3609=DIRECTION ( 'NONE',  ( -1.000000000000000000, 0.000000000000000000, 0.000000000000000000 ) ) ;
#3610=AXIS2_PLACEMENT_3D ( 'NONE', #57742, #62274, #57006 ) ;
#3611=VECTOR ( 'NONE', #3700, 1000.000000000000000 ) ;
#3630=CIRCLE ( 'NONE', #25192, 15.99999999999999822 ) ;
#3638=CARTESIAN_POINT ( 'NONE',  ( 4.999999999999999112, -41.91543099594819921, 2.663952781846001816 ) ) ;
#3664=EDGE_CURVE ( 'NONE', #39943, #70504, #14551, .T. ) ;
#3687=CYLINDRICAL_SURFACE ( 'NONE', #44428, 42.00000000000000000 ) ;
#3700=DIRECTION ( 'NONE',  ( -1.000000000000000000, 0.000000000000000000, 0.000000000000000000 ) ) ;
#3706=CIRCLE ( 'NONE', #13286, 37.49900000000000233 ) ;
#3723=DIRECTION ( 'NONE',  ( 0.000000000000000000, -0.9876883405951393247, 0.1564344650402207104 ) ) ;
#3727=DIRECTION ( 'NONE',  ( 0.000000000000000000, 0.5877852522924684742, 0.8090169943749506709 ) ) ;
#3729=DIRECTION ( 'NONE',  ( -1.000000000000000000, 0.000000000000000000, -0.000000000000000000 ) ) ;
#3738=DIRECTION ( 'NONE',  ( 0.000000000000000000, 0.000000000000000000, 1.000000000000000000 ) ) ;
#3752=DIRECTION ( 'NONE',  ( 0.000000000000000000, 0.000000000000000000, -1.000000000000000000 ) ) ;
#3753=CARTESIAN_POINT ( 'NONE',  ( 10.00000000000000000, 35.53030884539084866, 12.26510123303271982 ) ) ;
#3754=DIRECTION ( 'NONE',  ( -1.000000000000000000, -0.000000000000000000, -0.000000000000000000 ) ) ;
#3774=CYLINDRICAL_SURFACE ( 'NONE', #65297, 37.49900000000000233 ) ;
#3775=CARTESIAN_POINT ( 'NONE',  ( 10.00000000000000000, -6.555932627142143865, -37.01155633439065440 ) ) ;
#3824=EDGE_CURVE ( 'NONE', #44376, #71645, #71578, .T. ) ;
#3837=LINE ( 'NONE', #66964, #44023 ) ;
#3841=CIRCLE ( 'NONE', #45866, 42.00000000000000000 ) ;
#3845=ORIENTED_EDGE ( 'NONE', *, *, #52508, .T. ) ;
#3856=VERTEX_POINT ( 'NONE', #50117 ) ;
#3857=EDGE_CURVE ( 'NONE', #62068, #11372, #21743, .T. ) ;
#3864=CIRCLE ( 'NONE', #13445, 42.00000000000000000 ) ;
#3877=CARTESIAN_POINT ( 'NONE',  ( 0.000000000000000000, 10.96151621346540317, -35.95386929396244113 ) ) ;
#3900=AXIS2_PLACEMENT_3D ( 'NONE', #42745, #48748, #2192 ) ;
#3901=ORIENTED_EDGE ( 'NONE', *, *, #28803, .F. ) ;
#3926=ORIENTED_EDGE ( 'NONE', *, *, #20561, .F. ) ;
#3970=CYLINDRICAL_SURFACE ( 'NONE', #59384, 16.00000000000000000 ) ;
#3982=ORIENTED_EDGE ( 'NONE', *, *, #17730, .F. ) ;
#3993=ORIENTED_EDGE ( 'NONE', *, *, #22530, .T. ) ;
#4011=VERTEX_POINT ( 'NONE', #29057 ) ;
#4023=AXIS2_PLACEMENT_3D ( 'NONE', #47173, #57720, #70084 ) ;
#4024=DIRECTION ( 'NONE',  ( -1.000000000000000000, 0.000000000000000000, -0.000000000000000000 ) ) ;
#4043=EDGE_CURVE ( 'NONE', #29886, #68784, #43456, .T. ) ;
#4095=ORIENTED_EDGE ( 'NONE', *, *, #28169, .T. ) ;
#4109=CARTESIAN_POINT ( 'NONE',  ( 10.00000000000000000, 12.26510123303259725, 35.53030884539089840 ) ) ;
#4115=EDGE_CURVE ( 'NONE', #70536, #73020, #8594, .T. ) ;
#4117=EDGE_CURVE ( 'NONE', #2620, #56468, #28682, .T. ) ;
#4123=ORIENTED_EDGE ( 'NONE', *, *, #3244, .F. ) ;
#4126=DIRECTION ( 'NONE',  ( -1.000000000000000000, 0.000000000000000000, -0.000000000000000000 ) ) ;
#4140=AXIS2_PLACEMENT_3D ( 'NONE', #59967, #66700, #15565 ) ;
#4158=CARTESIAN_POINT ( 'NONE',  ( 10.00000000000000000, -37.58145647212455032, 16.68533520207890319 ) ) ;
#4160=CARTESIAN_POINT ( 'NONE',  ( 0.000000000000000000, 38.55633173627010279, 16.65560815589424593 ) ) ;
#4164=VECTOR ( 'NONE', #12813, 1000.000000000000000 ) ;
#4165=ORIENTED_EDGE ( 'NONE', *, *, #22883, .T. ) ;
#4182=DIRECTION ( 'NONE',  ( 0.000000000000000000, -0.9876883405951358830, -0.1564344650402420822 ) ) ;
#4183=AXIS2_PLACEMENT_3D ( 'NONE', #59354, #30027, #29647 ) ;
#4190=ORIENTED_EDGE ( 'NONE', *, *, #65389, .F. ) ;
#4195=ORIENTED_EDGE ( 'NONE', *, *, #45143, .F. ) ;
#4206=ORIENTED_EDGE ( 'NONE', *, *, #70890, .F. ) ;
#4242=CARTESIAN_POINT ( 'NONE',  ( 10.00000000000000000, -5.202137450156129717, -37.22597642581163768 ) ) ;
#4253=ORIENTED_EDGE ( 'NONE', *, *, #70967, .T. ) ;
#4267=ORIENTED_EDGE ( 'NONE', *, *, #23102, .T. ) ;
#4277=ORIENTED_EDGE ( 'NONE', *, *, #42626, .F. ) ;
#4289=CIRCLE ( 'NONE', #22302, 37.49900000000000944 ) ;
#4299=ORIENTED_EDGE ( 'NONE', *, *, #15009, .F. ) ;
#4312=VERTEX_POINT ( 'NONE', #22222 ) ;
#4320=DIRECTION ( 'NONE',  ( -1.000000000000000000, 0.000000000000000000, -0.000000000000000000 ) ) ;
#4333=ORIENTED_EDGE ( 'NONE', *, *, #17757, .T. ) ;
#4351=VERTEX_POINT ( 'NONE', #34607 ) ;
#4354=CARTESIAN_POINT ( 'NONE',  ( 0.000000000000000000, 0.000000000000000000, 0.000000000000000000 ) ) ;
#4363=EDGE_LOOP ( 'NONE', ( #18841, #70340, #60405, #40949 ) ) ;
#4368=DIRECTION ( 'NONE',  ( 0.000000000000000000, 0.000000000000000000, 1.000000000000000000 ) ) ;
#4383=AXIS2_PLACEMENT_3D ( 'NONE', #36541, #59488, #20736 ) ;
#4384=LINE ( 'NONE', #62648, #33767 ) ;
#4405=CARTESIAN_POINT ( 'NONE',  ( 10.00000000000000000, 38.55633173627010990, 16.65560815589424593 ) ) ;
#4413=CARTESIAN_POINT ( 'NONE',  ( 10.00000000000000000, 0.9569279952884557350, -2.499999999999984457 ) ) ;
#4448=FACE_OUTER_BOUND ( 'NONE', #26548, .T. ) ;
#4456=ADVANCED_FACE ( 'NONE', ( #6065 ), #35708, .T. ) ;
#4466=DIRECTION ( 'NONE',  ( 0.000000000000000000, 0.3090169943749412340, 0.9510565162951556406 ) ) ;
#4476=CARTESIAN_POINT ( 'NONE',  ( 0.000000000000000000, 0.000000000000000000, 0.000000000000000000 ) ) ;
#4484=ORIENTED_EDGE ( 'NONE', *, *, #3277, .T. ) ;
#4497=AXIS2_PLACEMENT_3D ( 'NONE', #65055, #41729, #25549 ) ;
#4507=DIRECTION ( 'NONE',  ( -1.000000000000000000, 0.000000000000000000, 0.000000000000000000 ) ) ;
#4512=DIRECTION ( 'NONE',  ( 0.000000000000000000, 0.000000000000000000, 1.000000000000000000 ) ) ;
#4515=DIRECTION ( 'NONE',  ( 0.000000000000000000, 0.9510565162951523099, 0.3090169943749517811 ) ) ;
#4529=VERTEX_POINT ( 'NONE', #70652 ) ;
#4530=EDGE_CURVE ( 'NONE', #68973, #52875, #3026, .T. ) ;
#4532=ADVANCED_FACE ( 'NONE', ( #7157 ), #13528, .T. ) ;
#4533=CARTESIAN_POINT ( 'NONE',  ( 0.000000000000000000, 0.8828120875905820508, -37.48860685352290290 ) ) ;
#4549=ORIENTED_EDGE ( 'NONE', *, *, #28533, .F. ) ;
#4562=EDGE_LOOP ( 'NONE', ( #37373, #61114, #9038, #63480 ) ) ;
#4564=ORIENTED_EDGE ( 'NONE', *, *, #35656, .F. ) ;
#4565=AXIS2_PLACEMENT_3D ( 'NONE', #45059, #16479, #56721 ) ;
#4586=VERTEX_POINT ( 'NONE', #20272 ) ;
#4599=AXIS2_PLACEMENT_3D ( 'NONE', #42041, #64977, #13455 ) ;
#4604=DIRECTION ( 'NONE',  ( -1.000000000000000000, -0.000000000000000000, -0.000000000000000000 ) ) ;
#4606=LINE ( 'NONE', #9852, #48955 ) ;
#4631=EDGE_CURVE ( 'NONE', #21975, #60113, #59039, .T. ) ;
#4633=DIRECTION ( 'NONE',  ( -1.000000000000000000, 0.000000000000000000, 0.000000000000000000 ) ) ;
#4638=ORIENTED_EDGE ( 'NONE', *, *, #34806, .T. ) ;
#4641=CARTESIAN_POINT ( 'NONE',  ( 4.999999999999999112, 40.98264845739763018, -9.188173127306860977 ) ) ;
#4650=EDGE_LOOP ( 'NONE', ( #11852, #64157, #68463, #41870 ) ) ;
#4686=DIRECTION ( 'NONE',  ( -1.000000000000000000, -0.000000000000000000, -0.000000000000000000 ) ) ;
#4699=DIRECTION ( 'NONE',  ( 0.000000000000000000, 0.000000000000000000, 1.000000000000000000 ) ) ;
#4713=CARTESIAN_POINT ( 'NONE',  ( 10.00000000000000000, 0.000000000000000000, 0.000000000000000000 ) ) ;
#4715=CARTESIAN_POINT ( 'NONE',  ( 10.00000000000000000, -0.8828120875898013420, -37.48860685352291711 ) ) ;
#4729=VECTOR ( 'NONE', #50882, 1000.000000000000000 ) ;
#4732=ORIENTED_EDGE ( 'NONE', *, *, #8407, .T. ) ;
#4748=CARTESIAN_POINT ( 'NONE',  ( 10.00000000000000000, -27.13269053701114331, 25.88420570971391754 ) ) ;
#4756=ORIENTED_EDGE ( 'NONE', *, *, #4117, .T. ) ;
#4775=ORIENTED_EDGE ( 'NONE', *, *, #9395, .F. ) ;
#4783=CARTESIAN_POINT ( 'NONE',  ( 5.000000000000000000, -26.79245525562690844, -32.34446384430000876 ) ) ;
#4786=ORIENTED_EDGE ( 'NONE', *, *, #5636, .T. ) ;
#4790=EDGE_CURVE ( 'NONE', #54282, #37558, #36228, .T. ) ;
#4796=DIRECTION ( 'NONE',  ( -1.000000000000000000, -0.000000000000000000, -0.000000000000000000 ) ) ;
#4798=DIRECTION ( 'NONE',  ( 1.000000000000000000, -0.000000000000000000, 0.000000000000000000 ) ) ;
#4802=DIRECTION ( 'NONE',  ( 1.000000000000000000, 0.000000000000000000, 0.000000000000000000 ) ) ;
#4807=VERTEX_POINT ( 'NONE', #27017 ) ;
#4819=CIRCLE ( 'NONE', #48049, 42.00000000000000000 ) ;
#4829=CIRCLE ( 'NONE', #24027, 16.00000000000000000 ) ;
#4834=AXIS2_PLACEMENT_3D ( 'NONE', #13457, #6716, #40938 ) ;
#4837=CIRCLE ( 'NONE', #13229, 37.49900000000000233 ) ;
#4839=CARTESIAN_POINT ( 'NONE',  ( 0.000000000000000000, -15.48615015657610527, 39.04073710021338428 ) ) ;
#4868=ADVANCED_FACE ( 'NONE', ( #29241 ), #62763, .T. ) ;
#4889=EDGE_CURVE ( 'NONE', #24772, #16853, #3841, .T. ) ;
#4897=CARTESIAN_POINT ( 'NONE',  ( 10.00000000000000000, 0.000000000000000000, 0.000000000000000000 ) ) ;
#4940=EDGE_LOOP ( 'NONE', ( #47533, #47636, #13608, #32918 ) ) ;
#4944=ORIENTED_EDGE ( 'NONE', *, *, #60867, .T. ) ;
#4961=LINE ( 'NONE', #21854, #11881 ) ;
#5039=ORIENTED_EDGE ( 'NONE', *, *, #64663, .T. ) ;
#5077=CARTESIAN_POINT ( 'NONE',  ( 10.00000000000000000, 27.13269053701096922, 25.88420570971410228 ) ) ;
#5084=CIRCLE ( 'NONE', #42317, 37.49900000000000233 ) ;
#5093=ADVANCED_FACE ( 'NONE', ( #20476 ), #32109, .T. ) ;
#5141=ORIENTED_EDGE ( 'NONE', *, *, #30022, .T. ) ;
#5148=CARTESIAN_POINT ( 'NONE',  ( 10.00000000000000000, 0.000000000000000000, 0.000000000000000000 ) ) ;
#5160=CYLINDRICAL_SURFACE ( 'NONE', #22035, 16.00000000000000000 ) ;
#5166=DIRECTION ( 'NONE',  ( 0.000000000000000000, 0.000000000000000000, -1.000000000000000000 ) ) ;
#5187=ORIENTED_EDGE ( 'NONE', *, *, #5789, .T. ) ;
#5219=EDGE_CURVE ( 'NONE', #5960, #20594, #9103, .T. ) ;
#5230=ORIENTED_EDGE ( 'NONE', *, *, #11316, .F. ) ;
#5247=CARTESIAN_POINT ( 'NONE',  ( 10.00000000000000000, 27.13269053701132094, -25.88420570971372570 ) ) ;
#5270=LINE ( 'NONE', #39092, #21522 ) ;
#5271=CARTESIAN_POINT ( 'NONE',  ( 10.00000000000000000, 0.000000000000000000, 0.000000000000000000 ) ) ;
#5330=AXIS2_PLACEMENT_3D ( 'NONE', #10273, #56525, #38483 ) ;
#5351=AXIS2_PLACEMENT_3D ( 'NONE', #5575, #22860, #334 ) ;
#5354=CARTESIAN_POINT ( 'NONE',  ( 0.000000000000000000, -35.53030884539077050, -12.26510123303296851 ) ) ;
#5369=AXIS2_PLACEMENT_3D ( 'NONE', #34199, #68430, #67675 ) ;
#5385=ADVANCED_FACE ( 'NONE', ( #58016 ), #41833, .T. ) ;
#5387=ORIENTED_EDGE ( 'NONE', *, *, #34446, .T. ) ;
#5392=ORIENTED_EDGE ( 'NONE', *, *, #55365, .F. ) ;
#5393=ORIENTED_EDGE ( 'NONE', *, *, #47773, .F. ) ;
#5409=ORIENTED_EDGE ( 'NONE', *, *, #34014, .F. ) ;
#5412=ORIENTED_EDGE ( 'NONE', *, *, #1804, .F. ) ;
#5462=VECTOR ( 'NONE', #21281, 1000.000000000000000 ) ;
#5486=DIRECTION ( 'NONE',  ( -1.000000000000000000, 0.000000000000000000, -0.000000000000000000 ) ) ;
#5505=DIRECTION ( 'NONE',  ( -1.000000000000000000, 0.000000000000000000, -0.000000000000000000 ) ) ;
#5512=CARTESIAN_POINT ( 'NONE',  ( 10.00000000000000000, 5.202137450156907761, -37.22597642581151689 ) ) ;
#5527=DIRECTION ( 'NONE',  ( -1.000000000000000000, -0.000000000000000000, 0.000000000000000000 ) ) ;
#5535=CARTESIAN_POINT ( 'NONE',  ( 10.00000000000000000, 0.000000000000000000, 0.000000000000000000 ) ) ;
#5537=AXIS2_PLACEMENT_3D ( 'NONE', #54589, #44053, #15093 ) ;
#5542=EDGE_LOOP ( 'NONE', ( #1153, #37017, #56985, #63447 ) ) ;
#5551=DIRECTION ( 'NONE',  ( 0.000000000000000000, 6.938893903907229364E-16, 1.000000000000000000 ) ) ;
#5555=DIRECTION ( 'NONE',  ( 0.000000000000000000, 0.9876883405951372152, 0.1564344650402346160 ) ) ;
#5562=DIRECTION ( 'NONE',  ( 0.000000000000000000, 0.000000000000000000, 1.000000000000000000 ) ) ;
#5575=CARTESIAN_POINT ( 'NONE',  ( 10.00000000000000000, -37.22597642581161637, 5.202137450156258502 ) ) ;
#5581=EDGE_LOOP ( 'NONE', ( #28125, #2649, #2352, #53451 ) ) ;
#5590=DIRECTION ( 'NONE',  ( -1.000000000000000000, 0.000000000000000000, 0.000000000000000000 ) ) ;
#5636=EDGE_CURVE ( 'NONE', #55462, #1624, #68483, .T. ) ;
#5660=ORIENTED_EDGE ( 'NONE', *, *, #66600, .F. ) ;
#5663=CARTESIAN_POINT ( 'NONE',  ( 0.000000000000000000, 10.74501242461282757, 35.92658777277515014 ) ) ;
#5683=ORIENTED_EDGE ( 'NONE', *, *, #38523, .T. ) ;
#5698=AXIS2_PLACEMENT_3D ( 'NONE', #11176, #33349, #63079 ) ;
#5707=EDGE_CURVE ( 'NONE', #26180, #9139, #33883, .T. ) ;
#5713=CARTESIAN_POINT ( 'NONE',  ( 0.000000000000000000, -21.40280677340398086, 36.13751322684410638 ) ) ;
#5742=VERTEX_POINT ( 'NONE', #22989 ) ;
#5754=LINE ( 'NONE', #39215, #37181 ) ;
#5770=VERTEX_POINT ( 'NONE', #28601 ) ;
#5775=CARTESIAN_POINT ( 'NONE',  ( 10.00000000000000000, -33.00180498840035170, -17.80606268964575278 ) ) ;
#5777=CARTESIAN_POINT ( 'NONE',  ( 10.00000000000000000, -21.32104025579135964, 30.84782396557210760 ) ) ;
#5781=AXIS2_PLACEMENT_3D ( 'NONE', #63399, #27694, #50618 ) ;
#5787=LINE ( 'NONE', #28691, #35863 ) ;
#5789=EDGE_CURVE ( 'NONE', #37324, #18341, #52284, .T. ) ;
#5822=CARTESIAN_POINT ( 'NONE',  ( 10.00000000000000000, -35.38097989696503021, -12.42422080174676147 ) ) ;
#5827=AXIS2_PLACEMENT_3D ( 'NONE', #24687, #47998, #65296 ) ;
#5861=CYLINDRICAL_SURFACE ( 'NONE', #67441, 37.49900000000000233 ) ;
#5865=AXIS2_PLACEMENT_3D ( 'NONE', #51849, #63887, #34934 ) ;
#5871=ADVANCED_FACE ( 'NONE', ( #12793 ), #57935, .T. ) ;
#5872=CARTESIAN_POINT ( 'NONE',  ( -1.200000000000000030E-05, 0.9569279952884607310, 2.500000000000015543 ) ) ;
#5877=CARTESIAN_POINT ( 'NONE',  ( 10.00000000000000000, 37.22597642581158084, -5.202137450156524068 ) ) ;
#5898=DIRECTION ( 'NONE',  ( 0.000000000000000000, 0.000000000000000000, 1.000000000000000000 ) ) ;
#5899=CARTESIAN_POINT ( 'NONE',  ( 0.000000000000000000, -4.992566952385247170, 37.16516213103275845 ) ) ;
#5916=ORIENTED_EDGE ( 'NONE', *, *, #36345, .F. ) ;
#5921=CARTESIAN_POINT ( 'NONE',  ( 0.000000000000000000, 0.000000000000000000, 0.000000000000000000 ) ) ;
#5957=DIRECTION ( 'NONE',  ( -1.000000000000000000, -0.000000000000000000, 0.000000000000000000 ) ) ;
#5960=VERTEX_POINT ( 'NONE', #59048 ) ;
#5977=EDGE_LOOP ( 'NONE', ( #69618, #51795, #56041, #23463 ) ) ;
#5980=ORIENTED_EDGE ( 'NONE', *, *, #27683, .F. ) ;
#5998=ADVANCED_FACE ( 'NONE', ( #65064 ), #36465, .T. ) ;
#6015=AXIS2_PLACEMENT_3D ( 'NONE', #61793, #15919, #62159 ) ;
#6065=FACE_OUTER_BOUND ( 'NONE', #16174, .T. ) ;
#6066=EDGE_CURVE ( 'NONE', #53345, #51292, #55616, .T. ) ;
#6075=AXIS2_PLACEMENT_3D ( 'NONE', #58626, #34584, #46246 ) ;
#6081=CARTESIAN_POINT ( 'NONE',  ( -10.00000000000000000, 0.000000000000000000, 0.000000000000000000 ) ) ;
#6094=DIRECTION ( 'NONE',  ( -1.000000000000000000, 0.000000000000000000, 0.000000000000000000 ) ) ;
#6097=LINE ( 'NONE', #63612, #28139 ) ;
#6108=ORIENTED_EDGE ( 'NONE', *, *, #15242, .F. ) ;
#6113=CARTESIAN_POINT ( 'NONE',  ( 4.999999999999999112, 40.68715046381943523, -10.41901085202036370 ) ) ;
#6116=DIRECTION ( 'NONE',  ( -1.000000000000000000, -0.000000000000000000, -0.000000000000000000 ) ) ;
#6131=ORIENTED_EDGE ( 'NONE', *, *, #17745, .F. ) ;
#6141=CARTESIAN_POINT ( 'NONE',  ( 10.00000000000000000, 0.000000000000000000, 0.000000000000000000 ) ) ;
#6170=DIRECTION ( 'NONE',  ( -1.000000000000000000, 0.000000000000000000, 0.000000000000000000 ) ) ;
#6206=EDGE_CURVE ( 'NONE', #37368, #3856, #61635, .T. ) ;
#6233=ORIENTED_EDGE ( 'NONE', *, *, #39, .T. ) ;
#6260=LINE ( 'NONE', #22429, #28685 ) ;
#6264=CYLINDRICAL_SURFACE ( 'NONE', #66469, 37.49900000000000233 ) ;
#6272=CARTESIAN_POINT ( 'NONE',  ( 10.00000000000000000, 0.000000000000000000, 0.000000000000000000 ) ) ;
#6308=CARTESIAN_POINT ( 'NONE',  ( 10.00000000000000000, 30.80686688397010542, 21.53537804866092387 ) ) ;
#6325=CYLINDRICAL_SURFACE ( 'NONE', #35017, 37.49900000000000233 ) ;
#6330=CIRCLE ( 'NONE', #59130, 42.00000000000000000 ) ;
#6378=EDGE_CURVE ( 'NONE', #60507, #66693, #45293, .T. ) ;
#6383=CYLINDRICAL_SURFACE ( 'NONE', #43794, 37.49900000000000233 ) ;
#6409=ORIENTED_EDGE ( 'NONE', *, *, #46294, .F. ) ;
#6419=ORIENTED_EDGE ( 'NONE', *, *, #40593, .F. ) ;
#6433=CARTESIAN_POINT ( 'NONE',  ( 10.00000000000000000, 0.000000000000000000, 0.000000000000000000 ) ) ;
#6437=CARTESIAN_POINT ( 'NONE',  ( 10.00000000000000000, -37.58145647212455032, 0.6853352020789044152 ) ) ;
#6444=DIRECTION ( 'NONE',  ( 0.000000000000000000, -0.7071067811865536790, 0.7071067811865413555 ) ) ;
#6463=VERTEX_POINT ( 'NONE', #59696 ) ;
#6464=DIRECTION ( 'NONE',  ( 1.000000000000000000, 0.000000000000000000, 0.000000000000000000 ) ) ;
#6488=VERTEX_POINT ( 'NONE', #2951 ) ;
#6514=FACE_OUTER_BOUND ( 'NONE', #21357, .T. ) ;
#6526=DIRECTION ( 'NONE',  ( 0.000000000000000000, 0.000000000000000000, 1.000000000000000000 ) ) ;
#6559=ADVANCED_FACE ( 'NONE', ( #32210 ), #20940, .T. ) ;
#6569=VERTEX_POINT ( 'NONE', #16046 ) ;
#6579=VERTEX_POINT ( 'NONE', #26946 ) ;
#6585=CARTESIAN_POINT ( 'NONE',  ( 10.00000000000000000, 0.000000000000000000, 0.000000000000000000 ) ) ;
#6588=CARTESIAN_POINT ( 'NONE',  ( 10.00000000000000000, -27.05870788708250885, 26.08949754953014022 ) ) ;
#6601=DIRECTION ( 'NONE',  ( 1.000000000000000000, 0.000000000000000000, 0.000000000000000000 ) ) ;
#6616=CARTESIAN_POINT ( 'NONE',  ( 10.00000000000000000, 16.23288003029543347, -33.80338159004267595 ) ) ;
#6642=EDGE_CURVE ( 'NONE', #37989, #63739, #38617, .T. ) ;
#6643=CARTESIAN_POINT ( 'NONE',  ( 0.000000000000000000, 4.992566952384984269, 37.16516213103279398 ) ) ;
#6661=AXIS2_PLACEMENT_3D ( 'NONE', #60681, #53928, #64842 ) ;
#6678=FACE_OUTER_BOUND ( 'NONE', #19337, .T. ) ;
#6705=CARTESIAN_POINT ( 'NONE',  ( 10.00000000000000000, -35.53030884539094103, 12.26510123303246935 ) ) ;
#6716=DIRECTION ( 'NONE',  ( -1.000000000000000000, -0.000000000000000000, 0.000000000000000000 ) ) ;
#6746=DIRECTION ( 'NONE',  ( 0.000000000000000000, 0.000000000000000000, 1.000000000000000000 ) ) ;
#6755=VERTEX_POINT ( 'NONE', #34829 ) ;
#6786=CARTESIAN_POINT ( 'NONE',  ( 0.000000000000000000, 17.80606268964585226, -33.00180498840028775 ) ) ;
#6800=FACE_OUTER_BOUND ( 'NONE', #19750, .T. ) ;
#6811=CARTESIAN_POINT ( 'NONE',  ( 10.00000000000000000, 0.000000000000000000, 0.000000000000000000 ) ) ;
#6843=AXIS2_PLACEMENT_3D ( 'NONE', #30451, #53763, #42493 ) ;
#6850=ORIENTED_EDGE ( 'NONE', *, *, #46524, .F. ) ;
#6866=VERTEX_POINT ( 'NONE', #69044 ) ;
#6874=ADVANCED_FACE ( 'NONE', ( #71233 ), #31016, .T. ) ;
#6898=CIRCLE ( 'NONE', #48899, 16.00000000000000000 ) ;
#6925=CARTESIAN_POINT ( 'NONE',  ( 4.999999999999999112, 40.68715046381927891, 10.41901085202092858 ) ) ;
#6937=DIRECTION ( 'NONE',  ( 0.000000000000000000, 0.000000000000000000, 1.000000000000000000 ) ) ;
#6942=DIRECTION ( 'NONE',  ( 0.000000000000000000, 0.000000000000000000, 1.000000000000000000 ) ) ;
#6953=DIRECTION ( 'NONE',  ( 0.000000000000000000, 0.000000000000000000, 1.000000000000000000 ) ) ;
#6957=ORIENTED_EDGE ( 'NONE', *, *, #59238, .T. ) ;
#6969=DIRECTION ( 'NONE',  ( 1.000000000000000000, 0.000000000000000000, 0.000000000000000000 ) ) ;
#6971=AXIS2_PLACEMENT_3D ( 'NONE', #24476, #35022, #18820 ) ;
#6982=LINE ( 'NONE', #41209, #70562 ) ;
#7024=LINE ( 'NONE', #29950, #30545 ) ;
#7042=CARTESIAN_POINT ( 'NONE',  ( 10.00000000000000000, -26.08949754953044220, 27.05870788708222818 ) ) ;
#7071=DIRECTION ( 'NONE',  ( -1.000000000000000000, -0.000000000000000000, -0.000000000000000000 ) ) ;
#7075=DIRECTION ( 'NONE',  ( 0.000000000000000000, -0.4539904997395351471, -0.8910065241883737830 ) ) ;
#7078=CARTESIAN_POINT ( 'NONE',  ( 0.000000000000000000, -29.81001611430991360, -22.74946021919165418 ) ) ;
#7082=CARTESIAN_POINT ( 'NONE',  ( 10.00000000000000000, 17.80606268964585226, -33.00180498840028775 ) ) ;
#7093=DIRECTION ( 'NONE',  ( 0.000000000000000000, -0.1564344650402380854, 0.9876883405951365491 ) ) ;
#7119=FILL_AREA_STYLE ('',( #65015 ) ) ;
#7128=EDGE_CURVE ( 'NONE', #30173, #51588, #37289, .T. ) ;
#7131=DIRECTION ( 'NONE',  ( -1.000000000000000000, -0.000000000000000000, 0.000000000000000000 ) ) ;
#7138=VERTEX_POINT ( 'NONE', #36895 ) ;
#7142=EDGE_LOOP ( 'NONE', ( #68629, #17378, #59631, #4786 ) ) ;
#7146=LINE ( 'NONE', #64299, #69748 ) ;
#7149=ORIENTED_EDGE ( 'NONE', *, *, #66707, .T. ) ;
#7157=FACE_OUTER_BOUND ( 'NONE', #57507, .T. ) ;
#7163=DIRECTION ( 'NONE',  ( 0.000000000000000000, -0.3090169943749349057, -0.9510565162951576390 ) ) ;
#7181=CARTESIAN_POINT ( 'NONE',  ( -10.00000000000000000, 0.000000000000000000, 0.000000000000000000 ) ) ;
#7201=EDGE_CURVE ( 'NONE', #49855, #24962, #71465, .T. ) ;
#7222=ORIENTED_EDGE ( 'NONE', *, *, #57036, .F. ) ;
#7266=CARTESIAN_POINT ( 'NONE',  ( 10.00000000000000000, 0.000000000000000000, 0.000000000000000000 ) ) ;
#7275=AXIS2_PLACEMENT_3D ( 'NONE', #54031, #14534, #49488 ) ;
#7318=CARTESIAN_POINT ( 'NONE',  ( 0.000000000000000000, 39.04073710021344112, 15.48615015657596672 ) ) ;
#7320=VERTEX_POINT ( 'NONE', #68385 ) ;
#7340=CARTESIAN_POINT ( 'NONE',  ( 10.00000000000000000, 37.22597642581158084, -5.202137450156524068 ) ) ;
#7341=PLANE ( 'NONE',  #55403 ) ;
#7375=DIRECTION ( 'NONE',  ( -1.000000000000000000, 0.000000000000000000, 0.000000000000000000 ) ) ;
#7384=ORIENTED_EDGE ( 'NONE', *, *, #31300, .F. ) ;
#7399=ADVANCED_FACE ( 'NONE', ( #34898 ), #40170, .T. ) ;
#7444=DIRECTION ( 'NONE',  ( 0.000000000000000000, 0.000000000000000000, 1.000000000000000000 ) ) ;
#7451=DIRECTION ( 'NONE',  ( -1.000000000000000000, -0.000000000000000000, -0.000000000000000000 ) ) ;
#7470=CARTESIAN_POINT ( 'NONE',  ( -10.00000000000000000, 0.000000000000000000, 0.000000000000000000 ) ) ;
#7488=AXIS2_PLACEMENT_3D ( 'NONE', #42669, #30266, #53209 ) ;
#7527=CARTESIAN_POINT ( 'NONE',  ( 4.999999999999999112, 21.40280677340371795, 36.13751322684426270 ) ) ;
#7528=CARTESIAN_POINT ( 'NONE',  ( 10.00000000000000000, -26.08949754953005495, -27.05870788708258701 ) ) ;
#7542=CIRCLE ( 'NONE', #32735, 16.00000000000000355 ) ;
#7558=CYLINDRICAL_SURFACE ( 'NONE', #25107, 16.00000000000000000 ) ;
#7566=DIRECTION ( 'NONE',  ( 0.000000000000000000, 0.000000000000000000, 1.000000000000000000 ) ) ;
#7599=DIRECTION ( 'NONE',  ( -1.000000000000000000, 0.000000000000000000, 0.000000000000000000 ) ) ;
#7615=CARTESIAN_POINT ( 'NONE',  ( 10.00000000000000000, -37.48860685352290290, -0.8828120875904512665 ) ) ;
#7626=CYLINDRICAL_SURFACE ( 'NONE', #65010, 16.00000000000000000 ) ;
#7643=CYLINDRICAL_SURFACE ( 'NONE', #24997, 42.00000000000000000 ) ;
#7658=FACE_OUTER_BOUND ( 'NONE', #65763, .T. ) ;
#7676=AXIS2_PLACEMENT_3D ( 'NONE', #60275, #48604, #13639 ) ;
#7695=CIRCLE ( 'NONE', #49693, 42.00000000000000000 ) ;
#7702=ORIENTED_EDGE ( 'NONE', *, *, #36649, .T. ) ;
#7709=EDGE_CURVE ( 'NONE', #34044, #57844, #49724, .T. ) ;
#7712=CARTESIAN_POINT ( 'NONE',  ( 0.000000000000000000, 36.88895765772642221, -6.736453364083161865 ) ) ;
#7713=AXIS2_PLACEMENT_3D ( 'NONE', #49761, #48296, #48667 ) ;
#7723=DIRECTION ( 'NONE',  ( -1.000000000000000000, -0.000000000000000000, 0.000000000000000000 ) ) ;
#7729=DIRECTION ( 'NONE',  ( 0.000000000000000000, 0.3090169943749480619, -0.9510565162951533091 ) ) ;
#7730=AXIS2_PLACEMENT_3D ( 'NONE', #63125, #34513, #23252 ) ;
#7735=DIRECTION ( 'NONE',  ( 0.000000000000000000, 0.4539904997395479702, -0.8910065241883673437 ) ) ;
#7772=CYLINDRICAL_SURFACE ( 'NONE', #36557, 16.00000000000000000 ) ;
#7781=ORIENTED_EDGE ( 'NONE', *, *, #29769, .T. ) ;
#7784=CYLINDRICAL_SURFACE ( 'NONE', #64603, 42.00000000000000000 ) ;
#7786=CARTESIAN_POINT ( 'NONE',  ( 0.000000000000000000, 0.000000000000000000, 0.000000000000000000 ) ) ;
#7803=ORIENTED_EDGE ( 'NONE', *, *, #13085, .F. ) ;
#7805=EDGE_CURVE ( 'NONE', #57727, #62061, #25699, .T. ) ;
#7809=LINE ( 'NONE', #53671, #9745 ) ;
#7812=CYLINDRICAL_SURFACE ( 'NONE', #1409, 16.00000000000000000 ) ;
#7820=FACE_OUTER_BOUND ( 'NONE', #33123, .T. ) ;
#7825=LINE ( 'NONE', #52953, #44351 ) ;
#7828=EDGE_CURVE ( 'NONE', #51811, #44034, #33305, .T. ) ;
#7833=FACE_OUTER_BOUND ( 'NONE', #4363, .T. ) ;
#7834=DIRECTION ( 'NONE',  ( 1.000000000000000000, 0.000000000000000000, -0.000000000000000000 ) ) ;
#7848=CYLINDRICAL_SURFACE ( 'NONE', #65959, 37.49900000000000233 ) ;
#7859=EDGE_LOOP ( 'NONE', ( #46539, #69107, #56585, #11654 ) ) ;
#7873=ORIENTED_EDGE ( 'NONE', *, *, #23283, .F. ) ;
#7907=VECTOR ( 'NONE', #47538, 1000.000000000000000 ) ;
#7917=EDGE_CURVE ( 'NONE', #32536, #16853, #16154, .T. ) ;
#7949=AXIS2_PLACEMENT_3D ( 'NONE', #26004, #48575, #36918 ) ;
#7952=VERTEX_POINT ( 'NONE', #36281 ) ;
#7960=AXIS2_PLACEMENT_3D ( 'NONE', #54212, #65126, #30151 ) ;
#7961=DIRECTION ( 'NONE',  ( 0.000000000000000000, 0.000000000000000000, 1.000000000000000000 ) ) ;
#7980=DIRECTION ( 'NONE',  ( -1.000000000000000000, -0.000000000000000000, -0.000000000000000000 ) ) ;
#7983=LINE ( 'NONE', #7615, #56673 ) ;
#7985=CARTESIAN_POINT ( 'NONE',  ( 10.00000000000000000, -12.26510123303284594, 35.53030884539080603 ) ) ;
#8010=AXIS2_PLACEMENT_3D ( 'NONE', #27479, #49665, #72589 ) ;
#8023=CARTESIAN_POINT ( 'NONE',  ( 10.00000000000000000, -9.188173127307003085, -40.98264845739760176 ) ) ;
#8028=DIRECTION ( 'NONE',  ( 0.000000000000000000, 0.000000000000000000, 1.000000000000000000 ) ) ;
#8031=DIRECTION ( 'NONE',  ( -1.000000000000000000, 0.000000000000000000, -0.000000000000000000 ) ) ;
#8034=ORIENTED_EDGE ( 'NONE', *, *, #62481, .F. ) ;
#8045=ORIENTED_EDGE ( 'NONE', *, *, #70967, .F. ) ;
#8052=LINE ( 'NONE', #43764, #35302 ) ;
#8055=LINE ( 'NONE', #52428, #42858 ) ;
#8063=AXIS2_PLACEMENT_3D ( 'NONE', #67630, #4126, #39064 ) ;
#8068=AXIS2_PLACEMENT_3D ( 'NONE', #4109, #20637, #3738 ) ;
#8116=CYLINDRICAL_SURFACE ( 'NONE', #2420, 16.00000000000000000 ) ;
#8124=PRODUCT_DEFINITION ( 'UNKNOWN', '', #25592, #42407 ) ;
#8126=ORIENTED_EDGE ( 'NONE', *, *, #35656, .T. ) ;
#8130=CARTESIAN_POINT ( 'NONE',  ( 10.00000000000000000, -10.74501242461308159, 35.92658777277507909 ) ) ;
#8131=AXIS2_PLACEMENT_3D ( 'NONE', #40494, #1057, #40876 ) ;
#8154=LINE ( 'NONE', #54033, #9886 ) ;
#8159=EDGE_CURVE ( 'NONE', #64024, #20082, #24123, .T. ) ;
#8161=CARTESIAN_POINT ( 'NONE',  ( 10.00000000000000000, -39.04073710021356192, 15.48615015657568250 ) ) ;
#8189=AXIS2_PLACEMENT_3D ( 'NONE', #59544, #8031, #30949 ) ;
#8215=ORIENTED_EDGE ( 'NONE', *, *, #31126, .T. ) ;
#8216=VERTEX_POINT ( 'NONE', #27595 ) ;
#8221=ORIENTED_EDGE ( 'NONE', *, *, #35465, .F. ) ;
#8228=ORIENTED_EDGE ( 'NONE', *, *, #43906, .T. ) ;
#8229=ORIENTED_EDGE ( 'NONE', *, *, #54100, .F. ) ;
#8247=EDGE_CURVE ( 'NONE', #61501, #52056, #28937, .T. ) ;
#8252=CARTESIAN_POINT ( 'NONE',  ( 0.000000000000000000, 0.000000000000000000, 0.000000000000000000 ) ) ;
#8258=CARTESIAN_POINT ( 'NONE',  ( 10.00000000000000000, -10.96151621346514382, 35.95386929396252640 ) ) ;
#8263=LINE ( 'NONE', #25553, #33730 ) ;
#8276=AXIS2_PLACEMENT_3D ( 'NONE', #29470, #958, #58427 ) ;
#8320=EDGE_LOOP ( 'NONE', ( #61757, #32515, #16543, #19046 ) ) ;
#8339=CARTESIAN_POINT ( 'NONE',  ( 10.00000000000000000, 0.000000000000000000, 0.000000000000000000 ) ) ;
#8341=DIRECTION ( 'NONE',  ( 0.000000000000000000, 0.9876883405951372152, 0.1564344650402347547 ) ) ;
#8383=ADVANCED_FACE ( 'NONE', ( #41837 ), #29803, .T. ) ;
#8387=EDGE_CURVE ( 'NONE', #305, #11760, #53492, .T. ) ;
#8388=CARTESIAN_POINT ( 'NONE',  ( 10.00000000000000000, 33.79645857604513992, 16.45098606841138178 ) ) ;
#8406=AXIS2_PLACEMENT_3D ( 'NONE', #2575, #43520, #21280 ) ;
#8407=EDGE_CURVE ( 'NONE', #57603, #54442, #41112, .T. ) ;
#8420=ORIENTED_EDGE ( 'NONE', *, *, #68442, .F. ) ;
#8432=ADVANCED_FACE ( 'NONE', ( #59139 ), #7626, .T. ) ;
#8438=CARTESIAN_POINT ( 'NONE',  ( 10.00000000000000000, -12.26510123303234501, -35.53030884539098366 ) ) ;
#8449=CARTESIAN_POINT ( 'NONE',  ( 10.00000000000000000, 35.38097989696528600, -12.42422080174602605 ) ) ;
#8457=VERTEX_POINT ( 'NONE', #69301 ) ;
#8466=ORIENTED_EDGE ( 'NONE', *, *, #70241, .F. ) ;
#8487=ADVANCED_FACE ( 'NONE', ( #64411 ), #35814, .T. ) ;
#8494=ORIENTED_EDGE ( 'NONE', *, *, #404, .T. ) ;
#8507=DIRECTION ( 'NONE',  ( -1.000000000000000000, 0.000000000000000000, -0.000000000000000000 ) ) ;
#8509=AXIS2_PLACEMENT_3D ( 'NONE', #68850, #17332, #16587 ) ;
#8510=EDGE_LOOP ( 'NONE', ( #10830, #61773, #30303, #8533 ) ) ;
#8513=ORIENTED_EDGE ( 'NONE', *, *, #18104, .T. ) ;
#8517=EDGE_CURVE ( 'NONE', #40304, #56703, #72176, .T. ) ;
#8523=DIRECTION ( 'NONE',  ( -1.000000000000000000, -0.000000000000000000, 0.000000000000000000 ) ) ;
#8527=ORIENTED_EDGE ( 'NONE', *, *, #63036, .T. ) ;
#8533=ORIENTED_EDGE ( 'NONE', *, *, #8854, .T. ) ;
#8536=CARTESIAN_POINT ( 'NONE',  ( 10.00000000000000000, -22.64427369931148348, -30.00120703465229965 ) ) ;
#8574=EDGE_CURVE ( 'NONE', #12587, #48259, #34952, .T. ) ;
#8575=AXIS2_PLACEMENT_3D ( 'NONE', #22069, #45012, #67939 ) ;
#8580=LINE ( 'NONE', #71332, #61854 ) ;
#8588=CARTESIAN_POINT ( 'NONE',  ( 10.00000000000000000, 0.000000000000000000, 0.000000000000000000 ) ) ;
#8594=CIRCLE ( 'NONE', #47034, 42.00000000000000000 ) ;
#8601=EDGE_CURVE ( 'NONE', #27431, #53345, #20572, .T. ) ;
#8643=FACE_OUTER_BOUND ( 'NONE', #1164, .T. ) ;
#8663=EDGE_CURVE ( 'NONE', #26693, #42186, #9775, .T. ) ;
#8680=ORIENTED_EDGE ( 'NONE', *, *, #53581, .T. ) ;
#8710=ORIENTED_EDGE ( 'NONE', *, *, #5636, .F. ) ;
#8745=EDGE_CURVE ( 'NONE', #36437, #53879, #69487, .T. ) ;
#8754=LINE ( 'NONE', #35829, #52052 ) ;
#8756=DIRECTION ( 'NONE',  ( -1.000000000000000000, 0.000000000000000000, 0.000000000000000000 ) ) ;
#8760=CARTESIAN_POINT ( 'NONE',  ( 10.00000000000000000, 16.23288003029543347, -33.80338159004267595 ) ) ;
#8762=DIRECTION ( 'NONE',  ( -1.000000000000000000, 0.000000000000000000, -0.000000000000000000 ) ) ;
#8763=AXIS2_PLACEMENT_3D ( 'NONE', #24946, #30214, #8028 ) ;
#8770=VECTOR ( 'NONE', #51721, 1000.000000000000000 ) ;
#8773=EDGE_LOOP ( 'NONE', ( #38359, #35048, #65098, #10354 ) ) ;
#8775=DIRECTION ( 'NONE',  ( -1.000000000000000000, 0.000000000000000000, 0.000000000000000000 ) ) ;
#8785=DIRECTION ( 'NONE',  ( 1.000000000000000000, 0.000000000000000000, -0.000000000000000000 ) ) ;
#8798=DIRECTION ( 'NONE',  ( 0.000000000000000000, -0.7071067811865536790, 0.7071067811865414665 ) ) ;
#8811=DIRECTION ( 'NONE',  ( -1.000000000000000000, 0.000000000000000000, 0.000000000000000000 ) ) ;
#8823=DIRECTION ( 'NONE',  ( -1.000000000000000000, 0.000000000000000000, 0.000000000000000000 ) ) ;
#8837=CARTESIAN_POINT ( 'NONE',  ( 0.000000000000000000, 0.000000000000000000, 0.000000000000000000 ) ) ;
#8844=ADVANCED_FACE ( 'NONE', ( #53308 ), #7812, .T. ) ;
#8854=EDGE_CURVE ( 'NONE', #52264, #44231, #73360, .T. ) ;
#8860=VERTEX_POINT ( 'NONE', #59693 ) ;
#8863=CARTESIAN_POINT ( 'NONE',  ( 10.00000000000000000, 37.16516213103285082, -4.992566952384588141 ) ) ;
#8869=CARTESIAN_POINT ( 'NONE',  ( 10.00000000000000000, -35.53030884539077050, -12.26510123303296851 ) ) ;
#8876=ORIENTED_EDGE ( 'NONE', *, *, #36597, .F. ) ;
#8883=CARTESIAN_POINT ( 'NONE',  ( 10.00000000000000000, -0.6853352020787742971, -37.58145647212455032 ) ) ;
#8885=CARTESIAN_POINT ( 'NONE',  ( 10.00000000000000000, 16.45098606841126454, 33.79645857604518966 ) ) ;
#8898=DIRECTION ( 'NONE',  ( -1.000000000000000000, -0.000000000000000000, 0.000000000000000000 ) ) ;
#8940=CIRCLE ( 'NONE', #40023, 16.00000000000000000 ) ;
#8943=CIRCLE ( 'NONE', #5369, 15.99999999999999822 ) ;
#8945=DIRECTION ( 'NONE',  ( -1.000000000000000000, 0.000000000000000000, 0.000000000000000000 ) ) ;
#8946=DIRECTION ( 'NONE',  ( 0.000000000000000000, 0.000000000000000000, 1.000000000000000000 ) ) ;
#8949=DIRECTION ( 'NONE',  ( -1.000000000000000000, 0.000000000000000000, 0.000000000000000000 ) ) ;
#8967=VERTEX_POINT ( 'NONE', #26943 ) ;
#8995=DIRECTION ( 'NONE',  ( -1.000000000000000000, 0.000000000000000000, -0.000000000000000000 ) ) ;
#8997=ADVANCED_FACE ( 'NONE', ( #32949 ), #2948, .T. ) ;
#9025=ORIENTED_EDGE ( 'NONE', *, *, #723, .T. ) ;
#9038=ORIENTED_EDGE ( 'NONE', *, *, #52804, .F. ) ;
#9059=ORIENTED_EDGE ( 'NONE', *, *, #73261, .T. ) ;
#9064=ORIENTED_EDGE ( 'NONE', *, *, #8601, .T. ) ;
#9075=EDGE_CURVE ( 'NONE', #3167, #38633, #60806, .T. ) ;
#9086=DIRECTION ( 'NONE',  ( 0.000000000000000000, 0.000000000000000000, -1.000000000000000000 ) ) ;
#9090=AXIS2_PLACEMENT_3D ( 'NONE', #22770, #5486, #28383 ) ;
#9103=CIRCLE ( 'NONE', #29534, 16.00000000000000000 ) ;
#9106=DIRECTION ( 'NONE',  ( 0.000000000000000000, 0.8090169943749487835, -0.5877852522924713607 ) ) ;
#9118=FACE_OUTER_BOUND ( 'NONE', #70268, .T. ) ;
#9121=FACE_OUTER_BOUND ( 'NONE', #8320, .T. ) ;
#9122=CARTESIAN_POINT ( 'NONE',  ( 10.00000000000000000, 10.41901085202078114, 40.68715046381932865 ) ) ;
#9131=EDGE_CURVE ( 'NONE', #5742, #7138, #10866, .T. ) ;
#9139=VERTEX_POINT ( 'NONE', #11154 ) ;
#9144=VECTOR ( 'NONE', #46647, 1000.000000000000000 ) ;
#9185=EDGE_CURVE ( 'NONE', #25170, #39943, #10404, .T. ) ;
#9246=FACE_OUTER_BOUND ( 'NONE', #52221, .T. ) ;
#9247=DIRECTION ( 'NONE',  ( 0.000000000000000000, 0.9876883405951382144, -0.1564344650402276493 ) ) ;
#9262=CARTESIAN_POINT ( 'NONE',  ( 0.000000000000000000, 12.26510123303308752, -35.53030884539072787 ) ) ;
#9290=DIRECTION ( 'NONE',  ( 0.000000000000000000, 0.9510565162951521989, 0.3090169943749515591 ) ) ;
#9332=FACE_OUTER_BOUND ( 'NONE', #68745, .T. ) ;
#9342=AXIS2_PLACEMENT_3D ( 'NONE', #47301, #42033, #64228 ) ;
#9352=ORIENTED_EDGE ( 'NONE', *, *, #46965, .F. ) ;
#9370=DIRECTION ( 'NONE',  ( -1.000000000000000000, 0.000000000000000000, -0.000000000000000000 ) ) ;
#9372=VECTOR ( 'NONE', #46910, 1000.000000000000000 ) ;
#9385=FACE_OUTER_BOUND ( 'NONE', #52527, .T. ) ;
#9395=EDGE_CURVE ( 'NONE', #44188, #24060, #12030, .T. ) ;
#9413=VERTEX_POINT ( 'NONE', #58869 ) ;
#9415=CIRCLE ( 'NONE', #51448, 42.00000000000000000 ) ;
#9417=EDGE_CURVE ( 'NONE', #20222, #51520, #60091, .T. ) ;
#9420=CIRCLE ( 'NONE', #26269, 42.00000000000000000 ) ;
#9445=EDGE_LOOP ( 'NONE', ( #46450, #58721, #63168, #57965 ) ) ;
#9457=DIRECTION ( 'NONE',  ( -1.000000000000000000, -0.000000000000000000, -0.000000000000000000 ) ) ;
#9470=CARTESIAN_POINT ( 'NONE',  ( 0.000000000000000000, -5.202137450156655518, 37.22597642581156663 ) ) ;
#9473=DIRECTION ( 'NONE',  ( 0.000000000000000000, 0.9876883405951372152, 0.1564344650402347547 ) ) ;
#9490=CARTESIAN_POINT ( 'NONE',  ( 10.00000000000000000, 16.95692799528845995, 2.500000000000000000 ) ) ;
#9526=CIRCLE ( 'NONE', #51553, 42.00000000000000000 ) ;
#9532=VECTOR ( 'NONE', #14051, 1000.000000000000000 ) ;
#9552=CARTESIAN_POINT ( 'NONE',  ( 0.000000000000000000, 16.65560815589464028, -38.55633173626993226 ) ) ;
#9592=DIRECTION ( 'NONE',  ( 0.000000000000000000, -0.9510565162951565288, 0.3090169943749384029 ) ) ;
#9604=ORIENTED_EDGE ( 'NONE', *, *, #50225, .F. ) ;
#9618=VERTEX_POINT ( 'NONE', #62199 ) ;
#9619=AXIS2_PLACEMENT_3D ( 'NONE', #15577, #39999, #61823 ) ;
#9638=CYLINDRICAL_SURFACE ( 'NONE', #62616, 16.00000000000000000 ) ;
#9658=CARTESIAN_POINT ( 'NONE',  ( 0.000000000000000000, 0.000000000000000000, 0.000000000000000000 ) ) ;
#9670=CARTESIAN_POINT ( 'NONE',  ( -10.00000000000000000, 0.000000000000000000, 0.000000000000000000 ) ) ;
#9674=ORIENTED_EDGE ( 'NONE', *, *, #66600, .T. ) ;
#9688=CIRCLE ( 'NONE', #51729, 37.49900000000000944 ) ;
#9691=ORIENTED_EDGE ( 'NONE', *, *, #26050, .F. ) ;
#9726=ORIENTED_EDGE ( 'NONE', *, *, #38449, .T. ) ;
#9730=ORIENTED_EDGE ( 'NONE', *, *, #53581, .F. ) ;
#9736=ORIENTED_EDGE ( 'NONE', *, *, #44559, .F. ) ;
#9745=VECTOR ( 'NONE', #42397, 1000.000000000000000 ) ;
#9761=EDGE_CURVE ( 'NONE', #71645, #37324, #67060, .T. ) ;
#9763=DIRECTION ( 'NONE',  ( -1.000000000000000000, 0.000000000000000000, 0.000000000000000000 ) ) ;
#9775=CIRCLE ( 'NONE', #58997, 42.00000000000000000 ) ;
#9781=DIRECTION ( 'NONE',  ( -1.000000000000000000, 0.000000000000000000, 0.000000000000000000 ) ) ;
#9783=CARTESIAN_POINT ( 'NONE',  ( 10.00000000000000000, -10.41901085202107247, 40.68715046381925049 ) ) ;
#9790=ORIENTED_EDGE ( 'NONE', *, *, #1037, .T. ) ;
#9796=ORIENTED_EDGE ( 'NONE', *, *, #41731, .F. ) ;
#9801=CARTESIAN_POINT ( 'NONE',  ( 10.00000000000000000, 30.84782396557218931, 21.32104025579126017 ) ) ;
#9831=DIRECTION ( 'NONE',  ( 1.000000000000000000, 0.000000000000000000, 0.000000000000000000 ) ) ;
#9837=FACE_OUTER_BOUND ( 'NONE', #4562, .T. ) ;
#9838=EDGE_CURVE ( 'NONE', #54942, #69529, #31035, .T. ) ;
#9841=CIRCLE ( 'NONE', #35068, 16.00000000000000000 ) ;
#9852=CARTESIAN_POINT ( 'NONE',  ( 5.000000000000000000, 22.48208911017500355, 35.47612816024530957 ) ) ;
#9857=EDGE_LOOP ( 'NONE', ( #30592, #61676, #22381, #15674 ) ) ;
#9873=DIRECTION ( 'NONE',  ( 0.000000000000000000, 0.000000000000000000, 1.000000000000000000 ) ) ;
#9886=VECTOR ( 'NONE', #32562, 1000.000000000000000 ) ;
#9901=DIRECTION ( 'NONE',  ( 0.000000000000000000, 0.000000000000000000, 1.000000000000000000 ) ) ;
#9923=ADVANCED_FACE ( 'NONE', ( #42980 ), #71896, .T. ) ;
#9930=DIRECTION ( 'NONE',  ( 0.000000000000000000, -0.8090169943749531134, 0.5877852522924653655 ) ) ;
#9937=ADVANCED_FACE ( 'NONE', ( #9121 ), #3508, .T. ) ;
#9939=CIRCLE ( 'NONE', #19538, 42.00000000000000000 ) ;
#9952=DIRECTION ( 'NONE',  ( -1.000000000000000000, 0.000000000000000000, -0.000000000000000000 ) ) ;
#9962=VERTEX_POINT ( 'NONE', #9490 ) ;
#9976=EDGE_LOOP ( 'NONE', ( #60940, #26239, #8221, #6131 ) ) ;
#10055=VECTOR ( 'NONE', #64325, 1000.000000000000000 ) ;
#10062=FACE_OUTER_BOUND ( 'NONE', #34289, .T. ) ;
#10063=CYLINDRICAL_SURFACE ( 'NONE', #23120, 37.49900000000000233 ) ;
#10064=CARTESIAN_POINT ( 'NONE',  ( 10.00000000000000000, -12.26510123303284594, 35.53030884539080603 ) ) ;
#10075=CARTESIAN_POINT ( 'NONE',  ( 0.000000000000000000, -40.98264845739743123, -9.188173127307734944 ) ) ;
#10098=ORIENTED_EDGE ( 'NONE', *, *, #17345, .T. ) ;
#10103=VECTOR ( 'NONE', #57068, 1000.000000000000000 ) ;
#10105=EDGE_LOOP ( 'NONE', ( #52493, #65577, #62284, #36774 ) ) ;
#10118=DIRECTION ( 'NONE',  ( 0.000000000000000000, -0.5877852522924624790, -0.8090169943749553338 ) ) ;
#10123=DIRECTION ( 'NONE',  ( 0.000000000000000000, 0.000000000000000000, -1.000000000000000000 ) ) ;
#10125=VECTOR ( 'NONE', #18022, 1000.000000000000000 ) ;
#10129=CIRCLE ( 'NONE', #5330, 16.00000000000000000 ) ;
#10143=ORIENTED_EDGE ( 'NONE', *, *, #29799, .T. ) ;
#10146=DIRECTION ( 'NONE',  ( 0.000000000000000000, -0.4539904997395540764, 0.8910065241883642351 ) ) ;
#10154=EDGE_CURVE ( 'NONE', #6866, #2581, #19076, .T. ) ;
#10159=( LENGTH_UNIT ( ) NAMED_UNIT ( * ) SI_UNIT ( .MILLI., .METRE. ) );
#10171=DIRECTION ( 'NONE',  ( -1.000000000000000000, 0.000000000000000000, 0.000000000000000000 ) ) ;
#10173=CIRCLE ( 'NONE', #67829, 15.99999999999999645 ) ;
#10174=EDGE_CURVE ( 'NONE', #23811, #6866, #11884, .T. ) ;
#10248=VERTEX_POINT ( 'NONE', #33479 ) ;
#10273=CARTESIAN_POINT ( 'NONE',  ( 10.00000000000000000, 26.08949754953062694, -27.05870788708203989 ) ) ;
#10275=AXIS2_PLACEMENT_3D ( 'NONE', #19364, #59600, #42315 ) ;
#10289=DIRECTION ( 'NONE',  ( -1.000000000000000000, 0.000000000000000000, -0.000000000000000000 ) ) ;
#10305=CARTESIAN_POINT ( 'NONE',  ( 0.000000000000000000, 6.555932627142952995, -37.01155633439051940 ) ) ;
#10311=FACE_OUTER_BOUND ( 'NONE', #11808, .T. ) ;
#10330=ORIENTED_EDGE ( 'NONE', *, *, #20110, .F. ) ;
#10332=CIRCLE ( 'NONE', #52354, 37.49900000000000944 ) ;
#10334=ORIENTED_EDGE ( 'NONE', *, *, #45699, .F. ) ;
#10354=ORIENTED_EDGE ( 'NONE', *, *, #37523, .T. ) ;
#10358=LINE ( 'NONE', #4748, #2698 ) ;
#10361=ADVANCED_FACE ( 'NONE', ( #71391 ), #64302, .T. ) ;
#10377=LINE ( 'NONE', #34799, #34220 ) ;
#10378=CARTESIAN_POINT ( 'NONE',  ( 0.000000000000000000, 40.98264845739763018, -9.188173127306864529 ) ) ;
#10398=DIRECTION ( 'NONE',  ( -1.000000000000000000, 0.000000000000000000, 0.000000000000000000 ) ) ;
#10404=LINE ( 'NONE', #67552, #48099 ) ;
#10405=DIRECTION ( 'NONE',  ( -1.000000000000000000, 0.000000000000000000, 0.000000000000000000 ) ) ;
#10412=EDGE_LOOP ( 'NONE', ( #4564, #68328, #52431, #54737 ) ) ;
#10419=DIRECTION ( 'NONE',  ( -1.000000000000000000, 0.000000000000000000, 0.000000000000000000 ) ) ;
#10421=EDGE_CURVE ( 'NONE', #13202, #60472, #55144, .T. ) ;
#10428=VERTEX_POINT ( 'NONE', #63934 ) ;
#10431=VECTOR ( 'NONE', #72157, 1000.000000000000000 ) ;
#10437=ORIENTED_EDGE ( 'NONE', *, *, #45452, .F. ) ;
#10438=CARTESIAN_POINT ( 'NONE',  ( 10.00000000000000000, 0.000000000000000000, 0.000000000000000000 ) ) ;
#10439=VERTEX_POINT ( 'NONE', #70646 ) ;
#10442=VECTOR ( 'NONE', #29191, 1000.000000000000000 ) ;
#10444=CYLINDRICAL_SURFACE ( 'NONE', #5351, 16.00000000000000000 ) ;
#10451=ORIENTED_EDGE ( 'NONE', *, *, #17094, .F. ) ;
#10500=VECTOR ( 'NONE', #69253, 1000.000000000000000 ) ;
#10503=AXIS2_PLACEMENT_3D ( 'NONE', #64283, #7131, #2267 ) ;
#10510=CARTESIAN_POINT ( 'NONE',  ( 0.000000000000000000, 25.88420570971438650, -27.13269053701069566 ) ) ;
#10519=AXIS2_PLACEMENT_3D ( 'NONE', #53714, #2256, #48080 ) ;
#10523=ORIENTED_EDGE ( 'NONE', *, *, #34356, .F. ) ;
#10529=AXIS2_PLACEMENT_3D ( 'NONE', #57585, #40654, #47038 ) ;
#10546=CIRCLE ( 'NONE', #34592, 16.00000000000000355 ) ;
#10608=EDGE_LOOP ( 'NONE', ( #19099, #6850, #7873, #12565 ) ) ;
#10629=AXIS2_PLACEMENT_3D ( 'NONE', #29856, #24243, #51314 ) ;
#10643=AXIS2_PLACEMENT_3D ( 'NONE', #42134, #70666, #2307 ) ;
#10654=LINE ( 'NONE', #33580, #29831 ) ;
#10662=CARTESIAN_POINT ( 'NONE',  ( 10.00000000000000000, 0.000000000000000000, 0.000000000000000000 ) ) ;
#10670=DIRECTION ( 'NONE',  ( 0.000000000000000000, 0.000000000000000000, 1.000000000000000000 ) ) ;
#10676=CARTESIAN_POINT ( 'NONE',  ( 0.000000000000000000, -30.84782396557233142, 21.32104025579104345 ) ) ;
#10682=EDGE_CURVE ( 'NONE', #48259, #23577, #9526, .T. ) ;
#10728=CARTESIAN_POINT ( 'NONE',  ( 0.000000000000000000, -37.22597642581153821, -5.202137450156795850 ) ) ;
#10736=DIRECTION ( 'NONE',  ( -1.000000000000000000, -0.000000000000000000, -0.000000000000000000 ) ) ;
#10737=DIRECTION ( 'NONE',  ( -1.000000000000000000, 0.000000000000000000, 0.000000000000000000 ) ) ;
#10744=DIRECTION ( 'NONE',  ( 0.000000000000000000, 0.000000000000000000, 1.000000000000000000 ) ) ;
#10776=EDGE_CURVE ( 'NONE', #47891, #17447, #2390, .T. ) ;
#10781=FACE_OUTER_BOUND ( 'NONE', #50587, .T. ) ;
#10830=ORIENTED_EDGE ( 'NONE', *, *, #12119, .F. ) ;
#10836=ORIENTED_EDGE ( 'NONE', *, *, #17676, .T. ) ;
#10861=CARTESIAN_POINT ( 'NONE',  ( 5.000000000000000000, 38.55633173627010279, 16.65560815589424593 ) ) ;
#10866=CIRCLE ( 'NONE', #62504, 42.00000000000000000 ) ;
#10886=AXIS2_PLACEMENT_3D ( 'NONE', #22212, #52260, #51521 ) ;
#10890=EDGE_CURVE ( 'NONE', #16321, #22970, #67214, .T. ) ;
#10901=ORIENTED_EDGE ( 'NONE', *, *, #51599, .T. ) ;
#10913=ORIENTED_EDGE ( 'NONE', *, *, #71633, .F. ) ;
#10914=FILL_AREA_STYLE_COLOUR ( '', #46488 ) ;
#10922=DIRECTION ( 'NONE',  ( -1.000000000000000000, -0.000000000000000000, -0.000000000000000000 ) ) ;
#10923=VERTEX_POINT ( 'NONE', #8161 ) ;
#10927=CIRCLE ( 'NONE', #52952, 12.50000000000000000 ) ;
#10959=CARTESIAN_POINT ( 'NONE',  ( 10.00000000000000000, -35.95386929396264009, 10.96151621346475658 ) ) ;
#10961=ADVANCED_FACE ( 'NONE', ( #29983 ), #47288, .T. ) ;
#10980=CARTESIAN_POINT ( 'NONE',  ( 10.00000000000000000, 22.64427369931169309, 30.00120703465213623 ) ) ;
#10987=ORIENTED_EDGE ( 'NONE', *, *, #26795, .T. ) ;
#10989=CARTESIAN_POINT ( 'NONE',  ( 10.00000000000000000, -15.48615015657555816, -39.04073710021360455 ) ) ;
#11033=VECTOR ( 'NONE', #27652, 1000.000000000000000 ) ;
#11058=EDGE_CURVE ( 'NONE', #54680, #37666, #33, .T. ) ;
#11064=CARTESIAN_POINT ( 'NONE',  ( 10.00000000000000000, 16.45098606841126454, 33.79645857604518966 ) ) ;
#11090=ORIENTED_EDGE ( 'NONE', *, *, #61010, .F. ) ;
#11091=ORIENTED_EDGE ( 'NONE', *, *, #10174, .T. ) ;
#11093=ORIENTED_EDGE ( 'NONE', *, *, #32817, .F. ) ;
#11112=ORIENTED_EDGE ( 'NONE', *, *, #18676, .F. ) ;
#11133=VECTOR ( 'NONE', #3185, 1000.000000000000000 ) ;
#11134=EDGE_LOOP ( 'NONE', ( #64151, #70431, #68226, #34572 ) ) ;
#11137=CARTESIAN_POINT ( 'NONE',  ( 10.00000000000000000, 30.00120703465205452, 22.64427369931179967 ) ) ;
#11154=CARTESIAN_POINT ( 'NONE',  ( 0.000000000000000000, -37.16516213103273714, -4.992566952385376844 ) ) ;
#11176=CARTESIAN_POINT ( 'NONE',  ( 10.00000000000000000, 35.53030884539084866, 12.26510123303271982 ) ) ;
#11209=CARTESIAN_POINT ( 'NONE',  ( 10.00000000000000000, 0.000000000000000000, 0.000000000000000000 ) ) ;
#11211=DIRECTION ( 'NONE',  ( 0.000000000000000000, 0.000000000000000000, 1.000000000000000000 ) ) ;
#11216=ORIENTED_EDGE ( 'NONE', *, *, #29521, .F. ) ;
#11222=EDGE_LOOP ( 'NONE', ( #25239, #49070, #65762, #52744 ) ) ;
#11230=EDGE_CURVE ( 'NONE', #62276, #59771, #30079, .T. ) ;
#11241=ADVANCED_FACE ( 'NONE', ( #27294 ), #44986, .T. ) ;
#11244=CARTESIAN_POINT ( 'NONE',  ( 0.000000000000000000, -9.188173127307001309, -40.98264845739759465 ) ) ;
#11248=CIRCLE ( 'NONE', #30443, 42.00000000000000000 ) ;
#11251=DIRECTION ( 'NONE',  ( -1.000000000000000000, 0.000000000000000000, 0.000000000000000000 ) ) ;
#11262=ORIENTED_EDGE ( 'NONE', *, *, #68442, .T. ) ;
#11265=ORIENTED_EDGE ( 'NONE', *, *, #32489, .F. ) ;
#11274=FILL_AREA_STYLE ('',( #10914 ) ) ;
#11304=ORIENTED_EDGE ( 'NONE', *, *, #13826, .T. ) ;
#11316=EDGE_CURVE ( 'NONE', #13377, #49169, #51661, .T. ) ;
#11325=DIRECTION ( 'NONE',  ( -1.000000000000000000, 0.000000000000000000, 0.000000000000000000 ) ) ;
#11326=CARTESIAN_POINT ( 'NONE',  ( 0.000000000000000000, 0.000000000000000000, 0.000000000000000000 ) ) ;
#11329=DIRECTION ( 'NONE',  ( 0.000000000000000000, -0.8090169943749531134, 0.5877852522924653655 ) ) ;
#11346=AXIS2_PLACEMENT_3D ( 'NONE', #2975, #44281, #3342 ) ;
#11371=DIRECTION ( 'NONE',  ( -1.000000000000000000, 0.000000000000000000, -0.000000000000000000 ) ) ;
#11372=VERTEX_POINT ( 'NONE', #59499 ) ;
#11375=VERTEX_POINT ( 'NONE', #3121 ) ;
#11380=DIRECTION ( 'NONE',  ( -1.000000000000000000, -0.000000000000000000, 0.000000000000000000 ) ) ;
#11388=EDGE_CURVE ( 'NONE', #37645, #1535, #44475, .T. ) ;
#11403=AXIS2_PLACEMENT_3D ( 'NONE', #14396, #8762, #3146 ) ;
#11417=CYLINDRICAL_SURFACE ( 'NONE', #1951, 42.00000000000000000 ) ;
#11426=EDGE_CURVE ( 'NONE', #13869, #73989, #19996, .T. ) ;
#11438=EDGE_CURVE ( 'NONE', #46185, #3104, #67279, .T. ) ;
#11439=CARTESIAN_POINT ( 'NONE',  ( 10.00000000000000000, 35.92658777277511462, 10.74501242461295014 ) ) ;
#11462=ORIENTED_EDGE ( 'NONE', *, *, #66893, .T. ) ;
#11464=CARTESIAN_POINT ( 'NONE',  ( 0.000000000000000000, -2.446882695291883605E-15, -2.499999999999983569 ) ) ;
#11468=DIRECTION ( 'NONE',  ( 0.000000000000000000, 0.000000000000000000, 1.000000000000000000 ) ) ;
#11470=CARTESIAN_POINT ( 'NONE',  ( 10.00000000000000000, 26.08949754953062694, -27.05870788708203989 ) ) ;
#11505=CIRCLE ( 'NONE', #65560, 16.00000000000000000 ) ;
#11514=AXIS2_PLACEMENT_3D ( 'NONE', #63678, #40357, #28700 ) ;
#11533=ORIENTED_EDGE ( 'NONE', *, *, #7917, .T. ) ;
#11555=ORIENTED_EDGE ( 'NONE', *, *, #8247, .F. ) ;
#11561=AXIS2_PLACEMENT_3D ( 'NONE', #63588, #63952, #34619 ) ;
#11570=ORIENTED_EDGE ( 'NONE', *, *, #38959, .T. ) ;
#11573=ORIENTED_EDGE ( 'NONE', *, *, #34441, .F. ) ;
#11574=ORIENTED_EDGE ( 'NONE', *, *, #37944, .F. ) ;
#11577=DIRECTION ( 'NONE',  ( -1.000000000000000000, -0.000000000000000000, -0.000000000000000000 ) ) ;
#11586=CARTESIAN_POINT ( 'NONE',  ( 10.00000000000000000, 21.32104025579158701, -30.84782396557194772 ) ) ;
#11591=CARTESIAN_POINT ( 'NONE',  ( 0.000000000000000000, -29.81001611431024045, 22.74946021919122430 ) ) ;
#11603=ADVANCED_FACE ( 'NONE', ( #9837 ), #67351, .T. ) ;
#11606=CARTESIAN_POINT ( 'NONE',  ( 10.00000000000000000, 0.000000000000000000, 0.000000000000000000 ) ) ;
#11634=CARTESIAN_POINT ( 'NONE',  ( 10.00000000000000000, 36.88895765772642932, -6.736453364083163642 ) ) ;
#11654=ORIENTED_EDGE ( 'NONE', *, *, #17745, .T. ) ;
#11664=DIRECTION ( 'NONE',  ( -1.000000000000000000, -0.000000000000000000, -0.000000000000000000 ) ) ;
#11669=LINE ( 'NONE', #74090, #3325 ) ;
#11680=LINE ( 'NONE', #35003, #68672 ) ;
#11691=EDGE_CURVE ( 'NONE', #64991, #26264, #58966, .T. ) ;
#11704=ADVANCED_FACE ( 'NONE', ( #69575 ), #46278, .T. ) ;
#11706=CYLINDRICAL_SURFACE ( 'NONE', #15667, 42.00000000000000000 ) ;
#11721=DIRECTION ( 'NONE',  ( 0.000000000000000000, 0.000000000000000000, 1.000000000000000000 ) ) ;
#11727=VERTEX_POINT ( 'NONE', #47021 ) ;
#11730=ORIENTED_EDGE ( 'NONE', *, *, #66893, .F. ) ;
#11737=DIRECTION ( 'NONE',  ( 0.000000000000000000, 0.000000000000000000, 1.000000000000000000 ) ) ;
#11749=CIRCLE ( 'NONE', #64576, 42.00000000000000000 ) ;
#11757=CARTESIAN_POINT ( 'NONE',  ( 10.00000000000000000, -33.00180498840060039, 17.80606268964528027 ) ) ;
#11759=ORIENTED_EDGE ( 'NONE', *, *, #33183, .T. ) ;
#11760=VERTEX_POINT ( 'NONE', #54141 ) ;
#11771=ADVANCED_FACE ( 'NONE', ( #30446 ), #18434, .T. ) ;
#11793=CYLINDRICAL_SURFACE ( 'NONE', #36104, 42.00000000000000000 ) ;
#11795=EDGE_CURVE ( 'NONE', #70536, #62068, #8263, .T. ) ;
#11797=EDGE_CURVE ( 'NONE', #1624, #6579, #30120, .T. ) ;
#11802=AXIS2_PLACEMENT_3D ( 'NONE', #3132, #14743, #65903 ) ;
#11808=EDGE_LOOP ( 'NONE', ( #3901, #4195, #43087, #31901 ) ) ;
#11818=AXIS2_PLACEMENT_3D ( 'NONE', #53513, #47141, #36582 ) ;
#11841=ORIENTED_EDGE ( 'NONE', *, *, #3857, .T. ) ;
#11846=DIRECTION ( 'NONE',  ( 0.000000000000000000, -9.787530781167598712E-16, -1.000000000000000000 ) ) ;
#11847=CARTESIAN_POINT ( 'NONE',  ( 10.00000000000000000, 37.01155633439059756, 6.555932627142549762 ) ) ;
#11849=DIRECTION ( 'NONE',  ( 0.000000000000000000, 0.4539904997395479702, -0.8910065241883673437 ) ) ;
#11852=ORIENTED_EDGE ( 'NONE', *, *, #18104, .F. ) ;
#11856=CARTESIAN_POINT ( 'NONE',  ( 10.00000000000000000, -27.05870788708213226, -26.08949754953053102 ) ) ;
#11868=CIRCLE ( 'NONE', #15471, 16.00000000000000000 ) ;
#11870=ADVANCED_FACE ( 'NONE', ( #16133 ), #60888, .T. ) ;
#11873=FACE_OUTER_BOUND ( 'NONE', #29497, .T. ) ;
#11881=VECTOR ( 'NONE', #44800, 1000.000000000000000 ) ;
#11884=CIRCLE ( 'NONE', #53915, 16.00000000000000000 ) ;
#11919=EDGE_LOOP ( 'NONE', ( #12846, #50425, #51123, #45232 ) ) ;
#11952=CIRCLE ( 'NONE', #31154, 37.49900000000000233 ) ;
#11957=VERTEX_POINT ( 'NONE', #72151 ) ;
#11968=DIRECTION ( 'NONE',  ( -1.000000000000000000, 0.000000000000000000, -0.000000000000000000 ) ) ;
#11982=AXIS2_PLACEMENT_3D ( 'NONE', #67076, #4320, #27205 ) ;
#11986=CARTESIAN_POINT ( 'NONE',  ( 10.00000000000000000, -3.925862922256464493, 41.81611651403861174 ) ) ;
#11989=ORIENTED_EDGE ( 'NONE', *, *, #41656, .T. ) ;
#11990=EDGE_CURVE ( 'NONE', #26052, #43117, #22147, .T. ) ;
#12001=AXIS2_PLACEMENT_3D ( 'NONE', #22201, #67319, #22575 ) ;
#12003=CIRCLE ( 'NONE', #54041, 16.00000000000000000 ) ;
#12014=DIRECTION ( 'NONE',  ( 0.000000000000000000, 0.000000000000000000, 1.000000000000000000 ) ) ;
#12019=ORIENTED_EDGE ( 'NONE', *, *, #11230, .T. ) ;
#12021=EDGE_CURVE ( 'NONE', #57727, #53203, #46558, .T. ) ;
#12030=CIRCLE ( 'NONE', #54067, 16.00000000000000000 ) ;
#12036=ORIENTED_EDGE ( 'NONE', *, *, #17345, .F. ) ;
#12039=DIRECTION ( 'NONE',  ( -1.000000000000000000, 0.000000000000000000, 0.000000000000000000 ) ) ;
#12054=CARTESIAN_POINT ( 'NONE',  ( 5.000000000000000000, -21.40280677340398086, 36.13751322684410638 ) ) ;
#12061=CARTESIAN_POINT ( 'NONE',  ( 10.00000000000000000, -33.79645857604501913, -16.45098606841161626 ) ) ;
#12064=DIRECTION ( 'NONE',  ( -1.000000000000000000, -0.000000000000000000, 0.000000000000000000 ) ) ;
#12066=EDGE_CURVE ( 'NONE', #10923, #1624, #51761, .T. ) ;
#12119=EDGE_CURVE ( 'NONE', #55893, #44231, #7809, .T. ) ;
#12130=VERTEX_POINT ( 'NONE', #47659 ) ;
#12140=AXIS2_PLACEMENT_3D ( 'NONE', #21772, #72519, #10118 ) ;
#12149=DIRECTION ( 'NONE',  ( 0.000000000000000000, 0.000000000000000000, 1.000000000000000000 ) ) ;
#12151=ORIENTED_EDGE ( 'NONE', *, *, #404, .F. ) ;
#12155=ADVANCED_FACE ( 'NONE', ( #29991 ), #2212, .T. ) ;
#12156=ADVANCED_FACE ( 'NONE', ( #64970 ), #52937, .T. ) ;
#12157=CARTESIAN_POINT ( 'NONE',  ( 0.000000000000000000, 5.202137450156389953, 37.22597642581160216 ) ) ;
#12178=ORIENTED_EDGE ( 'NONE', *, *, #28844, .T. ) ;
#12213=DIRECTION ( 'NONE',  ( 0.000000000000000000, 0.3090169943749412340, 0.9510565162951556406 ) ) ;
#12230=EDGE_CURVE ( 'NONE', #19685, #26052, #29726, .T. ) ;
#12273=DIRECTION ( 'NONE',  ( 0.000000000000000000, 0.000000000000000000, 1.000000000000000000 ) ) ;
#12295=DIRECTION ( 'NONE',  ( -1.000000000000000000, 0.000000000000000000, 0.000000000000000000 ) ) ;
#12338=CARTESIAN_POINT ( 'NONE',  ( 10.00000000000000000, 10.74501242461282757, 35.92658777277515014 ) ) ;
#12359=CARTESIAN_POINT ( 'NONE',  ( 0.000000000000000000, -35.92658777277517856, 10.74501242461269257 ) ) ;
#12364=EDGE_CURVE ( 'NONE', #52892, #42621, #2146, .T. ) ;
#12368=EDGE_LOOP ( 'NONE', ( #66122, #19417, #51039, #33268 ) ) ;
#12371=ORIENTED_EDGE ( 'NONE', *, *, #11795, .T. ) ;
#12375=CARTESIAN_POINT ( 'NONE',  ( 10.00000000000000000, 0.000000000000000000, 0.000000000000000000 ) ) ;
#12391=EDGE_CURVE ( 'NONE', #56950, #55462, #66922, .T. ) ;
#12397=DIRECTION ( 'NONE',  ( 0.000000000000000000, 0.000000000000000000, 1.000000000000000000 ) ) ;
#12408=DIRECTION ( 'NONE',  ( 0.000000000000000000, 0.000000000000000000, 1.000000000000000000 ) ) ;
#12423=DIRECTION ( 'NONE',  ( -1.000000000000000000, -0.000000000000000000, -0.000000000000000000 ) ) ;
#12430=DIRECTION ( 'NONE',  ( 0.000000000000000000, 0.000000000000000000, 1.000000000000000000 ) ) ;
#12436=DIRECTION ( 'NONE',  ( -1.000000000000000000, -0.000000000000000000, -0.000000000000000000 ) ) ;
#12443=CARTESIAN_POINT ( 'NONE',  ( 10.00000000000000000, 40.98264845739749518, 9.188173127307441845 ) ) ;
#12451=FACE_OUTER_BOUND ( 'NONE', #66302, .T. ) ;
#12459=DIRECTION ( 'NONE',  ( 0.000000000000000000, 0.000000000000000000, 1.000000000000000000 ) ) ;
#12463=EDGE_CURVE ( 'NONE', #38967, #23893, #57446, .T. ) ;
#12466=CARTESIAN_POINT ( 'NONE',  ( 0.000000000000000000, 0.000000000000000000, 0.000000000000000000 ) ) ;
#12468=AXIS2_PLACEMENT_3D ( 'NONE', #41030, #11325, #6444 ) ;
#12481=EDGE_CURVE ( 'NONE', #52158, #54849, #31010, .T. ) ;
#12485=ORIENTED_EDGE ( 'NONE', *, *, #7828, .F. ) ;
#12496=EDGE_CURVE ( 'NONE', #31431, #20705, #29900, .T. ) ;
#12509=CARTESIAN_POINT ( 'NONE',  ( 10.00000000000000000, -35.92658777277502935, -10.74501242461320594 ) ) ;
#12520=VECTOR ( 'NONE', #65300, 1000.000000000000000 ) ;
#12565=ORIENTED_EDGE ( 'NONE', *, *, #32351, .T. ) ;
#12578=CIRCLE ( 'NONE', #17419, 37.49900000000000944 ) ;
#12579=EDGE_CURVE ( 'NONE', #46805, #36613, #38225, .T. ) ;
#12582=DIRECTION ( 'NONE',  ( 0.000000000000000000, 0.3090169943749482839, -0.9510565162951533091 ) ) ;
#12587=VERTEX_POINT ( 'NONE', #31752 ) ;
#12633=AXIS2_PLACEMENT_3D ( 'NONE', #54499, #2299, #66886 ) ;
#12638=VERTEX_POINT ( 'NONE', #60352 ) ;
#12639=ORIENTED_EDGE ( 'NONE', *, *, #6066, .F. ) ;
#12656=ORIENTED_EDGE ( 'NONE', *, *, #41867, .F. ) ;
#12661=AXIS2_PLACEMENT_3D ( 'NONE', #35516, #40050, #63364 ) ;
#12676=CARTESIAN_POINT ( 'NONE',  ( 10.00000000000000178, 12.24744871391589385, -2.499999999999995559 ) ) ;
#12730=EDGE_CURVE ( 'NONE', #54468, #6463, #50173, .T. ) ;
#12734=VECTOR ( 'NONE', #26750, 1000.000000000000000 ) ;
#12741=CARTESIAN_POINT ( 'NONE',  ( 10.00000000000000000, -21.53537804866058991, -30.80686688397033635 ) ) ;
#12753=ORIENTED_EDGE ( 'NONE', *, *, #43722, .T. ) ;
#12782=CARTESIAN_POINT ( 'NONE',  ( 10.00000000000000000, -35.95386929396248377, -10.96151621346525751 ) ) ;
#12785=CARTESIAN_POINT ( 'NONE',  ( 0.000000000000000000, 15.48615015657637883, -39.04073710021327770 ) ) ;
#12793=FACE_OUTER_BOUND ( 'NONE', #19445, .T. ) ;
#12795=DIRECTION ( 'NONE',  ( -1.000000000000000000, 0.000000000000000000, 0.000000000000000000 ) ) ;
#12808=EDGE_LOOP ( 'NONE', ( #49825, #16202, #64207, #68879 ) ) ;
#12810=DIRECTION ( 'NONE',  ( -1.000000000000000000, 0.000000000000000000, -0.000000000000000000 ) ) ;
#12813=DIRECTION ( 'NONE',  ( 1.000000000000000000, -0.000000000000000000, -0.000000000000000000 ) ) ;
#12815=DIRECTION ( 'NONE',  ( 0.000000000000000000, 0.7071067811865437980, 0.7071067811865512365 ) ) ;
#12825=CIRCLE ( 'NONE', #28450, 16.00000000000000355 ) ;
#12846=ORIENTED_EDGE ( 'NONE', *, *, #20547, .T. ) ;
#12860=ORIENTED_EDGE ( 'NONE', *, *, #65401, .T. ) ;
#12864=CARTESIAN_POINT ( 'NONE',  ( 0.000000000000000000, -12.42422080174614862, -35.38097989696524337 ) ) ;
#12881=CARTESIAN_POINT ( 'NONE',  ( 10.00000000000000000, 0.000000000000000000, 0.000000000000000000 ) ) ;
#12882=DIRECTION ( 'NONE',  ( -1.000000000000000000, 0.000000000000000000, 0.000000000000000000 ) ) ;
#12891=DIRECTION ( 'NONE',  ( -1.000000000000000000, -0.000000000000000000, -0.000000000000000000 ) ) ;
#12895=CARTESIAN_POINT ( 'NONE',  ( 10.00000000000000000, -33.79645857604525361, 16.45098606841114730 ) ) ;
#12906=CARTESIAN_POINT ( 'NONE',  ( 0.000000000000000000, 0.000000000000000000, 0.000000000000000000 ) ) ;
#12914=CARTESIAN_POINT ( 'NONE',  ( 10.00000000000000000, 0.000000000000000000, 0.000000000000000000 ) ) ;
#12927=CIRCLE ( 'NONE', #21348, 42.00000000000000000 ) ;
#12930=ORIENTED_EDGE ( 'NONE', *, *, #33183, .F. ) ;
#12933=DIRECTION ( 'NONE',  ( -1.000000000000000000, -0.000000000000000000, 0.000000000000000000 ) ) ;
#12941=FACE_OUTER_BOUND ( 'NONE', #15536, .T. ) ;
#12956=CARTESIAN_POINT ( 'NONE',  ( -1.200000000000000030E-05, 16.95692799528845640, -2.500000000000000000 ) ) ;
#12960=ORIENTED_EDGE ( 'NONE', *, *, #52301, .F. ) ;
#12965=VECTOR ( 'NONE', #8775, 1000.000000000000000 ) ;
#12986=AXIS2_PLACEMENT_3D ( 'NONE', #63091, #37831, #49094 ) ;
#13017=AXIS2_PLACEMENT_3D ( 'NONE', #5271, #28172, #62415 ) ;
#13025=ORIENTED_EDGE ( 'NONE', *, *, #63003, .F. ) ;
#13028=DIRECTION ( 'NONE',  ( 0.000000000000000000, -0.9876883405951393247, 0.1564344650402205161 ) ) ;
#13046=EDGE_CURVE ( 'NONE', #24083, #7138, #70671, .T. ) ;
#13052=AXIS2_PLACEMENT_3D ( 'NONE', #57197, #23717, #35374 ) ;
#13067=ORIENTED_EDGE ( 'NONE', *, *, #17980, .T. ) ;
#13075=AXIS2_PLACEMENT_3D ( 'NONE', #33833, #49626, #21059 ) ;
#13085=EDGE_CURVE ( 'NONE', #73031, #2581, #47880, .T. ) ;
#13086=ADVANCED_FACE ( 'NONE', ( #66633 ), #25663, .T. ) ;
#13105=ORIENTED_EDGE ( 'NONE', *, *, #60393, .F. ) ;
#13115=CARTESIAN_POINT ( 'NONE',  ( 10.00000000000000000, 32.34446384429971744, 26.79245525562727082 ) ) ;
#13116=VECTOR ( 'NONE', #9781, 1000.000000000000000 ) ;
#13117=CARTESIAN_POINT ( 'NONE',  ( 0.000000000000000000, 0.000000000000000000, 0.000000000000000000 ) ) ;
#13143=EDGE_CURVE ( 'NONE', #37625, #73517, #16648, .T. ) ;
#13156=CYLINDRICAL_SURFACE ( 'NONE', #4497, 37.49900000000000233 ) ;
#13186=AXIS2_PLACEMENT_3D ( 'NONE', #59342, #30745, #1498 ) ;
#13189=CARTESIAN_POINT ( 'NONE',  ( 10.00000000000000000, 21.53537804866126137, -30.80686688396986028 ) ) ;
#13194=ORIENTED_EDGE ( 'NONE', *, *, #10776, .T. ) ;
#13202=VERTEX_POINT ( 'NONE', #47063 ) ;
#13204=ORIENTED_EDGE ( 'NONE', *, *, #32351, .F. ) ;
#13205=DIRECTION ( 'NONE',  ( 1.000000000000000000, 0.000000000000000000, 0.000000000000000000 ) ) ;
#13223=ADVANCED_FACE ( 'NONE', ( #40299 ), #41052, .T. ) ;
#13224=AXIS2_PLACEMENT_3D ( 'NONE', #37317, #36927, #36550 ) ;
#13229=AXIS2_PLACEMENT_3D ( 'NONE', #57261, #45986, #8341 ) ;
#13233=DIRECTION ( 'NONE',  ( -1.000000000000000000, 0.000000000000000000, 0.000000000000000000 ) ) ;
#13239=VECTOR ( 'NONE', #32049, 1000.000000000000000 ) ;
#13245=DIRECTION ( 'NONE',  ( -1.000000000000000000, 0.000000000000000000, 0.000000000000000000 ) ) ;
#13247=EDGE_CURVE ( 'NONE', #4586, #11727, #65929, .T. ) ;
#13259=EDGE_CURVE ( 'NONE', #52158, #16575, #26301, .T. ) ;
#13286=AXIS2_PLACEMENT_3D ( 'NONE', #31538, #20259, #25536 ) ;
#13288=CARTESIAN_POINT ( 'NONE',  ( 0.000000000000000000, 37.16516213103285082, -4.992566952384588141 ) ) ;
#13299=ORIENTED_EDGE ( 'NONE', *, *, #58326, .T. ) ;
#13310=EDGE_CURVE ( 'NONE', #57603, #26180, #32304, .T. ) ;
#13315=ORIENTED_EDGE ( 'NONE', *, *, #12364, .F. ) ;
#13335=DIRECTION ( 'NONE',  ( -1.000000000000000000, 0.000000000000000000, 0.000000000000000000 ) ) ;
#13367=CARTESIAN_POINT ( 'NONE',  ( 10.00000000000000000, 37.58145647212453611, 0.6853352020791767529 ) ) ;
#13377=VERTEX_POINT ( 'NONE', #32887 ) ;
#13392=EDGE_CURVE ( 'NONE', #34044, #24357, #27636, .T. ) ;
#13393=DIRECTION ( 'NONE',  ( 0.000000000000000000, 0.000000000000000000, 1.000000000000000000 ) ) ;
#13396=DIRECTION ( 'NONE',  ( -1.000000000000000000, -0.000000000000000000, -0.000000000000000000 ) ) ;
#13403=ORIENTED_EDGE ( 'NONE', *, *, #71382, .F. ) ;
#13445=AXIS2_PLACEMENT_3D ( 'NONE', #19265, #53119, #42577 ) ;
#13453=DIRECTION ( 'NONE',  ( 0.000000000000000000, 0.000000000000000000, -1.000000000000000000 ) ) ;
#13455=DIRECTION ( 'NONE',  ( 0.000000000000000000, 0.000000000000000000, -1.000000000000000000 ) ) ;
#13457=CARTESIAN_POINT ( 'NONE',  ( 0.000000000000000000, 0.000000000000000000, 0.000000000000000000 ) ) ;
#13467=DIRECTION ( 'NONE',  ( -1.000000000000000000, -0.000000000000000000, -0.000000000000000000 ) ) ;
#13485=ORIENTED_EDGE ( 'NONE', *, *, #51929, .T. ) ;
#13513=EDGE_CURVE ( 'NONE', #72913, #72132, #51537, .T. ) ;
#13521=EDGE_CURVE ( 'NONE', #21663, #62600, #38334, .T. ) ;
#13528=CYLINDRICAL_SURFACE ( 'NONE', #31451, 16.00000000000000000 ) ;
#13530=FACE_OUTER_BOUND ( 'NONE', #17130, .T. ) ;
#13533=CIRCLE ( 'NONE', #8763, 42.00000000000000000 ) ;
#13543=CARTESIAN_POINT ( 'NONE',  ( 10.00000000000000000, 38.55633173627034438, -16.65560815589369881 ) ) ;
#13563=ORIENTED_EDGE ( 'NONE', *, *, #40248, .F. ) ;
#13571=ORIENTED_EDGE ( 'NONE', *, *, #35543, .T. ) ;
#13577=ORIENTED_EDGE ( 'NONE', *, *, #4530, .T. ) ;
#13608=ORIENTED_EDGE ( 'NONE', *, *, #9185, .F. ) ;
#13619=DIRECTION ( 'NONE',  ( -1.000000000000000000, -0.000000000000000000, 0.000000000000000000 ) ) ;
#13634=CARTESIAN_POINT ( 'NONE',  ( -10.00000000000000000, 0.000000000000000000, 0.000000000000000000 ) ) ;
#13639=DIRECTION ( 'NONE',  ( 0.000000000000000000, -0.8910065241883722287, 0.4539904997395382558 ) ) ;
#13650=CARTESIAN_POINT ( 'NONE',  ( 10.00000000000000000, 31.52238457039599595, 27.75498641678753842 ) ) ;
#13672=VECTOR ( 'NONE', #53089, 1000.000000000000000 ) ;
#13679=VERTEX_POINT ( 'NONE', #32066 ) ;
#13684=CARTESIAN_POINT ( 'NONE',  ( 5.000000000000000000, 3.925862922256160736, 41.81611651403863306 ) ) ;
#13688=CYLINDRICAL_SURFACE ( 'NONE', #41663, 16.00000000000000000 ) ;
#13696=AXIS2_PLACEMENT_3D ( 'NONE', #4713, #62209, #34364 ) ;
#13705=CIRCLE ( 'NONE', #30551, 37.49900000000000944 ) ;
#13706=DIRECTION ( 'NONE',  ( -0.000000000000000000, 6.938893903907229364E-16, 1.000000000000000000 ) ) ;
#13727=DIRECTION ( 'NONE',  ( -1.000000000000000000, 0.000000000000000000, 0.000000000000000000 ) ) ;
#13785=ORIENTED_EDGE ( 'NONE', *, *, #62650, .F. ) ;
#13799=ADVANCED_FACE ( 'NONE', ( #21152 ), #39209, .T. ) ;
#13805=DIRECTION ( 'NONE',  ( 0.000000000000000000, 0.8910065241883688980, -0.4539904997395447506 ) ) ;
#13826=EDGE_CURVE ( 'NONE', #22970, #72597, #50090, .T. ) ;
#13831=VERTEX_POINT ( 'NONE', #44100 ) ;
#13840=AXIS2_PLACEMENT_3D ( 'NONE', #69373, #40814, #6953 ) ;
#13846=ORIENTED_EDGE ( 'NONE', *, *, #9395, .T. ) ;
#13864=VECTOR ( 'NONE', #45261, 1000.000000000000000 ) ;
#13869=VERTEX_POINT ( 'NONE', #32441 ) ;
#13877=DIRECTION ( 'NONE',  ( -1.000000000000000000, -0.000000000000000000, -0.000000000000000000 ) ) ;
#13880=ORIENTED_EDGE ( 'NONE', *, *, #28169, .F. ) ;
#13901=CARTESIAN_POINT ( 'NONE',  ( 0.000000000000000000, 16.45098606841173705, -33.79645857604496229 ) ) ;
#13979=DIRECTION ( 'NONE',  ( 0.000000000000000000, 0.000000000000000000, 1.000000000000000000 ) ) ;
#13980=DIRECTION ( 'NONE',  ( 0.000000000000000000, 0.7071067811865439090, 0.7071067811865512365 ) ) ;
#14007=DIRECTION ( 'NONE',  ( 0.000000000000000000, 0.000000000000000000, 1.000000000000000000 ) ) ;
#14008=FACE_OUTER_BOUND ( 'NONE', #25611, .T. ) ;
#14014=FACE_OUTER_BOUND ( 'NONE', #35026, .T. ) ;
#14027=VECTOR ( 'NONE', #58590, 1000.000000000000000 ) ;
#14049=DIRECTION ( 'NONE',  ( 1.000000000000000000, -0.000000000000000000, -0.000000000000000000 ) ) ;
#14051=DIRECTION ( 'NONE',  ( 1.000000000000000000, -0.000000000000000000, -0.000000000000000000 ) ) ;
#14060=DIRECTION ( 'NONE',  ( 1.000000000000000000, -0.000000000000000000, -0.000000000000000000 ) ) ;
#14062=CARTESIAN_POINT ( 'NONE',  ( 0.000000000000000000, 22.48208911017500355, 35.47612816024530957 ) ) ;
#14065=CIRCLE ( 'NONE', #53681, 37.49900000000001654 ) ;
#14089=DIRECTION ( 'NONE',  ( 0.000000000000000000, 0.1564344650402312298, -0.9876883405951375483 ) ) ;
#14109=FACE_OUTER_BOUND ( 'NONE', #67747, .T. ) ;
#14111=VECTOR ( 'NONE', #33749, 1000.000000000000000 ) ;
#14124=DIRECTION ( 'NONE',  ( -1.000000000000000000, -0.000000000000000000, 0.000000000000000000 ) ) ;
#14135=CIRCLE ( 'NONE', #34594, 37.49900000000000944 ) ;
#14153=DIRECTION ( 'NONE',  ( -1.000000000000000000, 0.000000000000000000, -0.000000000000000000 ) ) ;
#14159=ORIENTED_EDGE ( 'NONE', *, *, #34709, .F. ) ;
#14179=AXIS2_PLACEMENT_3D ( 'NONE', #43792, #4686, #10670 ) ;
#14196=AXIS2_PLACEMENT_3D ( 'NONE', #69982, #53445, #59096 ) ;
#14214=VERTEX_POINT ( 'NONE', #9801 ) ;
#14217=CIRCLE ( 'NONE', #59870, 42.00000000000000000 ) ;
#14232=ORIENTED_EDGE ( 'NONE', *, *, #32909, .F. ) ;
#14234=DIRECTION ( 'NONE',  ( 1.000000000000000000, 0.000000000000000000, 0.000000000000000000 ) ) ;
#14256=ORIENTED_EDGE ( 'NONE', *, *, #44687, .T. ) ;
#14260=ORIENTED_EDGE ( 'NONE', *, *, #8407, .F. ) ;
#14263=ORIENTED_EDGE ( 'NONE', *, *, #7828, .T. ) ;
#14264=DIRECTION ( 'NONE',  ( -1.000000000000000000, 0.000000000000000000, 0.000000000000000000 ) ) ;
#14279=CYLINDRICAL_SURFACE ( 'NONE', #70676, 16.00000000000000000 ) ;
#14286=AXIS2_PLACEMENT_3D ( 'NONE', #33051, #9763, #43625 ) ;
#14304=ORIENTED_EDGE ( 'NONE', *, *, #36310, .T. ) ;
#14319=EDGE_CURVE ( 'NONE', #49855, #47001, #14065, .T. ) ;
#14334=AXIS2_PLACEMENT_3D ( 'NONE', #47555, #8811, #53562 ) ;
#14388=CARTESIAN_POINT ( 'NONE',  ( -10.00000000000000000, 0.000000000000000000, 0.000000000000000000 ) ) ;
#14396=CARTESIAN_POINT ( 'NONE',  ( 10.00000000000000000, 35.95386929396241271, 10.96151621346552751 ) ) ;
#14419=ORIENTED_EDGE ( 'NONE', *, *, #43238, .T. ) ;
#14430=LINE ( 'NONE', #24971, #7907 ) ;
#14434=DIRECTION ( 'NONE',  ( -1.000000000000000000, -0.000000000000000000, 0.000000000000000000 ) ) ;
#14444=CARTESIAN_POINT ( 'NONE',  ( 0.000000000000000000, 30.00120703465205452, 22.64427369931179967 ) ) ;
#14449=VERTEX_POINT ( 'NONE', #29674 ) ;
#14452=ADVANCED_FACE ( 'NONE', ( #24074 ), #30055, .T. ) ;
#14459=EDGE_CURVE ( 'NONE', #420, #12638, #62114, .T. ) ;
#14497=FACE_OUTER_BOUND ( 'NONE', #8510, .T. ) ;
#14500=CARTESIAN_POINT ( 'NONE',  ( 10.00000000000000000, 0.000000000000000000, 0.000000000000000000 ) ) ;
#14502=DIRECTION ( 'NONE',  ( -1.000000000000000000, 0.000000000000000000, -0.000000000000000000 ) ) ;
#14530=DIRECTION ( 'NONE',  ( 0.000000000000000000, -0.7071067811865389130, -0.7071067811865563435 ) ) ;
#14534=DIRECTION ( 'NONE',  ( -1.000000000000000000, -0.000000000000000000, 0.000000000000000000 ) ) ;
#14540=ORIENTED_EDGE ( 'NONE', *, *, #46870, .F. ) ;
#14549=VERTEX_POINT ( 'NONE', #18772 ) ;
#14551=CIRCLE ( 'NONE', #62561, 15.99999999999999645 ) ;
#14557=CARTESIAN_POINT ( 'NONE',  ( 0.000000000000000000, 0.000000000000000000, 0.000000000000000000 ) ) ;
#14575=VERTEX_POINT ( 'NONE', #64650 ) ;
#14576=CIRCLE ( 'NONE', #20595, 16.00000000000000000 ) ;
#14586=CARTESIAN_POINT ( 'NONE',  ( 10.00000000000000000, -41.91543099594816368, -2.663952781846588014 ) ) ;
#14606=ADVANCED_FACE ( 'NONE', ( #55216 ), #32645, .T. ) ;
#14616=VERTEX_POINT ( 'NONE', #3370 ) ;
#14628=CARTESIAN_POINT ( 'NONE',  ( 0.000000000000000000, -32.34446384429951138, -26.79245525562750530 ) ) ;
#14653=AXIS2_PLACEMENT_3D ( 'NONE', #61256, #33396, #3752 ) ;
#14666=CARTESIAN_POINT ( 'NONE',  ( 10.00000000000000000, 36.13751322684419165, 21.40280677340384230 ) ) ;
#14673=EDGE_LOOP ( 'NONE', ( #36273, #60285, #20639, #34896 ) ) ;
#14694=ORIENTED_EDGE ( 'NONE', *, *, #12230, .T. ) ;
#14701=ORIENTED_EDGE ( 'NONE', *, *, #12463, .T. ) ;
#14702=VERTEX_POINT ( 'NONE', #55962 ) ;
#14706=CARTESIAN_POINT ( 'NONE',  ( 0.000000000000000000, -35.95386929396248377, -10.96151621346525751 ) ) ;
#14730=AXIS2_PLACEMENT_3D ( 'NONE', #16217, #27494, #55704 ) ;
#14743=DIRECTION ( 'NONE',  ( 1.000000000000000000, 0.000000000000000000, 0.000000000000000000 ) ) ;
#14779=ORIENTED_EDGE ( 'NONE', *, *, #32489, .T. ) ;
#14827=CARTESIAN_POINT ( 'NONE',  ( 10.00000000000000000, 0.000000000000000000, 0.000000000000000000 ) ) ;
#14846=EDGE_CURVE ( 'NONE', #62600, #20222, #23607, .T. ) ;
#14893=CARTESIAN_POINT ( 'NONE',  ( 10.00000000000000000, -10.96151621346514382, 35.95386929396252640 ) ) ;
#14895=ORIENTED_EDGE ( 'NONE', *, *, #10776, .F. ) ;
#14906=LINE ( 'NONE', #25814, #2640 ) ;
#14908=CARTESIAN_POINT ( 'NONE',  ( -10.00000000000000000, 0.000000000000000000, 0.000000000000000000 ) ) ;
#14911=CARTESIAN_POINT ( 'NONE',  ( 0.000000000000000000, -37.01155633439053361, -6.555932627142825986 ) ) ;
#14921=ORIENTED_EDGE ( 'NONE', *, *, #215, .T. ) ;
#14935=EDGE_CURVE ( 'NONE', #26601, #16458, #27874, .T. ) ;
#14974=ORIENTED_EDGE ( 'NONE', *, *, #3016, .T. ) ;
#14979=CYLINDRICAL_SURFACE ( 'NONE', #39492, 37.49900000000000233 ) ;
#15009=EDGE_CURVE ( 'NONE', #45314, #21818, #8154, .T. ) ;
#15034=CARTESIAN_POINT ( 'NONE',  ( 4.999999999999999112, 41.81611651403868990, -3.925862922255709542 ) ) ;
#15056=AXIS2_PLACEMENT_3D ( 'NONE', #69238, #56492, #50460 ) ;
#15093=DIRECTION ( 'NONE',  ( 0.000000000000000000, 0.000000000000000000, 1.000000000000000000 ) ) ;
#15112=CARTESIAN_POINT ( 'NONE',  ( 10.00000000000000000, -17.67226234102801286, -33.17418723428327354 ) ) ;
#15115=CIRCLE ( 'NONE', #37979, 42.00000000000000000 ) ;
#15132=CYLINDRICAL_SURFACE ( 'NONE', #27069, 16.00000000000000000 ) ;
#15136=VECTOR ( 'NONE', #50118, 1000.000000000000000 ) ;
#15143=ORIENTED_EDGE ( 'NONE', *, *, #59160, .F. ) ;
#15153=EDGE_LOOP ( 'NONE', ( #11304, #67609, #5409, #53259 ) ) ;
#15171=DIRECTION ( 'NONE',  ( -1.000000000000000000, -0.000000000000000000, 0.000000000000000000 ) ) ;
#15212=CIRCLE ( 'NONE', #25993, 42.00000000000000000 ) ;
#15215=EDGE_CURVE ( 'NONE', #19149, #61856, #43562, .T. ) ;
#15242=EDGE_CURVE ( 'NONE', #68973, #39661, #27973, .T. ) ;
#15248=EDGE_CURVE ( 'NONE', #11372, #73020, #17139, .T. ) ;
#15264=VERTEX_POINT ( 'NONE', #67011 ) ;
#15275=EDGE_CURVE ( 'NONE', #72197, #54634, #7542, .T. ) ;
#15326=LINE ( 'NONE', #48803, #64547 ) ;
#15329=ADVANCED_FACE ( 'NONE', ( #21141 ), #32425, .T. ) ;
#15335=DIRECTION ( 'NONE',  ( 1.000000000000000000, 0.000000000000000000, 0.000000000000000000 ) ) ;
#15341=VERTEX_POINT ( 'NONE', #39192 ) ;
#15354=ORIENTED_EDGE ( 'NONE', *, *, #3244, .T. ) ;
#15365=ORIENTED_EDGE ( 'NONE', *, *, #41767, .F. ) ;
#15431=CIRCLE ( 'NONE', #61117, 16.00000000000000000 ) ;
#15447=DIRECTION ( 'NONE',  ( 1.000000000000000000, -0.000000000000000000, 0.000000000000000000 ) ) ;
#15450=AXIS2_PLACEMENT_3D ( 'NONE', #44120, #72669, #53931 ) ;
#15471=AXIS2_PLACEMENT_3D ( 'NONE', #44344, #38705, #10123 ) ;
#15480=ORIENTED_EDGE ( 'NONE', *, *, #40609, .F. ) ;
#15489=CARTESIAN_POINT ( 'NONE',  ( 10.00000000000000000, 0.000000000000000000, 0.000000000000000000 ) ) ;
#15491=AXIS2_PLACEMENT_3D ( 'NONE', #10438, #60839, #43567 ) ;
#15498=CARTESIAN_POINT ( 'NONE',  ( 10.00000000000000000, 0.000000000000000000, 0.000000000000000000 ) ) ;
#15501=CYLINDRICAL_SURFACE ( 'NONE', #11403, 16.00000000000000000 ) ;
#15504=EDGE_LOOP ( 'NONE', ( #47525, #5393, #783, #48735, #62229, #40985 ) ) ;
#15509=ORIENTED_EDGE ( 'NONE', *, *, #13310, .F. ) ;
#15535=AXIS2_PLACEMENT_3D ( 'NONE', #58280, #53017, #24435 ) ;
#15536=EDGE_LOOP ( 'NONE', ( #68156, #65151, #62973, #23765 ) ) ;
#15545=CARTESIAN_POINT ( 'NONE',  ( -10.00000000000000000, 0.000000000000000000, 0.000000000000000000 ) ) ;
#15563=DIRECTION ( 'NONE',  ( 0.000000000000000000, 0.000000000000000000, 1.000000000000000000 ) ) ;
#15565=DIRECTION ( 'NONE',  ( 0.000000000000000000, 0.000000000000000000, -1.000000000000000000 ) ) ;
#15573=DIRECTION ( 'NONE',  ( 1.000000000000000000, 0.000000000000000000, 0.000000000000000000 ) ) ;
#15577=CARTESIAN_POINT ( 'NONE',  ( 0.000000000000000000, 0.000000000000000000, 0.000000000000000000 ) ) ;
#15579=ORIENTED_EDGE ( 'NONE', *, *, #34806, .F. ) ;
#15584=CARTESIAN_POINT ( 'NONE',  ( 0.000000000000000000, -35.38097989696520074, 12.42422080174625520 ) ) ;
#15586=CARTESIAN_POINT ( 'NONE',  ( 0.000000000000000000, 0.000000000000000000, 0.000000000000000000 ) ) ;
#15592=EDGE_CURVE ( 'NONE', #69529, #20602, #41230, .T. ) ;
#15598=DIRECTION ( 'NONE',  ( -1.000000000000000000, -0.000000000000000000, 0.000000000000000000 ) ) ;
#15606=AXIS2_PLACEMENT_3D ( 'NONE', #38253, #55173, #8946 ) ;
#15611=DIRECTION ( 'NONE',  ( -1.000000000000000000, -0.000000000000000000, 0.000000000000000000 ) ) ;
#15618=ORIENTED_EDGE ( 'NONE', *, *, #20561, .T. ) ;
#15647=VERTEX_POINT ( 'NONE', #58152 ) ;
#15666=AXIS2_PLACEMENT_3D ( 'NONE', #17816, #46398, #64072 ) ;
#15667=AXIS2_PLACEMENT_3D ( 'NONE', #33910, #57601, #68127 ) ;
#15674=ORIENTED_EDGE ( 'NONE', *, *, #52301, .T. ) ;
#15705=ORIENTED_EDGE ( 'NONE', *, *, #3664, .F. ) ;
#15714=EDGE_CURVE ( 'NONE', #25323, #9618, #37071, .T. ) ;
#15729=ORIENTED_EDGE ( 'NONE', *, *, #10174, .F. ) ;
#15755=FACE_OUTER_BOUND ( 'NONE', #43958, .T. ) ;
#15761=DIRECTION ( 'NONE',  ( 0.000000000000000000, 0.000000000000000000, 1.000000000000000000 ) ) ;
#15768=CARTESIAN_POINT ( 'NONE',  ( 10.00000000000000000, 37.48860685352291000, -0.8828120875901940279 ) ) ;
#15811=AXIS2_PLACEMENT_3D ( 'NONE', #72031, #26544, #65669 ) ;
#15821=ORIENTED_EDGE ( 'NONE', *, *, #13392, .F. ) ;
#15822=CARTESIAN_POINT ( 'NONE',  ( 10.00000000000000000, -30.00120703465222149, 22.64427369931158296 ) ) ;
#15825=ORIENTED_EDGE ( 'NONE', *, *, #60469, .T. ) ;
#15827=DIRECTION ( 'NONE',  ( 0.000000000000000000, 0.9510565162951544194, -0.3090169943749446757 ) ) ;
#15841=ORIENTED_EDGE ( 'NONE', *, *, #6378, .F. ) ;
#15850=ORIENTED_EDGE ( 'NONE', *, *, #73943, .F. ) ;
#15894=CARTESIAN_POINT ( 'NONE',  ( 0.000000000000000000, 0.000000000000000000, 0.000000000000000000 ) ) ;
#15919=DIRECTION ( 'NONE',  ( -1.000000000000000000, -0.000000000000000000, -0.000000000000000000 ) ) ;
#15943=CYLINDRICAL_SURFACE ( 'NONE', #11982, 16.00000000000000000 ) ;
#15954=CARTESIAN_POINT ( 'NONE',  ( 10.00000000000000000, -21.53537804866103045, 30.80686688397002371 ) ) ;
#15977=ADVANCED_FACE ( 'NONE', ( #68623 ), #18124, .T. ) ;
#15979=EDGE_LOOP ( 'NONE', ( #31586, #54749, #53526, #43146 ) ) ;
#15997=CARTESIAN_POINT ( 'NONE',  ( 10.00000000000000000, 0.000000000000000000, 37.49900000000000233 ) ) ;
#16018=VERTEX_POINT ( 'NONE', #38556 ) ;
#16022=AXIS2_PLACEMENT_3D ( 'NONE', #13901, #30826, #53037 ) ;
#16036=VECTOR ( 'NONE', #52164, 1000.000000000000000 ) ;
#16046=CARTESIAN_POINT ( 'NONE',  ( 0.000000000000000000, 33.00180498840072829, -17.80606268964504935 ) ) ;
#16055=DIRECTION ( 'NONE',  ( 0.000000000000000000, 0.4539904997395479702, -0.8910065241883673437 ) ) ;
#16072=CIRCLE ( 'NONE', #40119, 16.00000000000000000 ) ;
#16080=DIRECTION ( 'NONE',  ( -1.000000000000000000, 0.000000000000000000, 0.000000000000000000 ) ) ;
#16085=ORIENTED_EDGE ( 'NONE', *, *, #17382, .F. ) ;
#16113=EDGE_LOOP ( 'NONE', ( #28206, #45602, #63088, #22779 ) ) ;
#16118=DIRECTION ( 'NONE',  ( 0.000000000000000000, -0.3090169943749548342, 0.9510565162951511997 ) ) ;
#16127=DIRECTION ( 'NONE',  ( 0.000000000000000000, 0.000000000000000000, 1.000000000000000000 ) ) ;
#16131=AXIS2_PLACEMENT_3D ( 'NONE', #54710, #3609, #26129 ) ;
#16133=FACE_OUTER_BOUND ( 'NONE', #56887, .T. ) ;
#16148=DIRECTION ( 'NONE',  ( -1.000000000000000000, 0.000000000000000000, 0.000000000000000000 ) ) ;
#16154=CIRCLE ( 'NONE', #48568, 16.00000000000000000 ) ;
#16163=ORIENTED_EDGE ( 'NONE', *, *, #70365, .F. ) ;
#16169=VERTEX_POINT ( 'NONE', #19221 ) ;
#16171=ORIENTED_EDGE ( 'NONE', *, *, #46524, .T. ) ;
#16174=EDGE_LOOP ( 'NONE', ( #35942, #39851, #66334, #23510 ) ) ;
#16182=ADVANCED_FACE ( 'NONE', ( #48537 ), #71452, .T. ) ;
#16202=ORIENTED_EDGE ( 'NONE', *, *, #4115, .T. ) ;
#16207=CARTESIAN_POINT ( 'NONE',  ( 0.000000000000000000, 35.53030884539102630, -12.26510123303222599 ) ) ;
#16217=CARTESIAN_POINT ( 'NONE',  ( 10.00000000000000000, 37.58145647212455032, -0.6853352020786441789 ) ) ;
#16220=DIRECTION ( 'NONE',  ( 0.000000000000000000, 0.000000000000000000, -1.000000000000000000 ) ) ;
#16230=DIRECTION ( 'NONE',  ( -1.000000000000000000, 0.000000000000000000, 0.000000000000000000 ) ) ;
#16244=ORIENTED_EDGE ( 'NONE', *, *, #58984, .T. ) ;
#16262=EDGE_LOOP ( 'NONE', ( #32697, #27886, #36822, #45695 ) ) ;
#16287=DIRECTION ( 'NONE',  ( 0.000000000000000000, -0.4539904997395352027, -0.8910065241883737830 ) ) ;
#16321=VERTEX_POINT ( 'NONE', #11634 ) ;
#16354=EDGE_LOOP ( 'NONE', ( #25116, #32640, #43174, #61679 ) ) ;
#16364=ORIENTED_EDGE ( 'NONE', *, *, #17425, .F. ) ;
#16395=CARTESIAN_POINT ( 'NONE',  ( 10.00000000000000000, 37.58145647212453611, 0.6853352020791767529 ) ) ;
#16416=CIRCLE ( 'NONE', #27175, 37.49900000000000233 ) ;
#16428=CARTESIAN_POINT ( 'NONE',  ( 10.00000000000000000, 32.34446384430010113, -26.79245525562679831 ) ) ;
#16430=DIRECTION ( 'NONE',  ( -1.000000000000000000, 0.000000000000000000, -0.000000000000000000 ) ) ;
#16436=AXIS2_PLACEMENT_3D ( 'NONE', #7528, #1926, #42484 ) ;
#16458=VERTEX_POINT ( 'NONE', #22566 ) ;
#16474=DIRECTION ( 'NONE',  ( 0.000000000000000000, 0.5877852522924744694, -0.8090169943749465631 ) ) ;
#16479=DIRECTION ( 'NONE',  ( -1.000000000000000000, 0.000000000000000000, -0.000000000000000000 ) ) ;
#16490=ORIENTED_EDGE ( 'NONE', *, *, #29547, .F. ) ;
#16496=ORIENTED_EDGE ( 'NONE', *, *, #45452, .T. ) ;
#16504=CARTESIAN_POINT ( 'NONE',  ( 10.00000000000000000, 12.42422080174688404, -35.38097989696498047 ) ) ;
#16516=CARTESIAN_POINT ( 'NONE',  ( 0.000000000000000000, 35.38097989696528600, -12.42422080174602605 ) ) ;
#16532=ORIENTED_EDGE ( 'NONE', *, *, #51632, .F. ) ;
#16535=CIRCLE ( 'NONE', #10519, 16.00000000000000000 ) ;
#16543=ORIENTED_EDGE ( 'NONE', *, *, #36310, .F. ) ;
#16547=AXIS2_PLACEMENT_3D ( 'NONE', #841, #64328, #57946 ) ;
#16551=EDGE_LOOP ( 'NONE', ( #5683, #73849, #26170, #11533 ) ) ;
#16554=CARTESIAN_POINT ( 'NONE',  ( 5.000000000000000000, -22.48208911017474065, -35.47612816024548721 ) ) ;
#16575=VERTEX_POINT ( 'NONE', #18033 ) ;
#16581=DIRECTION ( 'NONE',  ( 1.000000000000000000, 0.000000000000000000, -0.000000000000000000 ) ) ;
#16587=DIRECTION ( 'NONE',  ( 0.000000000000000000, 0.000000000000000000, 1.000000000000000000 ) ) ;
#16597=CIRCLE ( 'NONE', #52594, 37.49900000000001654 ) ;
#16615=EDGE_CURVE ( 'NONE', #60292, #7320, #52122, .T. ) ;
#16621=VECTOR ( 'NONE', #70399, 1000.000000000000000 ) ;
#16631=ORIENTED_EDGE ( 'NONE', *, *, #12021, .T. ) ;
#16648=CIRCLE ( 'NONE', #58673, 42.00000000000000000 ) ;
#16691=DIRECTION ( 'NONE',  ( -1.000000000000000000, -0.000000000000000000, 0.000000000000000000 ) ) ;
#16746=VERTEX_POINT ( 'NONE', #19865 ) ;
#16751=EDGE_CURVE ( 'NONE', #60033, #66693, #70142, .T. ) ;
#16754=DIRECTION ( 'NONE',  ( -1.000000000000000000, 0.000000000000000000, -0.000000000000000000 ) ) ;
#16767=ORIENTED_EDGE ( 'NONE', *, *, #17980, .F. ) ;
#16775=DIRECTION ( 'NONE',  ( 0.000000000000000000, 0.3090169943749480619, -0.9510565162951533091 ) ) ;
#16779=ORIENTED_EDGE ( 'NONE', *, *, #70600, .T. ) ;
#16810=EDGE_CURVE ( 'NONE', #37277, #72197, #34868, .T. ) ;
#16814=CIRCLE ( 'NONE', #15450, 42.00000000000000000 ) ;
#16821=VECTOR ( 'NONE', #2674, 1000.000000000000000 ) ;
#16823=ORIENTED_EDGE ( 'NONE', *, *, #68445, .F. ) ;
#16832=AXIS2_PLACEMENT_3D ( 'NONE', #27492, #50426, #44803 ) ;
#16853=VERTEX_POINT ( 'NONE', #4839 ) ;
#16864=VERTEX_POINT ( 'NONE', #27354 ) ;
#16873=ORIENTED_EDGE ( 'NONE', *, *, #40493, .T. ) ;
#16875=ORIENTED_EDGE ( 'NONE', *, *, #19496, .F. ) ;
#16883=CARTESIAN_POINT ( 'NONE',  ( 10.00000000000000000, 0.000000000000000000, 0.000000000000000000 ) ) ;
#16892=EDGE_CURVE ( 'NONE', #69905, #5770, #50289, .T. ) ;
#16894=DIRECTION ( 'NONE',  ( -1.000000000000000000, -0.000000000000000000, -0.000000000000000000 ) ) ;
#16895=ADVANCED_FACE ( 'NONE', ( #61963 ), #10444, .T. ) ;
#16899=CIRCLE ( 'NONE', #56503, 42.00000000000000000 ) ;
#16949=CARTESIAN_POINT ( 'NONE',  ( 10.00000000000000000, -33.80338159004273280, -16.23288003029533044 ) ) ;
#16962=FACE_OUTER_BOUND ( 'NONE', #42623, .T. ) ;
#16968=EDGE_CURVE ( 'NONE', #70509, #68784, #53633, .T. ) ;
#16984=CARTESIAN_POINT ( 'NONE',  ( 0.000000000000000000, -33.17418723428294669, -17.67226234102862747 ) ) ;
#16997=CIRCLE ( 'NONE', #37411, 16.00000000000000000 ) ;
#17002=ADVANCED_FACE ( 'NONE', ( #41250 ), #7772, .T. ) ;
#17011=CARTESIAN_POINT ( 'NONE',  ( 10.00000000000000000, -4.992566952384716927, -37.16516213103282951 ) ) ;
#17017=ORIENTED_EDGE ( 'NONE', *, *, #3824, .T. ) ;
#17029=PRODUCT_CONTEXT ( 'NONE', #41173, 'mechanical' ) ;
#17040=EDGE_LOOP ( 'NONE', ( #21455, #73760, #73903, #34375 ) ) ;
#17054=VECTOR ( 'NONE', #27485, 1000.000000000000000 ) ;
#17060=EDGE_CURVE ( 'NONE', #40680, #5770, #62995, .T. ) ;
#17071=EDGE_CURVE ( 'NONE', #30533, #15341, #65391, .T. ) ;
#17084=ORIENTED_EDGE ( 'NONE', *, *, #7128, .F. ) ;
#17094=EDGE_CURVE ( 'NONE', #16458, #32536, #7024, .T. ) ;
#17103=ORIENTED_EDGE ( 'NONE', *, *, #42950, .T. ) ;
#17130=EDGE_LOOP ( 'NONE', ( #38423, #4277, #29296, #44218 ) ) ;
#17138=ORIENTED_EDGE ( 'NONE', *, *, #60798, .T. ) ;
#17139=LINE ( 'NONE', #40072, #8770 ) ;
#17192=CARTESIAN_POINT ( 'NONE',  ( 5.000000000000000000, -15.48615015657610705, 39.04073710021338428 ) ) ;
#17198=CARTESIAN_POINT ( 'NONE',  ( 10.00000000000000000, 0.000000000000000000, 0.000000000000000000 ) ) ;
#17200=ORIENTED_EDGE ( 'NONE', *, *, #8574, .F. ) ;
#17205=AXIS2_PLACEMENT_3D ( 'NONE', #2593, #17988, #7075 ) ;
#17230=EDGE_LOOP ( 'NONE', ( #18205, #57327, #50182, #15825 ) ) ;
#17237=VECTOR ( 'NONE', #73184, 1000.000000000000000 ) ;
#17242=DIRECTION ( 'NONE',  ( -1.000000000000000000, 0.000000000000000000, -0.000000000000000000 ) ) ;
#17248=AXIS2_PLACEMENT_3D ( 'NONE', #34109, #49904, #5562 ) ;
#17271=CIRCLE ( 'NONE', #66482, 16.00000000000000000 ) ;
#17280=CARTESIAN_POINT ( 'NONE',  ( 10.00000000000000000, 0.000000000000000000, 0.000000000000000000 ) ) ;
#17284=ORIENTED_EDGE ( 'NONE', *, *, #31670, .T. ) ;
#17288=( NAMED_UNIT ( * ) SI_UNIT ( $, .STERADIAN. ) SOLID_ANGLE_UNIT ( ) );
#17294=EDGE_LOOP ( 'NONE', ( #44961, #67940, #56505, #28191 ) ) ;
#17298=DIRECTION ( 'NONE',  ( -1.000000000000000000, 0.000000000000000000, -0.000000000000000000 ) ) ;
#17300=ORIENTED_EDGE ( 'NONE', *, *, #31126, .F. ) ;
#17315=EDGE_CURVE ( 'NONE', #70504, #53075, #10358, .T. ) ;
#17319=CIRCLE ( 'NONE', #7713, 16.00000000000000000 ) ;
#17323=ADVANCED_FACE ( 'NONE', ( #68256 ), #68997, .T. ) ;
#17332=DIRECTION ( 'NONE',  ( -1.000000000000000000, -0.000000000000000000, 0.000000000000000000 ) ) ;
#17338=CYLINDRICAL_SURFACE ( 'NONE', #32249, 42.00000000000000000 ) ;
#17345=EDGE_CURVE ( 'NONE', #56703, #47902, #39692, .T. ) ;
#17373=CYLINDRICAL_SURFACE ( 'NONE', #52679, 37.49900000000000233 ) ;
#17378=ORIENTED_EDGE ( 'NONE', *, *, #45699, .T. ) ;
#17380=ORIENTED_EDGE ( 'NONE', *, *, #12066, .T. ) ;
#17382=EDGE_CURVE ( 'NONE', #56343, #37995, #23064, .T. ) ;
#17385=VERTEX_POINT ( 'NONE', #15997 ) ;
#17392=ORIENTED_EDGE ( 'NONE', *, *, #29769, .F. ) ;
#17409=VECTOR ( 'NONE', #21042, 1000.000000000000000 ) ;
#17419=AXIS2_PLACEMENT_3D ( 'NONE', #12906, #64068, #23466 ) ;
#17420=DIRECTION ( 'NONE',  ( -1.000000000000000000, 0.000000000000000000, -0.000000000000000000 ) ) ;
#17425=EDGE_CURVE ( 'NONE', #37277, #19782, #21865, .T. ) ;
#17446=DIRECTION ( 'NONE',  ( -1.000000000000000000, 0.000000000000000000, 0.000000000000000000 ) ) ;
#17447=VERTEX_POINT ( 'NONE', #69355 ) ;
#17458=AXIS2_PLACEMENT_3D ( 'NONE', #35944, #69418, #28831 ) ;
#17461=ORIENTED_EDGE ( 'NONE', *, *, #3327, .T. ) ;
#17470=EDGE_CURVE ( 'NONE', #67105, #633, #36237, .T. ) ;
#17479=EDGE_CURVE ( 'NONE', #47114, #62549, #50677, .T. ) ;
#17507=CYLINDRICAL_SURFACE ( 'NONE', #3610, 37.49900000000000233 ) ;
#17514=DIRECTION ( 'NONE',  ( -1.000000000000000000, -0.000000000000000000, -0.000000000000000000 ) ) ;
#17516=EDGE_CURVE ( 'NONE', #60365, #8457, #36395, .T. ) ;
#17534=CARTESIAN_POINT ( 'NONE',  ( 10.00000000000000000, 33.00180498840046539, 17.80606268964551120 ) ) ;
#17535=DIRECTION ( 'NONE',  ( 0.000000000000000000, -0.8910065241883627918, -0.4539904997395568520 ) ) ;
#17555=CARTESIAN_POINT ( 'NONE',  ( 10.00000000000000000, 0.000000000000000000, 0.000000000000000000 ) ) ;
#17565=ORIENTED_EDGE ( 'NONE', *, *, #57221, .F. ) ;
#17576=CARTESIAN_POINT ( 'NONE',  ( 5.000000000000000000, -36.13751322684404244, -21.40280677340410165 ) ) ;
#17580=EDGE_CURVE ( 'NONE', #22270, #62061, #48280, .T. ) ;
#17587=ORIENTED_EDGE ( 'NONE', *, *, #38449, .F. ) ;
#17589=LINE ( 'NONE', #57820, #16036 ) ;
#17609=CARTESIAN_POINT ( 'NONE',  ( 0.000000000000000000, -12.26510123303234501, -35.53030884539098366 ) ) ;
#17626=CYLINDRICAL_SURFACE ( 'NONE', #44478, 16.00000000000000000 ) ;
#17632=DIRECTION ( 'NONE',  ( 0.000000000000000000, 0.9510565162951521989, 0.3090169943749515591 ) ) ;
#17640=CARTESIAN_POINT ( 'NONE',  ( 10.00000000000000000, 16.45098606841173705, -33.79645857604496229 ) ) ;
#17644=EDGE_CURVE ( 'NONE', #66693, #36199, #8052, .T. ) ;
#17658=ORIENTED_EDGE ( 'NONE', *, *, #12066, .F. ) ;
#17660=CARTESIAN_POINT ( 'NONE',  ( 0.000000000000000000, 41.81611651403861885, 3.925862922256313503 ) ) ;
#17673=ORIENTED_EDGE ( 'NONE', *, *, #70842, .F. ) ;
#17676=EDGE_CURVE ( 'NONE', #7138, #19308, #65582, .T. ) ;
#17682=CIRCLE ( 'NONE', #21251, 42.00000000000000000 ) ;
#17715=DIRECTION ( 'NONE',  ( -1.000000000000000000, 0.000000000000000000, 0.000000000000000000 ) ) ;
#17719=DIRECTION ( 'NONE',  ( 0.000000000000000000, 0.000000000000000000, -1.000000000000000000 ) ) ;
#17723=AXIS2_PLACEMENT_3D ( 'NONE', #7181, #1947, #18092 ) ;
#17727=DIRECTION ( 'NONE',  ( 0.000000000000000000, 0.000000000000000000, -1.000000000000000000 ) ) ;
#17729=ORIENTED_EDGE ( 'NONE', *, *, #57315, .T. ) ;
#17730=EDGE_CURVE ( 'NONE', #36199, #58686, #10129, .T. ) ;
#17733=VERTEX_POINT ( 'NONE', #44116 ) ;
#17745=EDGE_CURVE ( 'NONE', #2059, #7320, #67794, .T. ) ;
#17751=DIRECTION ( 'NONE',  ( -1.000000000000000000, 0.000000000000000000, 0.000000000000000000 ) ) ;
#17757=EDGE_CURVE ( 'NONE', #20440, #10439, #64136, .T. ) ;
#17780=DIRECTION ( 'NONE',  ( -1.000000000000000000, -0.000000000000000000, 0.000000000000000000 ) ) ;
#17802=AXIS2_PLACEMENT_3D ( 'NONE', #1945, #12436, #65071 ) ;
#17816=CARTESIAN_POINT ( 'NONE',  ( 0.000000000000000000, -6.555932627142143865, -37.01155633439065440 ) ) ;
#17832=VECTOR ( 'NONE', #42148, 1000.000000000000000 ) ;
#17840=CYLINDRICAL_SURFACE ( 'NONE', #18870, 42.00000000000000000 ) ;
#17875=LINE ( 'NONE', #1000, #40780 ) ;
#17877=ORIENTED_EDGE ( 'NONE', *, *, #653, .F. ) ;
#17880=DIRECTION ( 'NONE',  ( 0.000000000000000000, -0.9510565162951565288, 0.3090169943749383474 ) ) ;
#17910=CIRCLE ( 'NONE', #46740, 42.00000000000000000 ) ;
#17913=AXIS2_PLACEMENT_3D ( 'NONE', #6811, #29723, #1225 ) ;
#17938=AXIS2_PLACEMENT_3D ( 'NONE', #57002, #5505, #74275 ) ;
#17980=EDGE_CURVE ( 'NONE', #34136, #17385, #20914, .T. ) ;
#17988=DIRECTION ( 'NONE',  ( -1.000000000000000000, -0.000000000000000000, 0.000000000000000000 ) ) ;
#17992=DIRECTION ( 'NONE',  ( -1.000000000000000000, 0.000000000000000000, 0.000000000000000000 ) ) ;
#17993=CARTESIAN_POINT ( 'NONE',  ( 0.000000000000000000, 30.84782396557248418, -21.32104025579081252 ) ) ;
#18016=AXIS2_PLACEMENT_3D ( 'NONE', #15822, #10171, #62444 ) ;
#18022=DIRECTION ( 'NONE',  ( -1.000000000000000000, -0.000000000000000000, 0.000000000000000000 ) ) ;
#18032=( NAMED_UNIT ( * ) SI_UNIT ( $, .STERADIAN. ) SOLID_ANGLE_UNIT ( ) );
#18033=CARTESIAN_POINT ( 'NONE',  ( 10.00000000000000000, 16.65560815589464028, -38.55633173626993937 ) ) ;
#18042=CYLINDRICAL_SURFACE ( 'NONE', #6075, 16.00000000000000000 ) ;
#18053=ORIENTED_EDGE ( 'NONE', *, *, #21142, .T. ) ;
#18057=DIRECTION ( 'NONE',  ( 0.000000000000000000, 0.4539904997395412534, 0.8910065241883706744 ) ) ;
#18074=ADVANCED_FACE ( 'NONE', ( #70735 ), #36902, .T. ) ;
#18087=CYLINDRICAL_SURFACE ( 'NONE', #34170, 16.00000000000000000 ) ;
#18091=CARTESIAN_POINT ( 'NONE',  ( 10.00000000000000000, -16.23288003029473359, -33.80338159004301701 ) ) ;
#18092=DIRECTION ( 'NONE',  ( 0.000000000000000000, 0.000000000000000000, 1.000000000000000000 ) ) ;
#18104=EDGE_CURVE ( 'NONE', #25146, #23811, #53391, .T. ) ;
#18124=CYLINDRICAL_SURFACE ( 'NONE', #441, 42.00000000000000000 ) ;
#18169=CARTESIAN_POINT ( 'NONE',  ( 10.00000000000000000, -30.84782396557201878, -21.32104025579148399 ) ) ;
#18170=DIRECTION ( 'NONE',  ( -1.000000000000000000, -0.000000000000000000, -0.000000000000000000 ) ) ;
#18195=ORIENTED_EDGE ( 'NONE', *, *, #12391, .F. ) ;
#18196=DIRECTION ( 'NONE',  ( -1.000000000000000000, 0.000000000000000000, 0.000000000000000000 ) ) ;
#18202=AXIS2_PLACEMENT_3D ( 'NONE', #49143, #32207, #21294 ) ;
#18204=ORIENTED_EDGE ( 'NONE', *, *, #44205, .T. ) ;
#18205=ORIENTED_EDGE ( 'NONE', *, *, #12579, .F. ) ;
#18220=EDGE_LOOP ( 'NONE', ( #20483, #48672, #14701, #64275 ) ) ;
#18238=DIRECTION ( 'NONE',  ( 0.000000000000000000, 0.7071067811865437980, 0.7071067811865512365 ) ) ;
#18254=ADVANCED_FACE ( 'NONE', ( #39792 ), #51059, .T. ) ;
#18261=CARTESIAN_POINT ( 'NONE',  ( 10.00000000000000000, 25.88420570971438650, -27.13269053701069566 ) ) ;
#18271=AXIS2_PLACEMENT_3D ( 'NONE', #6585, #53549, #6937 ) ;
#18276=ORIENTED_EDGE ( 'NONE', *, *, #17071, .T. ) ;
#18284=ORIENTED_EDGE ( 'NONE', *, *, #1037, .F. ) ;
#18297=EDGE_CURVE ( 'NONE', #2620, #16169, #10173, .T. ) ;
#18341=VERTEX_POINT ( 'NONE', #41626 ) ;
#18368=AXIS2_PLACEMENT_3D ( 'NONE', #35630, #7071, #46198 ) ;
#18383=ORIENTED_EDGE ( 'NONE', *, *, #29547, .T. ) ;
#18386=EDGE_CURVE ( 'NONE', #8860, #72017, #19771, .T. ) ;
#18391=ADVANCED_FACE ( 'NONE', ( #64205 ), #24343, .T. ) ;
#18393=DIRECTION ( 'NONE',  ( 1.000000000000000000, 0.000000000000000000, 0.000000000000000000 ) ) ;
#18413=DIRECTION ( 'NONE',  ( -1.000000000000000000, 0.000000000000000000, 0.000000000000000000 ) ) ;
#18430=DIRECTION ( 'NONE',  ( 0.000000000000000000, 0.000000000000000000, 1.000000000000000000 ) ) ;
#18432=AXIS2_PLACEMENT_3D ( 'NONE', #30455, #47398, #19550 ) ;
#18434=CYLINDRICAL_SURFACE ( 'NONE', #20525, 16.00000000000000000 ) ;
#18446=CYLINDRICAL_SURFACE ( 'NONE', #41851, 42.00000000000000000 ) ;
#18448=FACE_OUTER_BOUND ( 'NONE', #46424, .T. ) ;
#18454=CARTESIAN_POINT ( 'NONE',  ( 10.00000000000000000, 17.67226234102826510, 33.17418723428314564 ) ) ;
#18457=DIRECTION ( 'NONE',  ( 1.000000000000000000, 0.000000000000000000, 0.000000000000000000 ) ) ;
#18469=CIRCLE ( 'NONE', #13696, 37.49900000000000944 ) ;
#18473=ORIENTED_EDGE ( 'NONE', *, *, #28803, .T. ) ;
#18504=EDGE_LOOP ( 'NONE', ( #38455, #32346, #43103, #22266 ) ) ;
#18517=CARTESIAN_POINT ( 'NONE',  ( 5.000000000000000000, -26.79245525562738095, 32.34446384429961796 ) ) ;
#18559=ORIENTED_EDGE ( 'NONE', *, *, #41656, .F. ) ;
#18563=CARTESIAN_POINT ( 'NONE',  ( 10.00000000000000000, 22.64427369931212297, -30.00120703465181293 ) ) ;
#18586=CYLINDRICAL_SURFACE ( 'NONE', #2736, 16.00000000000000000 ) ;
#18619=DIRECTION ( 'NONE',  ( 0.000000000000000000, -0.8910065241883721177, 0.4539904997395382003 ) ) ;
#18622=DIRECTION ( 'NONE',  ( -1.000000000000000000, 0.000000000000000000, 0.000000000000000000 ) ) ;
#18653=ADVANCED_FACE ( 'NONE', ( #63379 ), #62269, .T. ) ;
#18676=EDGE_CURVE ( 'NONE', #67705, #54680, #10377, .T. ) ;
#18699=CIRCLE ( 'NONE', #5537, 42.00000000000000000 ) ;
#18713=CARTESIAN_POINT ( 'NONE',  ( 10.00000000000000000, -16.45098606841149902, 33.79645857604508308 ) ) ;
#18771=VERTEX_POINT ( 'NONE', #47189 ) ;
#18772=CARTESIAN_POINT ( 'NONE',  ( 10.00000000000000000, 3.925862922256769583, -41.81611651403858332 ) ) ;
#18775=ORIENTED_EDGE ( 'NONE', *, *, #9761, .T. ) ;
#18793=CIRCLE ( 'NONE', #32043, 37.49900000000001654 ) ;
#18820=DIRECTION ( 'NONE',  ( 0.000000000000000000, 0.000000000000000000, 1.000000000000000000 ) ) ;
#18829=VERTEX_POINT ( 'NONE', #46829 ) ;
#18841=ORIENTED_EDGE ( 'NONE', *, *, #1144, .F. ) ;
#18849=EDGE_CURVE ( 'NONE', #49532, #38633, #59582, .T. ) ;
#18868=CARTESIAN_POINT ( 'NONE',  ( 10.00000000000000000, -12.42422080174614862, -35.38097989696524337 ) ) ;
#18870=AXIS2_PLACEMENT_3D ( 'NONE', #63722, #23858, #20054 ) ;
#18885=ORIENTED_EDGE ( 'NONE', *, *, #51632, .T. ) ;
#18893=CARTESIAN_POINT ( 'NONE',  ( 0.000000000000000000, -22.48208911017474065, -35.47612816024548721 ) ) ;
#18916=DIRECTION ( 'NONE',  ( 0.000000000000000000, -0.8090169943749531134, 0.5877852522924653655 ) ) ;
#18922=DIRECTION ( 'NONE',  ( -1.000000000000000000, -0.000000000000000000, -0.000000000000000000 ) ) ;
#18924=ORIENTED_EDGE ( 'NONE', *, *, #32995, .F. ) ;
#18925=CARTESIAN_POINT ( 'NONE',  ( 0.000000000000000000, 0.000000000000000000, 0.000000000000000000 ) ) ;
#18926=EDGE_CURVE ( 'NONE', #21615, #43377, #28253, .T. ) ;
#18937=VERTEX_POINT ( 'NONE', #2839 ) ;
#18952=DIRECTION ( 'NONE',  ( -1.000000000000000000, 0.000000000000000000, -0.000000000000000000 ) ) ;
#18957=CARTESIAN_POINT ( 'NONE',  ( 0.000000000000000000, -37.48860685352291711, 0.8828120875899322373 ) ) ;
#18967=DIRECTION ( 'NONE',  ( 0.000000000000000000, 1.000000000000000000, -9.787530781167598712E-16 ) ) ;
#18973=CIRCLE ( 'NONE', #8131, 16.00000000000000000 ) ;
#18982=AXIS2_PLACEMENT_3D ( 'NONE', #47769, #35740, #47049 ) ;
#18997=EDGE_CURVE ( 'NONE', #73020, #48094, #17319, .T. ) ;
#19012=ORIENTED_EDGE ( 'NONE', *, *, #9838, .T. ) ;
#19027=CARTESIAN_POINT ( 'NONE',  ( 10.00000000000000000, 16.95692799528845640, -2.500000000000000000 ) ) ;
#19037=ORIENTED_EDGE ( 'NONE', *, *, #50225, .T. ) ;
#19046=ORIENTED_EDGE ( 'NONE', *, *, #62327, .T. ) ;
#19064=ORIENTED_EDGE ( 'NONE', *, *, #18297, .T. ) ;
#19067=CIRCLE ( 'NONE', #65888, 15.99999999999999467 ) ;
#19076=CIRCLE ( 'NONE', #61109, 42.00000000000000000 ) ;
#19077=ORIENTED_EDGE ( 'NONE', *, *, #53580, .T. ) ;
#19086=DIRECTION ( 'NONE',  ( -1.000000000000000000, 0.000000000000000000, 0.000000000000000000 ) ) ;
#19099=ORIENTED_EDGE ( 'NONE', *, *, #30013, .T. ) ;
#19116=VECTOR ( 'NONE', #28155, 1000.000000000000000 ) ;
#19132=CIRCLE ( 'NONE', #38348, 15.99999999999999822 ) ;
#19147=ORIENTED_EDGE ( 'NONE', *, *, #13259, .T. ) ;
#19149=VERTEX_POINT ( 'NONE', #21944 ) ;
#19153=ORIENTED_EDGE ( 'NONE', *, *, #667, .F. ) ;
#19167=DIRECTION ( 'NONE',  ( 0.000000000000000000, 0.000000000000000000, 1.000000000000000000 ) ) ;
#19180=EDGE_CURVE ( 'NONE', #729, #13831, #27192, .T. ) ;
#19184=EDGE_CURVE ( 'NONE', #1614, #633, #56542, .T. ) ;
#19215=CARTESIAN_POINT ( 'NONE',  ( 0.000000000000000000, 33.17418723428333749, -17.67226234102790272 ) ) ;
#19221=CARTESIAN_POINT ( 'NONE',  ( 10.00000000000000000, -22.48208911017525580, 35.47612816024516036 ) ) ;
#19240=DIRECTION ( 'NONE',  ( -1.000000000000000000, 0.000000000000000000, 0.000000000000000000 ) ) ;
#19251=VERTEX_POINT ( 'NONE', #536 ) ;
#19265=CARTESIAN_POINT ( 'NONE',  ( 10.00000000000000000, 0.000000000000000000, 0.000000000000000000 ) ) ;
#19300=ORIENTED_EDGE ( 'NONE', *, *, #73261, .F. ) ;
#19302=CARTESIAN_POINT ( 'NONE',  ( 0.000000000000000000, 21.53537804866081373, 30.80686688397018358 ) ) ;
#19303=ORIENTED_EDGE ( 'NONE', *, *, #41867, .T. ) ;
#19308=VERTEX_POINT ( 'NONE', #53111 ) ;
#19337=EDGE_LOOP ( 'NONE', ( #51866, #72938, #31540, #43952 ) ) ;
#19364=CARTESIAN_POINT ( 'NONE',  ( -10.00000000000000000, 0.000000000000000000, 0.000000000000000000 ) ) ;
#19372=DIRECTION ( 'NONE',  ( -1.000000000000000000, 0.000000000000000000, -0.000000000000000000 ) ) ;
#19394=CARTESIAN_POINT ( 'NONE',  ( 10.00000000000000000, 33.79645857604513992, -16.45098606841138178 ) ) ;
#19397=DIRECTION ( 'NONE',  ( 0.000000000000000000, -9.787530781167598712E-16, -1.000000000000000000 ) ) ;
#19401=CARTESIAN_POINT ( 'NONE',  ( 0.000000000000000000, -33.80338159004273280, -16.23288003029533044 ) ) ;
#19405=EDGE_CURVE ( 'NONE', #36301, #20472, #2965, .T. ) ;
#19413=DIRECTION ( 'NONE',  ( 0.000000000000000000, -0.3090169943749349057, -0.9510565162951577500 ) ) ;
#19417=ORIENTED_EDGE ( 'NONE', *, *, #9838, .F. ) ;
#19424=DIRECTION ( 'NONE',  ( -1.000000000000000000, -0.000000000000000000, 0.000000000000000000 ) ) ;
#19437=VECTOR ( 'NONE', #25729, 1000.000000000000000 ) ;
#19445=EDGE_LOOP ( 'NONE', ( #4190, #63960, #47593, #45233 ) ) ;
#19454=DIRECTION ( 'NONE',  ( -1.000000000000000000, 0.000000000000000000, 0.000000000000000000 ) ) ;
#19459=CARTESIAN_POINT ( 'NONE',  ( 0.000000000000000000, 22.64427369931169309, 30.00120703465213623 ) ) ;
#19467=ORIENTED_EDGE ( 'NONE', *, *, #33809, .T. ) ;
#19472=EDGE_LOOP ( 'NONE', ( #11216, #10451, #56146, #47458 ) ) ;
#19489=EDGE_CURVE ( 'NONE', #66589, #14702, #71330, .T. ) ;
#19496=EDGE_CURVE ( 'NONE', #36613, #62068, #8943, .T. ) ;
#19517=ORIENTED_EDGE ( 'NONE', *, *, #28659, .F. ) ;
#19518=ADVANCED_FACE ( 'NONE', ( #57881 ), #6383, .T. ) ;
#19519=ORIENTED_EDGE ( 'NONE', *, *, #32334, .F. ) ;
#19538=AXIS2_PLACEMENT_3D ( 'NONE', #18925, #41872, #41142 ) ;
#19545=DIRECTION ( 'NONE',  ( 1.000000000000000000, 0.000000000000000000, -0.000000000000000000 ) ) ;
#19550=DIRECTION ( 'NONE',  ( 0.000000000000000000, 0.000000000000000000, -1.000000000000000000 ) ) ;
#19566=LINE ( 'NONE', #31587, #61112 ) ;
#19577=EDGE_CURVE ( 'NONE', #55579, #61669, #69520, .T. ) ;
#19583=EDGE_CURVE ( 'NONE', #12638, #15647, #63019, .T. ) ;
#19595=VECTOR ( 'NONE', #2137, 1000.000000000000000 ) ;
#19631=CARTESIAN_POINT ( 'NONE',  ( 10.00000000000000000, 5.202137450156907761, -37.22597642581151689 ) ) ;
#19645=DIRECTION ( 'NONE',  ( 0.000000000000000000, 0.000000000000000000, 1.000000000000000000 ) ) ;
#19650=CIRCLE ( 'NONE', #58098, 16.00000000000000000 ) ;
#19652=DIRECTION ( 'NONE',  ( 0.000000000000000000, -0.9510565162951500895, -0.3090169943749583314 ) ) ;
#19658=CIRCLE ( 'NONE', #37650, 42.00000000000000000 ) ;
#19659=AXIS2_PLACEMENT_3D ( 'NONE', #49600, #21782, #44732 ) ;
#19664=EDGE_CURVE ( 'NONE', #56468, #25977, #1791, .T. ) ;
#19666=CYLINDRICAL_SURFACE ( 'NONE', #34274, 37.49900000000000233 ) ;
#19672=CARTESIAN_POINT ( 'NONE',  ( 10.00000000000000000, 0.000000000000000000, 37.49900000000000233 ) ) ;
#19685=VERTEX_POINT ( 'NONE', #42801 ) ;
#19695=CARTESIAN_POINT ( 'NONE',  ( 0.000000000000000000, -39.04073710021332744, -15.48615015657624028 ) ) ;
#19715=CYLINDRICAL_SURFACE ( 'NONE', #30185, 16.00000000000000000 ) ;
#19727=VECTOR ( 'NONE', #14049, 1000.000000000000000 ) ;
#19735=DIRECTION ( 'NONE',  ( 1.000000000000000000, 0.000000000000000000, 0.000000000000000000 ) ) ;
#19750=EDGE_LOOP ( 'NONE', ( #71760, #42692, #11730, #59676 ) ) ;
#19767=CYLINDRICAL_SURFACE ( 'NONE', #38724, 42.00000000000000000 ) ;
#19771=CIRCLE ( 'NONE', #61826, 37.49900000000000944 ) ;
#19782=VERTEX_POINT ( 'NONE', #61206 ) ;
#19792=ADVANCED_FACE ( 'NONE', ( #72313 ), #56524, .T. ) ;
#19814=DIRECTION ( 'NONE',  ( 1.000000000000000000, 0.000000000000000000, 0.000000000000000000 ) ) ;
#19826=DIRECTION ( 'NONE',  ( 1.000000000000000000, -0.000000000000000000, -0.000000000000000000 ) ) ;
#19840=CARTESIAN_POINT ( 'NONE',  ( 10.00000000000000000, -33.80338159004296017, 16.23288003029484727 ) ) ;
#19844=ORIENTED_EDGE ( 'NONE', *, *, #26552, .T. ) ;
#19858=FACE_OUTER_BOUND ( 'NONE', #53173, .T. ) ;
#19865=CARTESIAN_POINT ( 'NONE',  ( 10.00000000000000000, -31.52238457039580055, -27.75498641678775869 ) ) ;
#19870=ORIENTED_EDGE ( 'NONE', *, *, #67297, .T. ) ;
#19873=FACE_OUTER_BOUND ( 'NONE', #35042, .T. ) ;
#19875=ORIENTED_EDGE ( 'NONE', *, *, #41968, .T. ) ;
#19898=CARTESIAN_POINT ( 'NONE',  ( 10.00000000000000000, 25.88420570971438650, -27.13269053701069566 ) ) ;
#19910=DIRECTION ( 'NONE',  ( -1.000000000000000000, 0.000000000000000000, 0.000000000000000000 ) ) ;
#19921=CARTESIAN_POINT ( 'NONE',  ( 0.000000000000000000, 21.32104025579158701, -30.84782396557194772 ) ) ;
#19929=ADVANCED_FACE ( 'NONE', ( #890 ), #35061, .T. ) ;
#19969=ORIENTED_EDGE ( 'NONE', *, *, #40057, .F. ) ;
#19970=DIRECTION ( 'NONE',  ( 0.000000000000000000, 0.8910065241883657894, 0.4539904997395509678 ) ) ;
#19973=DIRECTION ( 'NONE',  ( -1.000000000000000000, 0.000000000000000000, 0.000000000000000000 ) ) ;
#19996=LINE ( 'NONE', #71127, #48061 ) ;
#20009=EDGE_CURVE ( 'NONE', #65417, #51113, #29397, .T. ) ;
#20021=DIRECTION ( 'NONE',  ( -1.000000000000000000, 0.000000000000000000, 0.000000000000000000 ) ) ;
#20049=AXIS2_PLACEMENT_3D ( 'NONE', #53607, #26426, #2149 ) ;
#20053=LINE ( 'NONE', #3174, #69594 ) ;
#20054=DIRECTION ( 'NONE',  ( 0.000000000000000000, 0.000000000000000000, 1.000000000000000000 ) ) ;
#20082=VERTEX_POINT ( 'NONE', #22678 ) ;
#20085=ORIENTED_EDGE ( 'NONE', *, *, #23524, .T. ) ;
#20088=ADVANCED_FACE ( 'NONE', ( #68547 ), #59475, .T. ) ;
#20093=CARTESIAN_POINT ( 'NONE',  ( 0.000000000000000000, 17.80606268964540106, 33.00180498840052934 ) ) ;
#20110=EDGE_CURVE ( 'NONE', #12130, #54409, #17271, .T. ) ;
#20123=ORIENTED_EDGE ( 'NONE', *, *, #19405, .T. ) ;
#20128=AXIS2_PLACEMENT_3D ( 'NONE', #12782, #52645, #19167 ) ;
#20129=CIRCLE ( 'NONE', #16547, 16.00000000000000000 ) ;
#20135=CARTESIAN_POINT ( 'NONE',  ( 0.000000000000000000, 9.188173127307290855, 40.98264845739752360 ) ) ;
#20171=ORIENTED_EDGE ( 'NONE', *, *, #34446, .F. ) ;
#20198=DIRECTION ( 'NONE',  ( -1.000000000000000000, -0.000000000000000000, -0.000000000000000000 ) ) ;
#20204=AXIS2_PLACEMENT_3D ( 'NONE', #20912, #60778, #42740 ) ;
#20215=ORIENTED_EDGE ( 'NONE', *, *, #72615, .T. ) ;
#20222=VERTEX_POINT ( 'NONE', #51425 ) ;
#20246=CIRCLE ( 'NONE', #20308, 37.49900000000000944 ) ;
#20259=DIRECTION ( 'NONE',  ( -1.000000000000000000, -0.000000000000000000, 0.000000000000000000 ) ) ;
#20272=CARTESIAN_POINT ( 'NONE',  ( 10.00000000000000000, 22.48208911017551515, -35.47612816024499693 ) ) ;
#20283=CIRCLE ( 'NONE', #58717, 37.49900000000000233 ) ;
#20286=DIRECTION ( 'NONE',  ( 0.000000000000000000, 0.000000000000000000, 1.000000000000000000 ) ) ;
#20293=VECTOR ( 'NONE', #73490, 1000.000000000000000 ) ;
#20305=ORIENTED_EDGE ( 'NONE', *, *, #44761, .T. ) ;
#20308=AXIS2_PLACEMENT_3D ( 'NONE', #21097, #13619, #2761 ) ;
#20318=DIRECTION ( 'NONE',  ( 0.000000000000000000, 0.000000000000000000, 1.000000000000000000 ) ) ;
#20321=AXIS2_PLACEMENT_3D ( 'NONE', #51024, #57045, #22457 ) ;
#20350=CARTESIAN_POINT ( 'NONE',  ( 0.000000000000000000, 40.98264845739749518, 9.188173127307448951 ) ) ;
#20370=DIRECTION ( 'NONE',  ( -1.000000000000000000, 0.000000000000000000, -0.000000000000000000 ) ) ;
#20394=EDGE_CURVE ( 'NONE', #60472, #64608, #17589, .T. ) ;
#20430=AXIS2_PLACEMENT_3D ( 'NONE', #25978, #48907, #54200 ) ;
#20440=VERTEX_POINT ( 'NONE', #64204 ) ;
#20448=DIRECTION ( 'NONE',  ( -1.000000000000000000, 0.000000000000000000, 0.000000000000000000 ) ) ;
#20471=DIRECTION ( 'NONE',  ( -1.000000000000000000, -0.000000000000000000, 0.000000000000000000 ) ) ;
#20472=VERTEX_POINT ( 'NONE', #41266 ) ;
#20476=FACE_OUTER_BOUND ( 'NONE', #54763, .T. ) ;
#20483=ORIENTED_EDGE ( 'NONE', *, *, #54273, .F. ) ;
#20498=CARTESIAN_POINT ( 'NONE',  ( 0.000000000000000000, 0.000000000000000000, 0.000000000000000000 ) ) ;
#20505=DIRECTION ( 'NONE',  ( 0.000000000000000000, 0.000000000000000000, 1.000000000000000000 ) ) ;
#20525=AXIS2_PLACEMENT_3D ( 'NONE', #64313, #65785, #48124 ) ;
#20529=ORIENTED_EDGE ( 'NONE', *, *, #41767, .T. ) ;
#20534=ADVANCED_FACE ( 'NONE', ( #58180 ), #6325, .T. ) ;
#20547=EDGE_CURVE ( 'NONE', #4586, #22671, #14906, .T. ) ;
#20561=EDGE_CURVE ( 'NONE', #44780, #11375, #48220, .T. ) ;
#20572=CIRCLE ( 'NONE', #21747, 16.00000000000000355 ) ;
#20582=DIRECTION ( 'NONE',  ( -1.000000000000000000, 0.000000000000000000, 0.000000000000000000 ) ) ;
#20588=ORIENTED_EDGE ( 'NONE', *, *, #68412, .F. ) ;
#20594=VERTEX_POINT ( 'NONE', #20915 ) ;
#20595=AXIS2_PLACEMENT_3D ( 'NONE', #60905, #61649, #54887 ) ;
#20602=VERTEX_POINT ( 'NONE', #26553 ) ;
#20603=ADVANCED_FACE ( 'NONE', ( #49485 ), #9638, .T. ) ;
#20628=ORIENTED_EDGE ( 'NONE', *, *, #46294, .T. ) ;
#20637=DIRECTION ( 'NONE',  ( -1.000000000000000000, 0.000000000000000000, 0.000000000000000000 ) ) ;
#20639=ORIENTED_EDGE ( 'NONE', *, *, #53546, .F. ) ;
#20649=VERTEX_POINT ( 'NONE', #65315 ) ;
#20679=DIRECTION ( 'NONE',  ( -1.000000000000000000, 0.000000000000000000, 0.000000000000000000 ) ) ;
#20684=AXIS2_PLACEMENT_3D ( 'NONE', #67516, #28391, #56240 ) ;
#20705=VERTEX_POINT ( 'NONE', #45730 ) ;
#20731=AXIS2_PLACEMENT_3D ( 'NONE', #16395, #22795, #11849 ) ;
#20736=DIRECTION ( 'NONE',  ( 0.000000000000000000, 0.000000000000000000, -1.000000000000000000 ) ) ;
#20747=FACE_OUTER_BOUND ( 'NONE', #33669, .T. ) ;
#20755=DIRECTION ( 'NONE',  ( 0.000000000000000000, 0.000000000000000000, 1.000000000000000000 ) ) ;
#20768=CARTESIAN_POINT ( 'NONE',  ( 0.000000000000000000, 0.000000000000000000, 0.000000000000000000 ) ) ;
#20799=FACE_OUTER_BOUND ( 'NONE', #28028, .T. ) ;
#20802=ORIENTED_EDGE ( 'NONE', *, *, #53580, .F. ) ;
#20833=ORIENTED_EDGE ( 'NONE', *, *, #32761, .F. ) ;
#20848=AXIS2_PLACEMENT_3D ( 'NONE', #66985, #16230, #9473 ) ;
#20852=DIRECTION ( 'NONE',  ( 0.000000000000000000, 0.3090169943749410120, 0.9510565162951557516 ) ) ;
#20856=AXIS2_PLACEMENT_3D ( 'NONE', #72851, #13233, #65492 ) ;
#20862=ADVANCED_FACE ( 'NONE', ( #47188 ), #7341, .T. ) ;
#20890=ORIENTED_EDGE ( 'NONE', *, *, #46293, .T. ) ;
#20895=VECTOR ( 'NONE', #467, 1000.000000000000000 ) ;
#20902=CARTESIAN_POINT ( 'NONE',  ( 10.00000000000000000, -16.45098606841149902, 33.79645857604508308 ) ) ;
#20912=CARTESIAN_POINT ( 'NONE',  ( 0.000000000000000000, -5.202137450156129717, -37.22597642581163768 ) ) ;
#20914=CIRCLE ( 'NONE', #65362, 37.49900000000000233 ) ;
#20915=CARTESIAN_POINT ( 'NONE',  ( 10.00000000000000000, -6.736453364083817341, 36.88895765772630142 ) ) ;
#20940=CYLINDRICAL_SURFACE ( 'NONE', #23195, 16.00000000000000000 ) ;
#20959=AXIS2_PLACEMENT_3D ( 'NONE', #4476, #19973, #27372 ) ;
#21008=DIRECTION ( 'NONE',  ( -1.000000000000000000, -0.000000000000000000, 0.000000000000000000 ) ) ;
#21023=EDGE_CURVE ( 'NONE', #58797, #30533, #36271, .T. ) ;
#21033=DIRECTION ( 'NONE',  ( 0.000000000000000000, 0.000000000000000000, 1.000000000000000000 ) ) ;
#21042=DIRECTION ( 'NONE',  ( 1.000000000000000000, -0.000000000000000000, 0.000000000000000000 ) ) ;
#21058=EDGE_LOOP ( 'NONE', ( #49823, #55739, #22135, #22123 ) ) ;
#21059=DIRECTION ( 'NONE',  ( 0.000000000000000000, 0.000000000000000000, 1.000000000000000000 ) ) ;
#21079=ORIENTED_EDGE ( 'NONE', *, *, #69762, .T. ) ;
#21095=DIRECTION ( 'NONE',  ( 0.000000000000000000, 0.000000000000000000, -1.000000000000000000 ) ) ;
#21097=CARTESIAN_POINT ( 'NONE',  ( 0.000000000000000000, 0.000000000000000000, 0.000000000000000000 ) ) ;
#21108=DIRECTION ( 'NONE',  ( -1.000000000000000000, 0.000000000000000000, 0.000000000000000000 ) ) ;
#21109=LINE ( 'NONE', #56466, #24182 ) ;
#21130=DIRECTION ( 'NONE',  ( 1.000000000000000000, 0.000000000000000000, 0.000000000000000000 ) ) ;
#21141=FACE_OUTER_BOUND ( 'NONE', #57607, .T. ) ;
#21142=EDGE_CURVE ( 'NONE', #73989, #15264, #9841, .T. ) ;
#21152=FACE_OUTER_BOUND ( 'NONE', #5581, .T. ) ;
#21180=CARTESIAN_POINT ( 'NONE',  ( 4.999999999999999112, 3.925862922256769583, -41.81611651403857621 ) ) ;
#21193=DIRECTION ( 'NONE',  ( 0.000000000000000000, -0.3090169943749549453, 0.9510565162951511997 ) ) ;
#21196=DIRECTION ( 'NONE',  ( 0.000000000000000000, 1.000000000000000000, 3.469446951953614189E-15 ) ) ;
#21197=CARTESIAN_POINT ( 'NONE',  ( 10.00000000000000000, 41.91543099594818500, 2.663952781846293139 ) ) ;
#21205=AXIS2_PLACEMENT_3D ( 'NONE', #7470, #58231, #1134 ) ;
#21227=CIRCLE ( 'NONE', #34445, 16.00000000000000000 ) ;
#21228=ADVANCED_FACE ( 'NONE', ( #13530 ), #64672, .T. ) ;
#21229=DIRECTION ( 'NONE',  ( 0.000000000000000000, 0.000000000000000000, 1.000000000000000000 ) ) ;
#21237=CARTESIAN_POINT ( 'NONE',  ( 5.000000000000000000, -22.48208911017525580, 35.47612816024516036 ) ) ;
#21241=CIRCLE ( 'NONE', #8063, 16.00000000000000000 ) ;
#21251=AXIS2_PLACEMENT_3D ( 'NONE', #15586, #55811, #60353 ) ;
#21275=AXIS2_PLACEMENT_3D ( 'NONE', #68892, #57239, #11721 ) ;
#21276=ORIENTED_EDGE ( 'NONE', *, *, #19489, .T. ) ;
#21280=DIRECTION ( 'NONE',  ( 0.000000000000000000, 0.000000000000000000, 1.000000000000000000 ) ) ;
#21281=DIRECTION ( 'NONE',  ( -1.000000000000000000, 0.000000000000000000, 0.000000000000000000 ) ) ;
#21293=CARTESIAN_POINT ( 'NONE',  ( 0.000000000000000000, 0.000000000000000000, 0.000000000000000000 ) ) ;
#21294=DIRECTION ( 'NONE',  ( 0.000000000000000000, 0.000000000000000000, 1.000000000000000000 ) ) ;
#21326=AXIS2_PLACEMENT_3D ( 'NONE', #15498, #38436, #32775 ) ;
#21342=DIRECTION ( 'NONE',  ( -1.000000000000000000, 0.000000000000000000, 0.000000000000000000 ) ) ;
#21348=AXIS2_PLACEMENT_3D ( 'NONE', #64630, #64272, #30037 ) ;
#21357=EDGE_LOOP ( 'NONE', ( #69985, #31134, #29014, #44287 ) ) ;
#21368=EDGE_LOOP ( 'NONE', ( #54998, #67816, #39334, #74040 ) ) ;
#21374=CARTESIAN_POINT ( 'NONE',  ( 5.000000000000000000, 16.65560815589464028, -38.55633173626993226 ) ) ;
#21399=VECTOR ( 'NONE', #59646, 1000.000000000000000 ) ;
#21409=ORIENTED_EDGE ( 'NONE', *, *, #58148, .F. ) ;
#21412=CARTESIAN_POINT ( 'NONE',  ( 0.000000000000000000, -37.58145647212453611, -0.6853352020794456489 ) ) ;
#21416=ORIENTED_EDGE ( 'NONE', *, *, #33009, .T. ) ;
#21437=EDGE_CURVE ( 'NONE', #16575, #60507, #72869, .T. ) ;
#21439=EDGE_LOOP ( 'NONE', ( #12753, #17200, #66925, #57313 ) ) ;
#21455=ORIENTED_EDGE ( 'NONE', *, *, #12119, .T. ) ;
#21484=DIRECTION ( 'NONE',  ( 0.000000000000000000, -0.1564344650402380854, 0.9876883405951365491 ) ) ;
#21485=CIRCLE ( 'NONE', #43150, 42.00000000000000000 ) ;
#21486=CARTESIAN_POINT ( 'NONE',  ( 0.000000000000000000, 27.13269053701132094, -25.88420570971372570 ) ) ;
#21491=AXIS2_PLACEMENT_3D ( 'NONE', #12375, #28190, #51124 ) ;
#21495=VERTEX_POINT ( 'NONE', #7712 ) ;
#21499=VERTEX_POINT ( 'NONE', #39812 ) ;
#21506=CARTESIAN_POINT ( 'NONE',  ( 0.000000000000000000, -9.188173127307592836, 40.98264845739746676 ) ) ;
#21522=VECTOR ( 'NONE', #62031, 1000.000000000000000 ) ;
#21531=DIRECTION ( 'NONE',  ( 0.000000000000000000, 0.5877852522924684742, 0.8090169943749506709 ) ) ;
#21539=AXIS2_PLACEMENT_3D ( 'NONE', #56983, #62252, #45336 ) ;
#21547=AXIS2_PLACEMENT_3D ( 'NONE', #38093, #2459, #32071 ) ;
#21561=CYLINDRICAL_SURFACE ( 'NONE', #60027, 37.49900000000000233 ) ;
#21566=ORIENTED_EDGE ( 'NONE', *, *, #34356, .T. ) ;
#21596=AXIS2_PLACEMENT_3D ( 'NONE', #47651, #42024, #66793 ) ;
#21597=ORIENTED_EDGE ( 'NONE', *, *, #46965, .T. ) ;
#21609=CARTESIAN_POINT ( 'NONE',  ( 0.000000000000000000, 35.47612816024523852, 22.48208911017513145 ) ) ;
#21615=VERTEX_POINT ( 'NONE', #64867 ) ;
#21645=CARTESIAN_POINT ( 'NONE',  ( 10.00000000000000000, 0.000000000000000000, 0.000000000000000000 ) ) ;
#21655=AXIS2_PLACEMENT_3D ( 'NONE', #11856, #58110, #48586 ) ;
#21663=VERTEX_POINT ( 'NONE', #37414 ) ;
#21669=LINE ( 'NONE', #33304, #5462 ) ;
#21688=CARTESIAN_POINT ( 'NONE',  ( 0.000000000000000000, 37.58145647212453611, 0.6853352020791767529 ) ) ;
#21697=CARTESIAN_POINT ( 'NONE',  ( 10.00000000000000000, 0.000000000000000000, 0.000000000000000000 ) ) ;
#21699=CARTESIAN_POINT ( 'NONE',  ( 10.00000000000000000, 37.01155633439059756, 6.555932627142549762 ) ) ;
#21706=CIRCLE ( 'NONE', #39716, 16.00000000000000000 ) ;
#21743=CIRCLE ( 'NONE', #26517, 42.00000000000000000 ) ;
#21747=AXIS2_PLACEMENT_3D ( 'NONE', #3392, #72155, #66534 ) ;
#21754=VERTEX_POINT ( 'NONE', #56922 ) ;
#21772=CARTESIAN_POINT ( 'NONE',  ( 0.000000000000000000, 17.67226234102874116, -33.17418723428288274 ) ) ;
#21782=DIRECTION ( 'NONE',  ( -1.000000000000000000, 0.000000000000000000, 0.000000000000000000 ) ) ;
#21783=CYLINDRICAL_SURFACE ( 'NONE', #14286, 37.49900000000000233 ) ;
#21800=ORIENTED_EDGE ( 'NONE', *, *, #66707, .F. ) ;
#21805=DIRECTION ( 'NONE',  ( 0.000000000000000000, 0.000000000000000000, -1.000000000000000000 ) ) ;
#21810=DIRECTION ( 'NONE',  ( -1.000000000000000000, -0.000000000000000000, 0.000000000000000000 ) ) ;
#21818=VERTEX_POINT ( 'NONE', #22713 ) ;
#21823=DIRECTION ( 'NONE',  ( 0.000000000000000000, -0.4539904997395541320, 0.8910065241883640130 ) ) ;
#21828=ORIENTED_EDGE ( 'NONE', *, *, #25985, .T. ) ;
#21854=CARTESIAN_POINT ( 'NONE',  ( 10.00000000000000000, -29.81001611430991360, -22.74946021919165418 ) ) ;
#21865=CIRCLE ( 'NONE', #30227, 16.00000000000000355 ) ;
#21903=ORIENTED_EDGE ( 'NONE', *, *, #13046, .T. ) ;
#21939=DIRECTION ( 'NONE',  ( -1.000000000000000000, 0.000000000000000000, 0.000000000000000000 ) ) ;
#21944=CARTESIAN_POINT ( 'NONE',  ( 10.00000000000000000, 37.58145647212453611, 16.68533520207917675 ) ) ;
#21969=ADVANCED_FACE ( 'NONE', ( #41469 ), #29428, .T. ) ;
#21975=VERTEX_POINT ( 'NONE', #34718 ) ;
#21998=CARTESIAN_POINT ( 'NONE',  ( -10.00000000000000000, 0.000000000000000000, 0.000000000000000000 ) ) ;
#22012=CARTESIAN_POINT ( 'NONE',  ( 10.00000000000000000, 12.42422080174688404, -35.38097989696498047 ) ) ;
#22020=DIRECTION ( 'NONE',  ( -1.000000000000000000, -0.000000000000000000, -0.000000000000000000 ) ) ;
#22035=AXIS2_PLACEMENT_3D ( 'NONE', #39733, #5527, #22815 ) ;
#22069=CARTESIAN_POINT ( 'NONE',  ( 0.000000000000000000, 0.000000000000000000, 0.000000000000000000 ) ) ;
#22123=ORIENTED_EDGE ( 'NONE', *, *, #42950, .F. ) ;
#22135=ORIENTED_EDGE ( 'NONE', *, *, #33894, .F. ) ;
#22147=LINE ( 'NONE', #5247, #27718 ) ;
#22164=DIRECTION ( 'NONE',  ( -1.000000000000000000, 0.000000000000000000, 0.000000000000000000 ) ) ;
#22197=ORIENTED_EDGE ( 'NONE', *, *, #15275, .T. ) ;
#22201=CARTESIAN_POINT ( 'NONE',  ( 10.00000000000000000, 37.01155633439068282, -6.555932627142014191 ) ) ;
#22205=ORIENTED_EDGE ( 'NONE', *, *, #38301, .T. ) ;
#22212=CARTESIAN_POINT ( 'NONE',  ( 0.000000000000000000, 5.202137450156907761, -37.22597642581151689 ) ) ;
#22222=CARTESIAN_POINT ( 'NONE',  ( 10.00000000000000000, 25.88420570971400991, 27.13269053701105449 ) ) ;
#22254=ORIENTED_EDGE ( 'NONE', *, *, #8517, .F. ) ;
#22257=DIRECTION ( 'NONE',  ( 0.000000000000000000, 0.000000000000000000, 1.000000000000000000 ) ) ;
#22260=CARTESIAN_POINT ( 'NONE',  ( 10.00000000000000000, 35.47612816024523141, 22.48208911017513145 ) ) ;
#22266=ORIENTED_EDGE ( 'NONE', *, *, #63237, .T. ) ;
#22270=VERTEX_POINT ( 'NONE', #39536 ) ;
#22276=ORIENTED_EDGE ( 'NONE', *, *, #60867, .F. ) ;
#22284=DIRECTION ( 'NONE',  ( -1.000000000000000000, 0.000000000000000000, -0.000000000000000000 ) ) ;
#22302=AXIS2_PLACEMENT_3D ( 'NONE', #61914, #10398, #18619 ) ;
#22323=EDGE_CURVE ( 'NONE', #26140, #37645, #21109, .T. ) ;
#22324=CIRCLE ( 'NONE', #15056, 16.00000000000000000 ) ;
#22381=ORIENTED_EDGE ( 'NONE', *, *, #32817, .T. ) ;
#22416=DIRECTION ( 'NONE',  ( 0.000000000000000000, 0.000000000000000000, 1.000000000000000000 ) ) ;
#22429=CARTESIAN_POINT ( 'NONE',  ( 10.00000000000000000, 35.92658777277525672, -10.74501242461245809 ) ) ;
#22445=ORIENTED_EDGE ( 'NONE', *, *, #32845, .T. ) ;
#22446=DIRECTION ( 'NONE',  ( -1.000000000000000000, 0.000000000000000000, 0.000000000000000000 ) ) ;
#22457=DIRECTION ( 'NONE',  ( 0.000000000000000000, -0.1564344650402172410, -0.9876883405951399908 ) ) ;
#22464=AXIS2_PLACEMENT_3D ( 'NONE', #46565, #7451, #43160 ) ;
#22476=VERTEX_POINT ( 'NONE', #463 ) ;
#22478=AXIS2_PLACEMENT_3D ( 'NONE', #17555, #40488, #1427 ) ;
#22489=ORIENTED_EDGE ( 'NONE', *, *, #2162, .F. ) ;
#22530=EDGE_CURVE ( 'NONE', #38967, #4807, #11680, .T. ) ;
#22537=LINE ( 'NONE', #62403, #37348 ) ;
#22566=CARTESIAN_POINT ( 'NONE',  ( 10.00000000000000000, -12.42422080174663712, 35.38097989696507994 ) ) ;
#22574=ORIENTED_EDGE ( 'NONE', *, *, #2438, .F. ) ;
#22575=DIRECTION ( 'NONE',  ( 0.000000000000000000, -0.5877852522924624790, -0.8090169943749552228 ) ) ;
#22578=ORIENTED_EDGE ( 'NONE', *, *, #69753, .F. ) ;
#22593=ORIENTED_EDGE ( 'NONE', *, *, #12579, .T. ) ;
#22600=ORIENTED_EDGE ( 'NONE', *, *, #2933, .T. ) ;
#22605=CARTESIAN_POINT ( 'NONE',  ( 0.000000000000000000, 10.96151621346487914, 35.95386929396260456 ) ) ;
#22606=DIRECTION ( 'NONE',  ( 1.000000000000000000, -0.000000000000000000, -0.000000000000000000 ) ) ;
#22613=CARTESIAN_POINT ( 'NONE',  ( 4.999999999999999112, -41.91543099594816368, -2.663952781846588014 ) ) ;
#22619=AXIS2_PLACEMENT_3D ( 'NONE', #70873, #19372, #7729 ) ;
#22626=CIRCLE ( 'NONE', #43019, 42.00000000000000000 ) ;
#22631=DIRECTION ( 'NONE',  ( -1.000000000000000000, 0.000000000000000000, 0.000000000000000000 ) ) ;
#22635=AXIS2_PLACEMENT_3D ( 'NONE', #19215, #13205, #31598 ) ;
#22637=ORIENTED_EDGE ( 'NONE', *, *, #19184, .F. ) ;
#22638=AXIS2_PLACEMENT_3D ( 'NONE', #51178, #468, #34631 ) ;
#22656=ADVANCED_FACE ( 'NONE', ( #65067 ), #36840, .T. ) ;
#22671=VERTEX_POINT ( 'NONE', #47396 ) ;
#22677=CIRCLE ( 'NONE', #53849, 37.49900000000000233 ) ;
#22678=CARTESIAN_POINT ( 'NONE',  ( 0.000000000000000000, 2.663952781846149254, 41.91543099594818500 ) ) ;
#22687=ADVANCED_FACE ( 'NONE', ( #66177 ), #25562, .T. ) ;
#22690=ORIENTED_EDGE ( 'NONE', *, *, #20009, .F. ) ;
#22713=CARTESIAN_POINT ( 'NONE',  ( 0.000000000000000000, 16.23288003029497162, 33.80338159004289622 ) ) ;
#22724=DIRECTION ( 'NONE',  ( -1.000000000000000000, 0.000000000000000000, 0.000000000000000000 ) ) ;
#22740=FACE_OUTER_BOUND ( 'NONE', #64570, .T. ) ;
#22770=CARTESIAN_POINT ( 'NONE',  ( 10.00000000000000000, 30.80686688397010542, 21.53537804866092387 ) ) ;
#22773=DIRECTION ( 'NONE',  ( 0.000000000000000000, 0.000000000000000000, 1.000000000000000000 ) ) ;
#22775=CARTESIAN_POINT ( 'NONE',  ( 10.00000000000000000, -29.81001611430991360, -22.74946021919165418 ) ) ;
#22779=ORIENTED_EDGE ( 'NONE', *, *, #46325, .T. ) ;
#22784=CIRCLE ( 'NONE', #25185, 16.00000000000000355 ) ;
#22795=DIRECTION ( 'NONE',  ( -1.000000000000000000, 0.000000000000000000, -0.000000000000000000 ) ) ;
#22815=DIRECTION ( 'NONE',  ( 0.000000000000000000, 0.000000000000000000, 1.000000000000000000 ) ) ;
#22825=CARTESIAN_POINT ( 'NONE',  ( 10.00000000000000000, 22.64427369931169309, 30.00120703465213623 ) ) ;
#22832=LINE ( 'NONE', #45775, #39577 ) ;
#22836=CARTESIAN_POINT ( 'NONE',  ( 0.000000000000000000, -21.40280677340345505, -36.13751322684441192 ) ) ;
#22851=AXIS2_PLACEMENT_3D ( 'NONE', #73908, #23167, #61905 ) ;
#22860=DIRECTION ( 'NONE',  ( -1.000000000000000000, -0.000000000000000000, 0.000000000000000000 ) ) ;
#22873=LINE ( 'NONE', #64200, #48831 ) ;
#22876=ORIENTED_EDGE ( 'NONE', *, *, #5219, .T. ) ;
#22883=EDGE_CURVE ( 'NONE', #48642, #22476, #5084, .T. ) ;
#22931=CYLINDRICAL_SURFACE ( 'NONE', #21205, 42.00000000000000000 ) ;
#22970=VERTEX_POINT ( 'NONE', #46941 ) ;
#22983=DIRECTION ( 'NONE',  ( -1.000000000000000000, 0.000000000000000000, 0.000000000000000000 ) ) ;
#22989=CARTESIAN_POINT ( 'NONE',  ( 0.000000000000000000, 26.79245525562714292, 32.34446384429980981 ) ) ;
#23021=CARTESIAN_POINT ( 'NONE',  ( 10.00000000000000000, -39.04073710021333454, -15.48615015657624738 ) ) ;
#23033=DIRECTION ( 'NONE',  ( 0.000000000000000000, -0.1564344650402382242, 0.9876883405951366601 ) ) ;
#23039=VERTEX_POINT ( 'NONE', #7078 ) ;
#23043=LINE ( 'NONE', #58722, #44437 ) ;
#23057=DIRECTION ( 'NONE',  ( -1.000000000000000000, -0.000000000000000000, -0.000000000000000000 ) ) ;
#23064=CIRCLE ( 'NONE', #67483, 16.00000000000000000 ) ;
#23091=DIRECTION ( 'NONE',  ( -1.000000000000000000, 0.000000000000000000, 0.000000000000000000 ) ) ;
#23102=EDGE_CURVE ( 'NONE', #57628, #28591, #29090, .T. ) ;
#23118=ADVANCED_FACE ( 'NONE', ( #69354 ), #18586, .T. ) ;
#23120=AXIS2_PLACEMENT_3D ( 'NONE', #27346, #16080, #39767 ) ;
#23141=DIRECTION ( 'NONE',  ( 0.000000000000000000, -1.000000000000000000, -1.040834085586084257E-14 ) ) ;
#23142=DIRECTION ( 'NONE',  ( 0.000000000000000000, 0.4539904997395479702, -0.8910065241883673437 ) ) ;
#23143=CARTESIAN_POINT ( 'NONE',  ( 10.00000000000000000, 0.000000000000000000, 0.000000000000000000 ) ) ;
#23167=DIRECTION ( 'NONE',  ( -1.000000000000000000, 0.000000000000000000, 0.000000000000000000 ) ) ;
#23175=CIRCLE ( 'NONE', #399, 16.00000000000000000 ) ;
#23186=DIRECTION ( 'NONE',  ( 0.000000000000000000, 0.000000000000000000, 1.000000000000000000 ) ) ;
#23195=AXIS2_PLACEMENT_3D ( 'NONE', #60809, #43895, #50247 ) ;
#23252=DIRECTION ( 'NONE',  ( 0.000000000000000000, 0.000000000000000000, 1.000000000000000000 ) ) ;
#23264=EDGE_CURVE ( 'NONE', #26052, #68973, #1564, .T. ) ;
#23276=EDGE_CURVE ( 'NONE', #48441, #10439, #1716, .T. ) ;
#23283=EDGE_CURVE ( 'NONE', #8457, #6569, #2821, .T. ) ;
#23291=CARTESIAN_POINT ( 'NONE',  ( 0.000000000000000000, 15.48615015657581750, 39.04073710021349797 ) ) ;
#23377=LINE ( 'NONE', #53419, #17832 ) ;
#23385=CARTESIAN_POINT ( 'NONE',  ( 0.000000000000000000, 41.81611651403868990, -3.925862922255709542 ) ) ;
#23389=DIRECTION ( 'NONE',  ( 0.000000000000000000, -0.8910065241883626808, -0.4539904997395570740 ) ) ;
#23394=DIRECTION ( 'NONE',  ( 0.000000000000000000, -0.5877852522924624790, -0.8090169943749550008 ) ) ;
#23403=ORIENTED_EDGE ( 'NONE', *, *, #47685, .T. ) ;
#23435=CYLINDRICAL_SURFACE ( 'NONE', #56610, 16.00000000000000000 ) ;
#23438=CARTESIAN_POINT ( 'NONE',  ( 10.00000000000000000, -10.74501242461258244, -35.92658777277521409 ) ) ;
#23441=AXIS2_PLACEMENT_3D ( 'NONE', #53669, #26195, #37869 ) ;
#23463=ORIENTED_EDGE ( 'NONE', *, *, #14846, .T. ) ;
#23466=DIRECTION ( 'NONE',  ( 0.000000000000000000, -0.8910065241883721177, 0.4539904997395382003 ) ) ;
#23467=AXIS2_PLACEMENT_3D ( 'NONE', #11470, #69728, #52815 ) ;
#23476=ORIENTED_EDGE ( 'NONE', *, *, #1060, .T. ) ;
#23505=EDGE_CURVE ( 'NONE', #38633, #9962, #58420, .T. ) ;
#23510=ORIENTED_EDGE ( 'NONE', *, *, #36711, .T. ) ;
#23524=EDGE_CURVE ( 'NONE', #16575, #36199, #13533, .T. ) ;
#23532=CIRCLE ( 'NONE', #9090, 16.00000000000000355 ) ;
#23562=CIRCLE ( 'NONE', #800, 16.00000000000000355 ) ;
#23564=ORIENTED_EDGE ( 'NONE', *, *, #7709, .F. ) ;
#23577=VERTEX_POINT ( 'NONE', #41498 ) ;
#23594=EDGE_LOOP ( 'NONE', ( #62149, #3477, #30593, #47801 ) ) ;
#23604=EDGE_CURVE ( 'NONE', #24357, #18771, #9939, .T. ) ;
#23607=LINE ( 'NONE', #52168, #24292 ) ;
#23613=ORIENTED_EDGE ( 'NONE', *, *, #3016, .F. ) ;
#23624=DIRECTION ( 'NONE',  ( -1.000000000000000000, 0.000000000000000000, -0.000000000000000000 ) ) ;
#23627=DIRECTION ( 'NONE',  ( -1.000000000000000000, -0.000000000000000000, -0.000000000000000000 ) ) ;
#23648=DIRECTION ( 'NONE',  ( 0.000000000000000000, 0.000000000000000000, 1.000000000000000000 ) ) ;
#23654=ORIENTED_EDGE ( 'NONE', *, *, #30022, .F. ) ;
#23710=AXIS2_PLACEMENT_3D ( 'NONE', #26608, #72468, #73955 ) ;
#23717=DIRECTION ( 'NONE',  ( -1.000000000000000000, 0.000000000000000000, -0.000000000000000000 ) ) ;
#23722=CARTESIAN_POINT ( 'NONE',  ( 0.000000000000000000, 40.68715046381943523, -10.41901085202036370 ) ) ;
#23727=DIRECTION ( 'NONE',  ( 0.000000000000000000, -6.982962677686267499E-15, 1.000000000000000000 ) ) ;
#23737=VERTEX_POINT ( 'NONE', #60290 ) ;
#23765=ORIENTED_EDGE ( 'NONE', *, *, #16751, .T. ) ;
#23788=ORIENTED_EDGE ( 'NONE', *, *, #33009, .F. ) ;
#23801=CIRCLE ( 'NONE', #65818, 37.49900000000000233 ) ;
#23807=FACE_OUTER_BOUND ( 'NONE', #24307, .T. ) ;
#23811=VERTEX_POINT ( 'NONE', #50829 ) ;
#23832=DIRECTION ( 'NONE',  ( 0.000000000000000000, 0.000000000000000000, 1.000000000000000000 ) ) ;
#23847=CIRCLE ( 'NONE', #27428, 16.00000000000000000 ) ;
#23852=DIRECTION ( 'NONE',  ( 1.000000000000000000, 0.000000000000000000, 0.000000000000000000 ) ) ;
#23858=DIRECTION ( 'NONE',  ( -1.000000000000000000, -0.000000000000000000, -0.000000000000000000 ) ) ;
#23864=FACE_OUTER_BOUND ( 'NONE', #52126, .T. ) ;
#23866=AXIS2_PLACEMENT_3D ( 'NONE', #59371, #18393, #36063 ) ;
#23874=DIRECTION ( 'NONE',  ( -1.000000000000000000, 0.000000000000000000, 0.000000000000000000 ) ) ;
#23885=CIRCLE ( 'NONE', #65912, 42.00000000000000000 ) ;
#23893=VERTEX_POINT ( 'NONE', #28927 ) ;
#23902=AXIS2_PLACEMENT_3D ( 'NONE', #71929, #12933, #2081 ) ;
#23926=CARTESIAN_POINT ( 'NONE',  ( 10.00000000000000000, -26.08949754953005495, -27.05870788708258701 ) ) ;
#23943=CARTESIAN_POINT ( 'NONE',  ( 10.00000000000000000, -22.74946021919110706, -29.81001611431033282 ) ) ;
#23952=AXIS2_PLACEMENT_3D ( 'NONE', #7340, #13335, #43032 ) ;
#23955=AXIS2_PLACEMENT_3D ( 'NONE', #49851, #4024, #16775 ) ;
#23956=ORIENTED_EDGE ( 'NONE', *, *, #58148, .T. ) ;
#23990=CIRCLE ( 'NONE', #55205, 15.99999999999999822 ) ;
#23999=DIRECTION ( 'NONE',  ( -1.000000000000000000, -0.000000000000000000, 0.000000000000000000 ) ) ;
#24000=VERTEX_POINT ( 'NONE', #66479 ) ;
#24001=ORIENTED_EDGE ( 'NONE', *, *, #19583, .F. ) ;
#24006=DIRECTION ( 'NONE',  ( -1.000000000000000000, -0.000000000000000000, -0.000000000000000000 ) ) ;
#24023=LINE ( 'NONE', #1494, #14027 ) ;
#24027=AXIS2_PLACEMENT_3D ( 'NONE', #61935, #27327, #304 ) ;
#24031=AXIS2_PLACEMENT_3D ( 'NONE', #61556, #4802, #5166 ) ;
#24032=CIRCLE ( 'NONE', #6015, 37.49900000000000233 ) ;
#24033=VECTOR ( 'NONE', #64402, 1000.000000000000000 ) ;
#24037=ORIENTED_EDGE ( 'NONE', *, *, #18849, .F. ) ;
#24060=VERTEX_POINT ( 'NONE', #48800 ) ;
#24074=FACE_OUTER_BOUND ( 'NONE', #3535, .T. ) ;
#24083=VERTEX_POINT ( 'NONE', #43920 ) ;
#24086=ORIENTED_EDGE ( 'NONE', *, *, #48207, .T. ) ;
#24092=CARTESIAN_POINT ( 'NONE',  ( 10.00000000000000000, 0.000000000000000000, 0.000000000000000000 ) ) ;
#24102=FACE_OUTER_BOUND ( 'NONE', #42524, .T. ) ;
#24115=ADVANCED_FACE ( 'NONE', ( #10062 ), #45410, .T. ) ;
#24120=CARTESIAN_POINT ( 'NONE',  ( 0.000000000000000000, 0.6853352020795618893, -37.58145647212453611 ) ) ;
#24123=CIRCLE ( 'NONE', #51754, 16.00000000000000000 ) ;
#24125=CYLINDRICAL_SURFACE ( 'NONE', #57137, 16.00000000000000000 ) ;
#24147=ORIENTED_EDGE ( 'NONE', *, *, #46130, .F. ) ;
#24171=DIRECTION ( 'NONE',  ( 0.000000000000000000, -6.982962677686267499E-15, 1.000000000000000000 ) ) ;
#24182=VECTOR ( 'NONE', #61724, 1000.000000000000000 ) ;
#24240=ORIENTED_EDGE ( 'NONE', *, *, #63413, .F. ) ;
#24243=DIRECTION ( 'NONE',  ( -1.000000000000000000, 0.000000000000000000, 0.000000000000000000 ) ) ;
#24244=EDGE_LOOP ( 'NONE', ( #39133, #52167, #53836, #19077 ) ) ;
#24286=DIRECTION ( 'NONE',  ( 0.000000000000000000, 0.000000000000000000, 1.000000000000000000 ) ) ;
#24287=DIRECTION ( 'NONE',  ( -1.000000000000000000, 0.000000000000000000, 0.000000000000000000 ) ) ;
#24292=VECTOR ( 'NONE', #56726, 1000.000000000000000 ) ;
#24298=CARTESIAN_POINT ( 'NONE',  ( 10.00000000000000000, -35.92658777277517856, 10.74501242461269257 ) ) ;
#24301=AXIS2_PLACEMENT_3D ( 'NONE', #52887, #1432, #28841 ) ;
#24302=AXIS2_PLACEMENT_3D ( 'NONE', #73886, #22020, #10744 ) ;
#24307=EDGE_LOOP ( 'NONE', ( #43380, #66789, #50375, #2546 ) ) ;
#24308=ORIENTED_EDGE ( 'NONE', *, *, #8517, .T. ) ;
#24311=ORIENTED_EDGE ( 'NONE', *, *, #43906, .F. ) ;
#24312=ORIENTED_EDGE ( 'NONE', *, *, #29177, .T. ) ;
#24318=CARTESIAN_POINT ( 'NONE',  ( 10.00000000000000000, 17.67226234102874116, -33.17418723428288274 ) ) ;
#24343=CYLINDRICAL_SURFACE ( 'NONE', #2970, 16.00000000000000000 ) ;
#24357=VERTEX_POINT ( 'NONE', #20135 ) ;
#24383=ORIENTED_EDGE ( 'NONE', *, *, #73019, .F. ) ;
#24388=CARTESIAN_POINT ( 'NONE',  ( 0.000000000000000000, 35.53030884539084866, 12.26510123303271982 ) ) ;
#24421=VERTEX_POINT ( 'NONE', #2892 ) ;
#24429=VERTEX_POINT ( 'NONE', #19401 ) ;
#24431=ADVANCED_FACE ( 'NONE', ( #66026 ), #60388, .T. ) ;
#24435=DIRECTION ( 'NONE',  ( 0.000000000000000000, 0.1564344650402243742, 0.9876883405951387696 ) ) ;
#24476=CARTESIAN_POINT ( 'NONE',  ( 0.000000000000000000, 0.000000000000000000, 0.000000000000000000 ) ) ;
#24504=ORIENTED_EDGE ( 'NONE', *, *, #70600, .F. ) ;
#24520=DIRECTION ( 'NONE',  ( 0.000000000000000000, 0.000000000000000000, 1.000000000000000000 ) ) ;
#24536=DIRECTION ( 'NONE',  ( 0.000000000000000000, -0.8910065241883627918, -0.4539904997395569630 ) ) ;
#24546=DIRECTION ( 'NONE',  ( -1.000000000000000000, -0.000000000000000000, -0.000000000000000000 ) ) ;
#24571=DIRECTION ( 'NONE',  ( -1.000000000000000000, -0.000000000000000000, -0.000000000000000000 ) ) ;
#24638=DIRECTION ( 'NONE',  ( -1.000000000000000000, 0.000000000000000000, 0.000000000000000000 ) ) ;
#24669=CIRCLE ( 'NONE', #43904, 16.00000000000000000 ) ;
#24683=ORIENTED_EDGE ( 'NONE', *, *, #57389, .F. ) ;
#24687=CARTESIAN_POINT ( 'NONE',  ( 0.000000000000000000, -33.79645857604525361, 16.45098606841114730 ) ) ;
#24750=DIRECTION ( 'NONE',  ( -1.000000000000000000, -0.000000000000000000, 0.000000000000000000 ) ) ;
#24757=AXIS2_PLACEMENT_3D ( 'NONE', #30634, #24638, #37421 ) ;
#24772=VERTEX_POINT ( 'NONE', #25601 ) ;
#24784=ORIENTED_EDGE ( 'NONE', *, *, #29091, .F. ) ;
#24798=DIRECTION ( 'NONE',  ( -1.000000000000000000, 0.000000000000000000, 0.000000000000000000 ) ) ;
#24828=CARTESIAN_POINT ( 'NONE',  ( 10.00000000000000000, 0.000000000000000000, 0.000000000000000000 ) ) ;
#24837=CARTESIAN_POINT ( 'NONE',  ( 10.00000000000000000, -35.47612816024539484, 22.48208911017487921 ) ) ;
#24841=EDGE_CURVE ( 'NONE', #53437, #16864, #35323, .T. ) ;
#24872=AXIS2_PLACEMENT_3D ( 'NONE', #28250, #17715, #23727 ) ;
#24876=ORIENTED_EDGE ( 'NONE', *, *, #45269, .F. ) ;
#24900=CARTESIAN_POINT ( 'NONE',  ( 10.00000000000000000, 0.000000000000000000, 0.000000000000000000 ) ) ;
#24905=EDGE_LOOP ( 'NONE', ( #497, #44323, #43483, #8680 ) ) ;
#24931=DIRECTION ( 'NONE',  ( -1.000000000000000000, -0.000000000000000000, -0.000000000000000000 ) ) ;
#24946=CARTESIAN_POINT ( 'NONE',  ( 10.00000000000000000, 0.000000000000000000, 0.000000000000000000 ) ) ;
#24952=ORIENTED_EDGE ( 'NONE', *, *, #31733, .T. ) ;
#24962=VERTEX_POINT ( 'NONE', #5663 ) ;
#24964=VERTEX_POINT ( 'NONE', #63178 ) ;
#24965=ORIENTED_EDGE ( 'NONE', *, *, #19180, .T. ) ;
#24971=CARTESIAN_POINT ( 'NONE',  ( 10.00000000000000000, -17.80606268964516659, -33.00180498840066434 ) ) ;
#24997=AXIS2_PLACEMENT_3D ( 'NONE', #14388, #42239, #14007 ) ;
#25007=DIRECTION ( 'NONE',  ( -1.000000000000000000, 0.000000000000000000, -0.000000000000000000 ) ) ;
#25034=ORIENTED_EDGE ( 'NONE', *, *, #13143, .T. ) ;
#25038=CIRCLE ( 'NONE', #26216, 37.49900000000000944 ) ;
#25043=AXIS2_PLACEMENT_3D ( 'NONE', #5354, #6094, #51186 ) ;
#25073=FACE_OUTER_BOUND ( 'NONE', #38602, .T. ) ;
#25093=VECTOR ( 'NONE', #59495, 1000.000000000000000 ) ;
#25097=AXIS2_PLACEMENT_3D ( 'NONE', #14893, #70916, #9247 ) ;
#25107=AXIS2_PLACEMENT_3D ( 'NONE', #18454, #70683, #2700 ) ;
#25116=ORIENTED_EDGE ( 'NONE', *, *, #41534, .F. ) ;
#25136=ORIENTED_EDGE ( 'NONE', *, *, #59449, .T. ) ;
#25146=VERTEX_POINT ( 'NONE', #34959 ) ;
#25170=VERTEX_POINT ( 'NONE', #48446 ) ;
#25184=ORIENTED_EDGE ( 'NONE', *, *, #13259, .F. ) ;
#25185=AXIS2_PLACEMENT_3D ( 'NONE', #37579, #8995, #3379 ) ;
#25190=EDGE_CURVE ( 'NONE', #20602, #74032, #73784, .T. ) ;
#25192=AXIS2_PLACEMENT_3D ( 'NONE', #52757, #35096, #47125 ) ;
#25199=EDGE_CURVE ( 'NONE', #69818, #13377, #59738, .T. ) ;
#25205=DIRECTION ( 'NONE',  ( -1.000000000000000000, -0.000000000000000000, -0.000000000000000000 ) ) ;
#25228=CARTESIAN_POINT ( 'NONE',  ( 4.999999999999999112, -41.81611651403864727, 3.925862922256025289 ) ) ;
#25234=CARTESIAN_POINT ( 'NONE',  ( 10.00000000000000000, 0.000000000000000000, 0.000000000000000000 ) ) ;
#25239=ORIENTED_EDGE ( 'NONE', *, *, #46423, .F. ) ;
#25245=EDGE_LOOP ( 'NONE', ( #12371, #16875, #36879, #14974 ) ) ;
#25274=ORIENTED_EDGE ( 'NONE', *, *, #62059, .F. ) ;
#25285=DIRECTION ( 'NONE',  ( -1.000000000000000000, 0.000000000000000000, 0.000000000000000000 ) ) ;
#25308=DIRECTION ( 'NONE',  ( -1.000000000000000000, -0.000000000000000000, -0.000000000000000000 ) ) ;
#25316=CARTESIAN_POINT ( 'NONE',  ( 0.000000000000000000, 0.000000000000000000, 0.000000000000000000 ) ) ;
#25321=CYLINDRICAL_SURFACE ( 'NONE', #33690, 42.00000000000000000 ) ;
#25323=VERTEX_POINT ( 'NONE', #42447 ) ;
#25339=EDGE_LOOP ( 'NONE', ( #8466, #9796, #51353, #24312 ) ) ;
#25418=CARTESIAN_POINT ( 'NONE',  ( 10.00000000000000000, 33.17418723428333749, -17.67226234102790272 ) ) ;
#25422=DIRECTION ( 'NONE',  ( -1.000000000000000000, 0.000000000000000000, -0.000000000000000000 ) ) ;
#25436=DIRECTION ( 'NONE',  ( 0.000000000000000000, 0.000000000000000000, 1.000000000000000000 ) ) ;
#25438=VERTEX_POINT ( 'NONE', #10075 ) ;
#25446=DIRECTION ( 'NONE',  ( -1.000000000000000000, 0.000000000000000000, -0.000000000000000000 ) ) ;
#25492=LINE ( 'NONE', #19840, #62346 ) ;
#25536=DIRECTION ( 'NONE',  ( 0.000000000000000000, -0.8910065241883627918, -0.4539904997395568520 ) ) ;
#25549=DIRECTION ( 'NONE',  ( 0.000000000000000000, 0.000000000000000000, 1.000000000000000000 ) ) ;
#25553=CARTESIAN_POINT ( 'NONE',  ( 4.999999999999999112, 41.81611651403861885, 3.925862922256313503 ) ) ;
#25561=CARTESIAN_POINT ( 'NONE',  ( 10.00000000000000000, -37.22597642581153821, -5.202137450156795850 ) ) ;
#25562=CYLINDRICAL_SURFACE ( 'NONE', #35060, 37.49900000000000233 ) ;
#25584=DIRECTION ( 'NONE',  ( -1.000000000000000000, -0.000000000000000000, -0.000000000000000000 ) ) ;
#25592=PRODUCT_DEFINITION_FORMATION_WITH_SPECIFIED_SOURCE ( 'ANY', '', #62027, .NOT_KNOWN. ) ;
#25601=CARTESIAN_POINT ( 'NONE',  ( 0.000000000000000000, -16.65560815589439159, 38.55633173627004595 ) ) ;
#25603=ADVANCED_FACE ( 'NONE', ( #9246 ), #60402, .T. ) ;
#25611=EDGE_LOOP ( 'NONE', ( #72421, #53523, #32363, #600 ) ) ;
#25617=CIRCLE ( 'NONE', #56870, 42.00000000000000000 ) ;
#25663=CYLINDRICAL_SURFACE ( 'NONE', #26237, 42.00000000000000000 ) ;
#25672=CARTESIAN_POINT ( 'NONE',  ( 5.000000000000000000, 32.34446384430010113, -26.79245525562679831 ) ) ;
#25673=CARTESIAN_POINT ( 'NONE',  ( 0.000000000000000000, 0.000000000000000000, 0.000000000000000000 ) ) ;
#25694=ORIENTED_EDGE ( 'NONE', *, *, #57747, .F. ) ;
#25697=EDGE_CURVE ( 'NONE', #7952, #14616, #43490, .T. ) ;
#25699=CIRCLE ( 'NONE', #42505, 42.00000000000000000 ) ;
#25712=CYLINDRICAL_SURFACE ( 'NONE', #29465, 16.00000000000000000 ) ;
#25722=VECTOR ( 'NONE', #56322, 1000.000000000000000 ) ;
#25726=CARTESIAN_POINT ( 'NONE',  ( 50.00005079999999680, 12.24744871391588852, 2.500000000000003553 ) ) ;
#25729=DIRECTION ( 'NONE',  ( -1.000000000000000000, 0.000000000000000000, -0.000000000000000000 ) ) ;
#25768=AXIS2_PLACEMENT_3D ( 'NONE', #36792, #54457, #3723 ) ;
#25785=AXIS2_PLACEMENT_3D ( 'NONE', #57993, #11380, #11737 ) ;
#25814=CARTESIAN_POINT ( 'NONE',  ( 5.000000000000000000, 22.48208911017551870, -35.47612816024499693 ) ) ;
#25837=CARTESIAN_POINT ( 'NONE',  ( 0.000000000000000000, 0.000000000000000000, 0.000000000000000000 ) ) ;
#25892=AXIS2_PLACEMENT_3D ( 'NONE', #37677, #9831, #21095 ) ;
#25915=FACE_OUTER_BOUND ( 'NONE', #23594, .T. ) ;
#25951=EDGE_CURVE ( 'NONE', #57324, #2620, #67908, .T. ) ;
#25954=ADVANCED_FACE ( 'NONE', ( #12941 ), #606, .T. ) ;
#25968=ORIENTED_EDGE ( 'NONE', *, *, #1330, .F. ) ;
#25977=VERTEX_POINT ( 'NONE', #41166 ) ;
#25978=CARTESIAN_POINT ( 'NONE',  ( 10.00000000000000000, 0.000000000000000000, 0.000000000000000000 ) ) ;
#25982=EDGE_LOOP ( 'NONE', ( #32653, #12639, #20215, #68453 ) ) ;
#25985=EDGE_CURVE ( 'NONE', #6755, #38459, #36657, .T. ) ;
#25990=CIRCLE ( 'NONE', #7960, 16.00000000000000711 ) ;
#25993=AXIS2_PLACEMENT_3D ( 'NONE', #32168, #38575, #72754 ) ;
#26004=CARTESIAN_POINT ( 'NONE',  ( 0.000000000000000000, 0.000000000000000000, 0.000000000000000000 ) ) ;
#26022=DIRECTION ( 'NONE',  ( -1.000000000000000000, -0.000000000000000000, 0.000000000000000000 ) ) ;
#26030=DIRECTION ( 'NONE',  ( 0.000000000000000000, -0.8910065241883722287, 0.4539904997395382003 ) ) ;
#26047=DIRECTION ( 'NONE',  ( 1.000000000000000000, 0.000000000000000000, 0.000000000000000000 ) ) ;
#26050=EDGE_CURVE ( 'NONE', #60033, #56046, #63092, .T. ) ;
#26052=VERTEX_POINT ( 'NONE', #36255 ) ;
#26077=CARTESIAN_POINT ( 'NONE',  ( 10.00000000000000000, 33.00180498840072829, -17.80606268964504935 ) ) ;
#26129=DIRECTION ( 'NONE',  ( 0.000000000000000000, 0.000000000000000000, 1.000000000000000000 ) ) ;
#26132=LINE ( 'NONE', #32878, #56296 ) ;
#26140=VERTEX_POINT ( 'NONE', #19695 ) ;
#26160=VECTOR ( 'NONE', #5590, 1000.000000000000000 ) ;
#26163=CIRCLE ( 'NONE', #43165, 15.99999999999999645 ) ;
#26164=DIRECTION ( 'NONE',  ( -1.000000000000000000, 0.000000000000000000, 0.000000000000000000 ) ) ;
#26170=ORIENTED_EDGE ( 'NONE', *, *, #17094, .T. ) ;
#26180=VERTEX_POINT ( 'NONE', #39229 ) ;
#26195=DIRECTION ( 'NONE',  ( -1.000000000000000000, 0.000000000000000000, -0.000000000000000000 ) ) ;
#26208=DIRECTION ( 'NONE',  ( -1.000000000000000000, 0.000000000000000000, 0.000000000000000000 ) ) ;
#26216=AXIS2_PLACEMENT_3D ( 'NONE', #50384, #54922, #4182 ) ;
#26223=CARTESIAN_POINT ( 'NONE',  ( 0.000000000000000000, 30.80686688397010542, 21.53537804866092387 ) ) ;
#26237=AXIS2_PLACEMENT_3D ( 'NONE', #13634, #2411, #54608 ) ;
#26239=ORIENTED_EDGE ( 'NONE', *, *, #3087, .T. ) ;
#26240=DIRECTION ( 'NONE',  ( 0.000000000000000000, 0.000000000000000000, 1.000000000000000000 ) ) ;
#26253=CARTESIAN_POINT ( 'NONE',  ( 10.00000000000000000, -26.79245525562738095, 32.34446384429961796 ) ) ;
#26264=VERTEX_POINT ( 'NONE', #66684 ) ;
#26269=AXIS2_PLACEMENT_3D ( 'NONE', #73673, #27818, #67307 ) ;
#26275=DIRECTION ( 'NONE',  ( -1.000000000000000000, 0.000000000000000000, 0.000000000000000000 ) ) ;
#26281=CARTESIAN_POINT ( 'NONE',  ( 10.00000000000000000, -21.32104025579091910, -30.84782396557241313 ) ) ;
#26282=CARTESIAN_POINT ( 'NONE',  ( 0.000000000000000000, 0.000000000000000000, 0.000000000000000000 ) ) ;
#26301=CIRCLE ( 'NONE', #40697, 16.00000000000000000 ) ;
#26308=VECTOR ( 'NONE', #58578, 1000.000000000000000 ) ;
#26309=DIRECTION ( 'NONE',  ( 0.000000000000000000, 0.4539904997395477482, -0.8910065241883673437 ) ) ;
#26326=ORIENTED_EDGE ( 'NONE', *, *, #72376, .F. ) ;
#26400=DIRECTION ( 'NONE',  ( 1.000000000000000000, 0.000000000000000000, 0.000000000000000000 ) ) ;
#26412=CARTESIAN_POINT ( 'NONE',  ( 10.00000000000000000, -17.67226234102849958, 33.17418723428301774 ) ) ;
#26419=ORIENTED_EDGE ( 'NONE', *, *, #44761, .F. ) ;
#26426=DIRECTION ( 'NONE',  ( -1.000000000000000000, -0.000000000000000000, 0.000000000000000000 ) ) ;
#26428=ORIENTED_EDGE ( 'NONE', *, *, #37523, .F. ) ;
#26429=CARTESIAN_POINT ( 'NONE',  ( 0.000000000000000000, -12.42422080174663712, 35.38097989696507994 ) ) ;
#26444=ORIENTED_EDGE ( 'NONE', *, *, #40892, .T. ) ;
#26479=CARTESIAN_POINT ( 'NONE',  ( -10.00000000000000000, 0.000000000000000000, 0.000000000000000000 ) ) ;
#26517=AXIS2_PLACEMENT_3D ( 'NONE', #27188, #44883, #33581 ) ;
#26519=VECTOR ( 'NONE', #58388, 1000.000000000000000 ) ;
#26528=VERTEX_POINT ( 'NONE', #48191 ) ;
#26544=DIRECTION ( 'NONE',  ( -1.000000000000000000, -0.000000000000000000, 0.000000000000000000 ) ) ;
#26548=EDGE_LOOP ( 'NONE', ( #52980, #29871, #43416, #19875 ) ) ;
#26552=EDGE_CURVE ( 'NONE', #5770, #68267, #25990, .T. ) ;
#26553=CARTESIAN_POINT ( 'NONE',  ( 10.00000000000000000, -3.925862922255855647, -41.81611651403866858 ) ) ;
#26577=DIRECTION ( 'NONE',  ( -1.000000000000000000, 0.000000000000000000, -0.000000000000000000 ) ) ;
#26601=VERTEX_POINT ( 'NONE', #52964 ) ;
#26608=CARTESIAN_POINT ( 'NONE',  ( 10.00000000000000000, -35.95386929396264009, 10.96151621346475658 ) ) ;
#26610=MECHANICAL_DESIGN_GEOMETRIC_PRESENTATION_REPRESENTATION('',(#66249),#68666);
#26615=ORIENTED_EDGE ( 'NONE', *, *, #47198, .T. ) ;
#26655=DIRECTION ( 'NONE',  ( -1.000000000000000000, 0.000000000000000000, 0.000000000000000000 ) ) ;
#26693=VERTEX_POINT ( 'NONE', #23291 ) ;
#26711=ORIENTED_EDGE ( 'NONE', *, *, #41414, .T. ) ;
#26713=ORIENTED_EDGE ( 'NONE', *, *, #71180, .T. ) ;
#26735=ADVANCED_FACE ( 'NONE', ( #46583 ), #22931, .T. ) ;
#26747=ORIENTED_EDGE ( 'NONE', *, *, #56208, .F. ) ;
#26750=DIRECTION ( 'NONE',  ( -1.000000000000000000, -0.000000000000000000, 0.000000000000000000 ) ) ;
#26757=CARTESIAN_POINT ( 'NONE',  ( 10.00000000000000000, -30.80686688396994910, -21.53537804866113703 ) ) ;
#26767=CARTESIAN_POINT ( 'NONE',  ( 10.00000000000000000, 0.000000000000000000, 0.000000000000000000 ) ) ;
#26777=CARTESIAN_POINT ( 'NONE',  ( 10.00000000000000000, 30.80686688397041451, -21.53537804866048688 ) ) ;
#26784=EDGE_CURVE ( 'NONE', #58261, #73517, #67106, .T. ) ;
#26787=EDGE_LOOP ( 'NONE', ( #61541, #44456, #48028, #60586 ) ) ;
#26795=EDGE_CURVE ( 'NONE', #69818, #14214, #18793, .T. ) ;
#26801=EDGE_LOOP ( 'NONE', ( #28645, #71297, #24147, #14256 ) ) ;
#26830=EDGE_CURVE ( 'NONE', #65939, #23811, #32880, .T. ) ;
#26901=CYLINDRICAL_SURFACE ( 'NONE', #41503, 42.00000000000000000 ) ;
#26922=ORIENTED_EDGE ( 'NONE', *, *, #53546, .T. ) ;
#26943=CARTESIAN_POINT ( 'NONE',  ( 10.00000000000000000, -27.75498641678720446, -31.52238457039628727 ) ) ;
#26946=CARTESIAN_POINT ( 'NONE',  ( 10.00000000000000000, -37.58145647212455032, 16.68533520207890319 ) ) ;
#26948=AXIS2_PLACEMENT_3D ( 'NONE', #694, #12295, #13028 ) ;
#26992=VERTEX_POINT ( 'NONE', #33962 ) ;
#26996=CARTESIAN_POINT ( 'NONE',  ( 0.000000000000000000, 37.01155633439059756, 6.555932627142549762 ) ) ;
#27017=CARTESIAN_POINT ( 'NONE',  ( 0.000000000000000000, 22.74946021919175720, -29.81001611430984255 ) ) ;
#27022=CARTESIAN_POINT ( 'NONE',  ( 10.00000000000000000, 6.736453364083557105, 36.88895765772635826 ) ) ;
#27037=AXIS2_PLACEMENT_3D ( 'NONE', #23143, #46812, #46431 ) ;
#27050=CIRCLE ( 'NONE', #57090, 37.49900000000000944 ) ;
#27069=AXIS2_PLACEMENT_3D ( 'NONE', #26777, #50076, #61004 ) ;
#27073=CARTESIAN_POINT ( 'NONE',  ( 0.000000000000000000, 0.000000000000000000, 0.000000000000000000 ) ) ;
#27085=DIRECTION ( 'NONE',  ( -1.000000000000000000, 0.000000000000000000, -0.000000000000000000 ) ) ;
#27115=CARTESIAN_POINT ( 'NONE',  ( 10.00000000000000000, -2.663952781845854378, -41.91543099594820632 ) ) ;
#27117=CIRCLE ( 'NONE', #69162, 15.99999999999999645 ) ;
#27118=EDGE_LOOP ( 'NONE', ( #51133, #31465, #13299, #73770 ) ) ;
#27125=DIRECTION ( 'NONE',  ( -1.000000000000000000, -0.000000000000000000, -0.000000000000000000 ) ) ;
#27137=CARTESIAN_POINT ( 'NONE',  ( 0.000000000000000000, -10.41901085202107247, 40.68715046381925049 ) ) ;
#27151=CARTESIAN_POINT ( 'NONE',  ( 10.00000000000000000, -33.80338159004296017, 16.23288003029484727 ) ) ;
#27152=ORIENTED_EDGE ( 'NONE', *, *, #66151, .F. ) ;
#27157=EDGE_CURVE ( 'NONE', #59771, #12130, #33231, .T. ) ;
#27175=AXIS2_PLACEMENT_3D ( 'NONE', #8588, #43187, #31502 ) ;
#27188=CARTESIAN_POINT ( 'NONE',  ( 0.000000000000000000, 0.000000000000000000, 0.000000000000000000 ) ) ;
#27192=LINE ( 'NONE', #62175, #53497 ) ;
#27196=ORIENTED_EDGE ( 'NONE', *, *, #7709, .T. ) ;
#27205=DIRECTION ( 'NONE',  ( 0.000000000000000000, 0.000000000000000000, 1.000000000000000000 ) ) ;
#27213=EDGE_CURVE ( 'NONE', #16746, #51113, #867, .T. ) ;
#27231=AXIS2_PLACEMENT_3D ( 'NONE', #42347, #48344, #13393 ) ;
#27247=ORIENTED_EDGE ( 'NONE', *, *, #45196, .F. ) ;
#27255=AXIS2_PLACEMENT_3D ( 'NONE', #65422, #44714, #55975 ) ;
#27259=ORIENTED_EDGE ( 'NONE', *, *, #59238, .F. ) ;
#27262=EDGE_LOOP ( 'NONE', ( #21409, #34678, #71917, #9674 ) ) ;
#27294=FACE_OUTER_BOUND ( 'NONE', #26801, .T. ) ;
#27307=DIRECTION ( 'NONE',  ( -1.000000000000000000, 0.000000000000000000, 0.000000000000000000 ) ) ;
#27308=DIRECTION ( 'NONE',  ( 0.000000000000000000, 1.000000000000000000, -9.787530781167596740E-16 ) ) ;
#27317=AXIS2_PLACEMENT_3D ( 'NONE', #38610, #66085, #2945 ) ;
#27325=AXIS2_PLACEMENT_3D ( 'NONE', #16984, #27508, #11329 ) ;
#27327=DIRECTION ( 'NONE',  ( -1.000000000000000000, 0.000000000000000000, 0.000000000000000000 ) ) ;
#27332=DIRECTION ( 'NONE',  ( -1.000000000000000000, -0.000000000000000000, -0.000000000000000000 ) ) ;
#27333=EDGE_CURVE ( 'NONE', #48627, #2059, #33276, .T. ) ;
#27336=VECTOR ( 'NONE', #14502, 1000.000000000000000 ) ;
#27346=CARTESIAN_POINT ( 'NONE',  ( 10.00000000000000000, 0.000000000000000000, 0.000000000000000000 ) ) ;
#27352=ORIENTED_EDGE ( 'NONE', *, *, #15714, .F. ) ;
#27354=CARTESIAN_POINT ( 'NONE',  ( 0.000000000000000000, 6.736453364083555329, 36.88895765772635116 ) ) ;
#27372=DIRECTION ( 'NONE',  ( 0.000000000000000000, 0.4539904997395412534, 0.8910065241883706744 ) ) ;
#27378=CIRCLE ( 'NONE', #14179, 42.00000000000000000 ) ;
#27391=EDGE_CURVE ( 'NONE', #18937, #11372, #65718, .T. ) ;
#27398=CIRCLE ( 'NONE', #33404, 16.00000000000000000 ) ;
#27419=CIRCLE ( 'NONE', #12986, 16.00000000000000000 ) ;
#27428=AXIS2_PLACEMENT_3D ( 'NONE', #10959, #51916, #63955 ) ;
#27431=VERTEX_POINT ( 'NONE', #34243 ) ;
#27441=EDGE_LOOP ( 'NONE', ( #65547, #9064, #51471, #19870 ) ) ;
#27466=EDGE_CURVE ( 'NONE', #4529, #30100, #11669, .T. ) ;
#27479=CARTESIAN_POINT ( 'NONE',  ( 0.000000000000000000, 0.000000000000000000, 0.000000000000000000 ) ) ;
#27485=DIRECTION ( 'NONE',  ( -1.000000000000000000, 0.000000000000000000, 0.000000000000000000 ) ) ;
#27492=CARTESIAN_POINT ( 'NONE',  ( -10.00000000000000000, 0.000000000000000000, 0.000000000000000000 ) ) ;
#27494=DIRECTION ( 'NONE',  ( -1.000000000000000000, 0.000000000000000000, -0.000000000000000000 ) ) ;
#27497=CARTESIAN_POINT ( 'NONE',  ( 0.000000000000000000, 0.000000000000000000, 0.000000000000000000 ) ) ;
#27506=CIRCLE ( 'NONE', #56346, 16.00000000000000000 ) ;
#27507=DIRECTION ( 'NONE',  ( 0.000000000000000000, 0.000000000000000000, 1.000000000000000000 ) ) ;
#27508=DIRECTION ( 'NONE',  ( -1.000000000000000000, 0.000000000000000000, 0.000000000000000000 ) ) ;
#27514=ADVANCED_FACE ( 'NONE', ( #16962 ), #39899, .T. ) ;
#27520=ORIENTED_EDGE ( 'NONE', *, *, #52982, .T. ) ;
#27543=DIRECTION ( 'NONE',  ( -1.000000000000000000, 0.000000000000000000, 0.000000000000000000 ) ) ;
#27564=ADVANCED_FACE ( 'NONE', ( #71034 ), #13156, .T. ) ;
#27591=DIRECTION ( 'NONE',  ( -1.000000000000000000, 0.000000000000000000, 0.000000000000000000 ) ) ;
#27594=CARTESIAN_POINT ( 'NONE',  ( 10.00000000000000000, 30.84782396557248418, -21.32104025579081252 ) ) ;
#27595=CARTESIAN_POINT ( 'NONE',  ( 0.000000000000000000, -35.92658777277502935, -10.74501242461320594 ) ) ;
#27597=AXIS2_PLACEMENT_3D ( 'NONE', #5512, #21008, #22416 ) ;
#27622=AXIS2_PLACEMENT_3D ( 'NONE', #62058, #10922, #56793 ) ;
#27636=LINE ( 'NONE', #50562, #20293 ) ;
#27649=AXIS2_PLACEMENT_3D ( 'NONE', #30278, #71978, #20852 ) ;
#27650=ADVANCED_FACE ( 'NONE', ( #64309 ), #54136, .T. ) ;
#27652=DIRECTION ( 'NONE',  ( 1.000000000000000000, -0.000000000000000000, 0.000000000000000000 ) ) ;
#27656=CYLINDRICAL_SURFACE ( 'NONE', #21539, 16.00000000000000000 ) ;
#27661=FACE_OUTER_BOUND ( 'NONE', #66232, .T. ) ;
#27683=EDGE_CURVE ( 'NONE', #23039, #11760, #60983, .T. ) ;
#27685=DIRECTION ( 'NONE',  ( -1.000000000000000000, -0.000000000000000000, 0.000000000000000000 ) ) ;
#27694=DIRECTION ( 'NONE',  ( 1.000000000000000000, 0.000000000000000000, 0.000000000000000000 ) ) ;
#27718=VECTOR ( 'NONE', #11968, 1000.000000000000000 ) ;
#27723=ORIENTED_EDGE ( 'NONE', *, *, #47020, .F. ) ;
#27732=ADVANCED_FACE ( 'NONE', ( #15755 ), #38318, .T. ) ;
#27777=CARTESIAN_POINT ( 'NONE',  ( 10.00000000000000000, -30.00120703465189465, -22.64427369931201639 ) ) ;
#27788=CARTESIAN_POINT ( 'NONE',  ( 10.00000000000000000, 0.000000000000000000, 0.000000000000000000 ) ) ;
#27794=CARTESIAN_POINT ( 'NONE',  ( 10.00000000000000000, 10.96151621346487914, 35.95386929396260456 ) ) ;
#27818=DIRECTION ( 'NONE',  ( -1.000000000000000000, -0.000000000000000000, -0.000000000000000000 ) ) ;
#27836=ORIENTED_EDGE ( 'NONE', *, *, #63592, .F. ) ;
#27841=DIRECTION ( 'NONE',  ( -1.000000000000000000, 0.000000000000000000, 0.000000000000000000 ) ) ;
#27842=ORIENTED_EDGE ( 'NONE', *, *, #23264, .F. ) ;
#27854=EDGE_LOOP ( 'NONE', ( #33190, #53325, #66391, #1473 ) ) ;
#27869=CARTESIAN_POINT ( 'NONE',  ( 4.999999999999999112, -38.55633173627022359, 16.65560815589396526 ) ) ;
#27874=CIRCLE ( 'NONE', #3900, 16.00000000000000355 ) ;
#27886=ORIENTED_EDGE ( 'NONE', *, *, #23505, .T. ) ;
#27896=LINE ( 'NONE', #72631, #13239 ) ;
#27909=VECTOR ( 'NONE', #48254, 1000.000000000000000 ) ;
#27915=ADVANCED_FACE ( 'NONE', ( #62384 ), #68391, .T. ) ;
#27922=EDGE_CURVE ( 'NONE', #61856, #37995, #45460, .T. ) ;
#27924=ORIENTED_EDGE ( 'NONE', *, *, #41085, .F. ) ;
#27973=CIRCLE ( 'NONE', #38767, 16.00000000000000000 ) ;
#28028=EDGE_LOOP ( 'NONE', ( #44104, #44319, #62126, #57078 ) ) ;
#28029=ADVANCED_FACE ( 'NONE', ( #30627 ), #3576, .F. ) ;
#28040=AXIS2_PLACEMENT_3D ( 'NONE', #32209, #20582, #48772 ) ;
#28043=ORIENTED_EDGE ( 'NONE', *, *, #65389, .T. ) ;
#28057=DIRECTION ( 'NONE',  ( 0.000000000000000000, 0.000000000000000000, 1.000000000000000000 ) ) ;
#28070=ADVANCED_FACE ( 'NONE', ( #47932 ), #70854, .F. ) ;
#28125=ORIENTED_EDGE ( 'NONE', *, *, #66151, .T. ) ;
#28139=VECTOR ( 'NONE', #46669, 1000.000000000000000 ) ;
#28147=CARTESIAN_POINT ( 'NONE',  ( 5.000000000000000000, 31.52238457039599595, 27.75498641678753842 ) ) ;
#28150=CARTESIAN_POINT ( 'NONE',  ( 0.000000000000000000, 0.000000000000000000, 0.000000000000000000 ) ) ;
#28155=DIRECTION ( 'NONE',  ( -1.000000000000000000, -0.000000000000000000, 0.000000000000000000 ) ) ;
#28157=AXIS2_PLACEMENT_3D ( 'NONE', #17280, #50742, #51119 ) ;
#28165=DIRECTION ( 'NONE',  ( 0.000000000000000000, 0.000000000000000000, 1.000000000000000000 ) ) ;
#28169=EDGE_CURVE ( 'NONE', #45064, #46185, #27378, .T. ) ;
#28172=DIRECTION ( 'NONE',  ( -1.000000000000000000, -0.000000000000000000, -0.000000000000000000 ) ) ;
#28180=ORIENTED_EDGE ( 'NONE', *, *, #3277, .F. ) ;
#28190=DIRECTION ( 'NONE',  ( -1.000000000000000000, 0.000000000000000000, 0.000000000000000000 ) ) ;
#28191=ORIENTED_EDGE ( 'NONE', *, *, #66308, .T. ) ;
#28192=EDGE_CURVE ( 'NONE', #1535, #47891, #23801, .T. ) ;
#28206=ORIENTED_EDGE ( 'NONE', *, *, #60393, .T. ) ;
#28228=LINE ( 'NONE', #12054, #72252 ) ;
#28250=CARTESIAN_POINT ( 'NONE',  ( 10.00000000000000000, 0.000000000000000000, 0.000000000000000000 ) ) ;
#28251=ORIENTED_EDGE ( 'NONE', *, *, #70165, .F. ) ;
#28253=CIRCLE ( 'NONE', #4140, 16.00000000000000000 ) ;
#28261=ADVANCED_FACE ( 'NONE', ( #23807 ), #40358, .T. ) ;
#28268=ORIENTED_EDGE ( 'NONE', *, *, #19489, .F. ) ;
#28342=EDGE_CURVE ( 'NONE', #62549, #37645, #41827, .T. ) ;
#28343=CIRCLE ( 'NONE', #7949, 42.00000000000000000 ) ;
#28350=CARTESIAN_POINT ( 'NONE',  ( 10.00000000000000000, -36.88895765772628010, -6.736453364083947015 ) ) ;
#28383=DIRECTION ( 'NONE',  ( 0.000000000000000000, 0.1564344650402313408, -0.9876883405951376593 ) ) ;
#28391=DIRECTION ( 'NONE',  ( -1.000000000000000000, 0.000000000000000000, 0.000000000000000000 ) ) ;
#28435=CARTESIAN_POINT ( 'NONE',  ( 10.00000000000000000, 0.000000000000000000, 0.000000000000000000 ) ) ;
#28450=AXIS2_PLACEMENT_3D ( 'NONE', #5, #23999, #51443 ) ;
#28484=ORIENTED_EDGE ( 'NONE', *, *, #73943, .T. ) ;
#28503=CARTESIAN_POINT ( 'NONE',  ( 0.000000000000000000, 0.000000000000000000, 0.000000000000000000 ) ) ;
#28507=AXIS2_PLACEMENT_3D ( 'NONE', #28570, #51516, #40240 ) ;
#28514=AXIS2_PLACEMENT_3D ( 'NONE', #11064, #22724, #4699 ) ;
#28517=CARTESIAN_POINT ( 'NONE',  ( 10.00000000000000000, -16.65560815589383381, -38.55633173627028754 ) ) ;
#28533=EDGE_CURVE ( 'NONE', #48094, #37368, #2257, .T. ) ;
#28542=ORIENTED_EDGE ( 'NONE', *, *, #32133, .T. ) ;
#28555=AXIS2_PLACEMENT_3D ( 'NONE', #26282, #72868, #43240 ) ;
#28570=CARTESIAN_POINT ( 'NONE',  ( 10.00000000000000000, 6.555932627142418312, 37.01155633439060466 ) ) ;
#28582=AXIS2_PLACEMENT_3D ( 'NONE', #1668, #65162, #35820 ) ;
#28591=VERTEX_POINT ( 'NONE', #27115 ) ;
#28601=CARTESIAN_POINT ( 'NONE',  ( 0.000000000000000000, -6.736453364083290651, -36.88895765772640090 ) ) ;
#28638=CARTESIAN_POINT ( 'NONE',  ( -10.00000000000000000, 0.000000000000000000, 0.000000000000000000 ) ) ;
#28645=ORIENTED_EDGE ( 'NONE', *, *, #4631, .T. ) ;
#28652=ORIENTED_EDGE ( 'NONE', *, *, #23102, .F. ) ;
#28653=CARTESIAN_POINT ( 'NONE',  ( 0.000000000000000000, 0.000000000000000000, 0.000000000000000000 ) ) ;
#28659=EDGE_CURVE ( 'NONE', #57179, #24964, #22677, .T. ) ;
#28674=DIRECTION ( 'NONE',  ( -1.000000000000000000, 0.000000000000000000, 0.000000000000000000 ) ) ;
#28682=LINE ( 'NONE', #5777, #70986 ) ;
#28685=VECTOR ( 'NONE', #1015, 1000.000000000000000 ) ;
#28691=CARTESIAN_POINT ( 'NONE',  ( 5.000000000000000000, -31.52238457039579345, -27.75498641678775158 ) ) ;
#28692=ORIENTED_EDGE ( 'NONE', *, *, #56112, .T. ) ;
#28700=DIRECTION ( 'NONE',  ( 0.000000000000000000, 0.000000000000000000, 1.000000000000000000 ) ) ;
#28711=EDGE_CURVE ( 'NONE', #26180, #55579, #23847, .T. ) ;
#28722=LINE ( 'NONE', #5077, #69849 ) ;
#28739=AXIS2_PLACEMENT_3D ( 'NONE', #2825, #14434, #1719 ) ;
#28745=VECTOR ( 'NONE', #64702, 1000.000000000000000 ) ;
#28760=ADVANCED_FACE ( 'NONE', ( #45927 ), #39913, .T. ) ;
#28762=CARTESIAN_POINT ( 'NONE',  ( 0.000000000000000000, 37.58145647212453611, 0.6853352020791767529 ) ) ;
#28766=ADVANCED_FACE ( 'NONE', ( #39535, #62862 ), #51170, .F. ) ;
#28775=AXIS2_PLACEMENT_3D ( 'NONE', #53611, #19397, #2155 ) ;
#28792=ADVANCED_FACE ( 'NONE', ( #24102 ), #17338, .T. ) ;
#28803=EDGE_CURVE ( 'NONE', #66673, #38385, #74101, .T. ) ;
#28813=CIRCLE ( 'NONE', #32389, 16.00000000000000355 ) ;
#28831=DIRECTION ( 'NONE',  ( 0.000000000000000000, 0.9510565162951544194, -0.3090169943749447867 ) ) ;
#28833=ADVANCED_FACE ( 'NONE', ( #2680 ), #14279, .T. ) ;
#28841=DIRECTION ( 'NONE',  ( 0.000000000000000000, 0.000000000000000000, -1.000000000000000000 ) ) ;
#28844=EDGE_CURVE ( 'NONE', #62061, #69818, #47884, .T. ) ;
#28849=ORIENTED_EDGE ( 'NONE', *, *, #41492, .F. ) ;
#28856=CIRCLE ( 'NONE', #15666, 16.00000000000000000 ) ;
#28870=LINE ( 'NONE', #51421, #26160 ) ;
#28900=DIRECTION ( 'NONE',  ( -1.000000000000000000, 0.000000000000000000, 0.000000000000000000 ) ) ;
#28927=CARTESIAN_POINT ( 'NONE',  ( 10.00000000000000000, 21.32104025579158701, -30.84782396557194772 ) ) ;
#28937=CIRCLE ( 'NONE', #70947, 37.49900000000000233 ) ;
#28972=DIRECTION ( 'NONE',  ( 0.000000000000000000, 0.000000000000000000, 1.000000000000000000 ) ) ;
#28987=VECTOR ( 'NONE', #73634, 1000.000000000000000 ) ;
#28996=ORIENTED_EDGE ( 'NONE', *, *, #388, .T. ) ;
#28998=DIRECTION ( 'NONE',  ( 0.000000000000000000, -0.8910065241883626808, -0.4539904997395570740 ) ) ;
#29014=ORIENTED_EDGE ( 'NONE', *, *, #34709, .T. ) ;
#29018=ORIENTED_EDGE ( 'NONE', *, *, #48396, .F. ) ;
#29021=LINE ( 'NONE', #21237, #10500 ) ;
#29057=CARTESIAN_POINT ( 'NONE',  ( 10.00000000000000000, -36.13751322684434797, 21.40280677340358295 ) ) ;
#29062=CARTESIAN_POINT ( 'NONE',  ( 10.00000000000000000, 37.16516213103277977, 4.992566952385115719 ) ) ;
#29065=CARTESIAN_POINT ( 'NONE',  ( 10.00000000000000000, -35.38097989696520074, 12.42422080174625520 ) ) ;
#29090=CIRCLE ( 'NONE', #48314, 16.00000000000000000 ) ;
#29091=EDGE_CURVE ( 'NONE', #66590, #23737, #11868, .T. ) ;
#29109=ORIENTED_EDGE ( 'NONE', *, *, #56901, .F. ) ;
#29114=EDGE_CURVE ( 'NONE', #26992, #46185, #62777, .T. ) ;
#29119=EDGE_LOOP ( 'NONE', ( #49093, #20085, #46831, #15841 ) ) ;
#29168=DIRECTION ( 'NONE',  ( 0.000000000000000000, -0.1564344650402170744, -0.9876883405951398798 ) ) ;
#29177=EDGE_CURVE ( 'NONE', #64823, #72774, #73638, .T. ) ;
#29191=DIRECTION ( 'NONE',  ( -1.000000000000000000, -0.000000000000000000, 0.000000000000000000 ) ) ;
#29197=FACE_OUTER_BOUND ( 'NONE', #21439, .T. ) ;
#29199=ORIENTED_EDGE ( 'NONE', *, *, #10421, .T. ) ;
#29208=EDGE_CURVE ( 'NONE', #45217, #48031, #59923, .T. ) ;
#29211=DIRECTION ( 'NONE',  ( -1.000000000000000000, 0.000000000000000000, 0.000000000000000000 ) ) ;
#29234=CARTESIAN_POINT ( 'NONE',  ( 10.00000000000000000, -37.22597642581161637, 5.202137450156258502 ) ) ;
#29237=EDGE_LOOP ( 'NONE', ( #15850, #73294, #51671, #64294 ) ) ;
#29241=FACE_OUTER_BOUND ( 'NONE', #45657, .T. ) ;
#29275=CARTESIAN_POINT ( 'NONE',  ( 10.00000000000000000, 0.000000000000000000, 0.000000000000000000 ) ) ;
#29280=ORIENTED_EDGE ( 'NONE', *, *, #27157, .F. ) ;
#29281=ORIENTED_EDGE ( 'NONE', *, *, #33201, .T. ) ;
#29296=ORIENTED_EDGE ( 'NONE', *, *, #62755, .F. ) ;
#29336=CARTESIAN_POINT ( 'NONE',  ( 0.000000000000000000, 0.000000000000000000, 0.000000000000000000 ) ) ;
#29348=EDGE_CURVE ( 'NONE', #10428, #42999, #52565, .T. ) ;
#29366=VECTOR ( 'NONE', #44065, 1000.000000000000000 ) ;
#29371=EDGE_CURVE ( 'NONE', #4351, #26140, #64580, .T. ) ;
#29379=ORIENTED_EDGE ( 'NONE', *, *, #45932, .T. ) ;
#29380=DIRECTION ( 'NONE',  ( 0.000000000000000000, 0.000000000000000000, 1.000000000000000000 ) ) ;
#29397=LINE ( 'NONE', #68908, #58115 ) ;
#29415=DIRECTION ( 'NONE',  ( -1.000000000000000000, -0.000000000000000000, 0.000000000000000000 ) ) ;
#29428=CYLINDRICAL_SURFACE ( 'NONE', #61419, 16.00000000000000355 ) ;
#29436=LINE ( 'NONE', #46756, #2177 ) ;
#29447=DIRECTION ( 'NONE',  ( 0.000000000000000000, 0.000000000000000000, 1.000000000000000000 ) ) ;
#29465=AXIS2_PLACEMENT_3D ( 'NONE', #37382, #20448, #31346 ) ;
#29470=CARTESIAN_POINT ( 'NONE',  ( 10.00000000000000000, 37.22597642581150268, 5.202137450157037435 ) ) ;
#29482=ORIENTED_EDGE ( 'NONE', *, *, #653, .T. ) ;
#29497=EDGE_LOOP ( 'NONE', ( #71383, #73871, #38978, #11462 ) ) ;
#29521=EDGE_CURVE ( 'NONE', #32536, #71453, #16597, .T. ) ;
#29534=AXIS2_PLACEMENT_3D ( 'NONE', #38877, #57281, #67819 ) ;
#29547=EDGE_CURVE ( 'NONE', #22970, #72913, #66984, .T. ) ;
#29566=EDGE_LOOP ( 'NONE', ( #58266, #70599, #73491, #44112, #24876, #39220 ) ) ;
#29583=DIRECTION ( 'NONE',  ( -1.000000000000000000, -0.000000000000000000, -0.000000000000000000 ) ) ;
#29596=EDGE_CURVE ( 'NONE', #49911, #16321, #34568, .T. ) ;
#29610=DIRECTION ( 'NONE',  ( 0.000000000000000000, 0.000000000000000000, 1.000000000000000000 ) ) ;
#29637=CARTESIAN_POINT ( 'NONE',  ( 0.000000000000000000, -10.96151621346461447, -35.95386929396268272 ) ) ;
#29647=DIRECTION ( 'NONE',  ( 0.000000000000000000, 0.8090169943749486725, -0.5877852522924713607 ) ) ;
#29674=CARTESIAN_POINT ( 'NONE',  ( 0.000000000000000000, -22.74946021919110706, -29.81001611431033282 ) ) ;
#29704=CIRCLE ( 'NONE', #36909, 37.49900000000000944 ) ;
#29723=DIRECTION ( 'NONE',  ( -1.000000000000000000, -0.000000000000000000, -0.000000000000000000 ) ) ;
#29726=CIRCLE ( 'NONE', #27317, 16.00000000000000000 ) ;
#29728=AXIS2_PLACEMENT_3D ( 'NONE', #49583, #3754, #44332 ) ;
#29742=AXIS2_PLACEMENT_3D ( 'NONE', #24318, #47249, #70156 ) ;
#29766=DIRECTION ( 'NONE',  ( -1.000000000000000000, -0.000000000000000000, -0.000000000000000000 ) ) ;
#29769=EDGE_CURVE ( 'NONE', #20594, #54282, #6982, .T. ) ;
#29772=DIRECTION ( 'NONE',  ( -1.000000000000000000, -0.000000000000000000, 0.000000000000000000 ) ) ;
#29775=ORIENTED_EDGE ( 'NONE', *, *, #33809, .F. ) ;
#29799=EDGE_CURVE ( 'NONE', #51292, #72197, #49059, .T. ) ;
#29801=DIRECTION ( 'NONE',  ( -1.000000000000000000, -0.000000000000000000, -0.000000000000000000 ) ) ;
#29803=CYLINDRICAL_SURFACE ( 'NONE', #73301, 42.00000000000000000 ) ;
#29809=CARTESIAN_POINT ( 'NONE',  ( 10.00000000000000000, -2.663952781846440576, 41.91543099594817789 ) ) ;
#29831=VECTOR ( 'NONE', #21939, 1000.000000000000000 ) ;
#29837=AXIS2_PLACEMENT_3D ( 'NONE', #62097, #72247, #16220 ) ;
#29856=CARTESIAN_POINT ( 'NONE',  ( 10.00000000000000000, 6.555932627142418312, 37.01155633439060466 ) ) ;
#29865=CIRCLE ( 'NONE', #45513, 37.49900000000000944 ) ;
#29871=ORIENTED_EDGE ( 'NONE', *, *, #44492, .F. ) ;
#29886=VERTEX_POINT ( 'NONE', #73363 ) ;
#29900=LINE ( 'NONE', #47946, #43007 ) ;
#29919=AXIS2_PLACEMENT_3D ( 'NONE', #12741, #58247, #46973 ) ;
#29944=ORIENTED_EDGE ( 'NONE', *, *, #67200, .F. ) ;
#29950=CARTESIAN_POINT ( 'NONE',  ( 10.00000000000000000, -12.42422080174663712, 35.38097989696507994 ) ) ;
#29969=DIRECTION ( 'NONE',  ( -1.000000000000000000, 0.000000000000000000, 0.000000000000000000 ) ) ;
#29977=ORIENTED_EDGE ( 'NONE', *, *, #26784, .F. ) ;
#29983=FACE_OUTER_BOUND ( 'NONE', #73898, .T. ) ;
#29991=FACE_OUTER_BOUND ( 'NONE', #71901, .T. ) ;
#30013=EDGE_CURVE ( 'NONE', #30109, #40304, #48688, .T. ) ;
#30021=VECTOR ( 'NONE', #56421, 1000.000000000000000 ) ;
#30022=EDGE_CURVE ( 'NONE', #14616, #11957, #14217, .T. ) ;
#30024=AXIS2_PLACEMENT_3D ( 'NONE', #51197, #40673, #486 ) ;
#30027=DIRECTION ( 'NONE',  ( -1.000000000000000000, 0.000000000000000000, -0.000000000000000000 ) ) ;
#30032=ORIENTED_EDGE ( 'NONE', *, *, #33286, .F. ) ;
#30037=DIRECTION ( 'NONE',  ( 0.000000000000000000, 0.000000000000000000, 1.000000000000000000 ) ) ;
#30055=CYLINDRICAL_SURFACE ( 'NONE', #52488, 16.00000000000000000 ) ;
#30079=CIRCLE ( 'NONE', #22851, 16.00000000000000000 ) ;
#30083=DIRECTION ( 'NONE',  ( -1.000000000000000000, 0.000000000000000000, 0.000000000000000000 ) ) ;
#30086=CIRCLE ( 'NONE', #64931, 37.49900000000000944 ) ;
#30094=CARTESIAN_POINT ( 'NONE',  ( -10.00000000000000000, 0.000000000000000000, 0.000000000000000000 ) ) ;
#30100=VERTEX_POINT ( 'NONE', #57206 ) ;
#30109=VERTEX_POINT ( 'NONE', #63600 ) ;
#30113=VERTEX_POINT ( 'NONE', #5713 ) ;
#30120=CIRCLE ( 'NONE', #50530, 16.00000000000000000 ) ;
#30122=DIRECTION ( 'NONE',  ( 1.000000000000000000, -0.000000000000000000, 0.000000000000000000 ) ) ;
#30151=DIRECTION ( 'NONE',  ( 0.000000000000000000, -0.9876883405951393247, 0.1564344650402204329 ) ) ;
#30158=ORIENTED_EDGE ( 'NONE', *, *, #48396, .T. ) ;
#30159=CARTESIAN_POINT ( 'NONE',  ( 0.000000000000000000, -38.55633173626998911, -16.65560815589452304 ) ) ;
#30161=DIRECTION ( 'NONE',  ( 0.000000000000000000, 0.000000000000000000, 1.000000000000000000 ) ) ;
#30173=VERTEX_POINT ( 'NONE', #18091 ) ;
#30185=AXIS2_PLACEMENT_3D ( 'NONE', #53566, #70846, #65231 ) ;
#30214=DIRECTION ( 'NONE',  ( -1.000000000000000000, -0.000000000000000000, -0.000000000000000000 ) ) ;
#30227=AXIS2_PLACEMENT_3D ( 'NONE', #58441, #30241, #12582 ) ;
#30241=DIRECTION ( 'NONE',  ( -1.000000000000000000, 0.000000000000000000, -0.000000000000000000 ) ) ;
#30242=CIRCLE ( 'NONE', #60272, 42.00000000000000000 ) ;
#30266=DIRECTION ( 'NONE',  ( -1.000000000000000000, -0.000000000000000000, -0.000000000000000000 ) ) ;
#30278=CARTESIAN_POINT ( 'NONE',  ( 10.00000000000000000, -37.22597642581153821, -5.202137450156795850 ) ) ;
#30303=ORIENTED_EDGE ( 'NONE', *, *, #2942, .F. ) ;
#30332=ORIENTED_EDGE ( 'NONE', *, *, #53392, .F. ) ;
#30374=DIRECTION ( 'NONE',  ( -1.000000000000000000, 0.000000000000000000, -0.000000000000000000 ) ) ;
#30412=ORIENTED_EDGE ( 'NONE', *, *, #24841, .T. ) ;
#30441=ADVANCED_FACE ( 'NONE', ( #38337 ), #21783, .T. ) ;
#30443=AXIS2_PLACEMENT_3D ( 'NONE', #21293, #4796, #28057 ) ;
#30446=FACE_OUTER_BOUND ( 'NONE', #60048, .T. ) ;
#30451=CARTESIAN_POINT ( 'NONE',  ( 10.00000000000000000, 0.000000000000000000, 0.000000000000000000 ) ) ;
#30455=CARTESIAN_POINT ( 'NONE',  ( 0.000000000000000000, 35.95386929396241271, 10.96151621346552751 ) ) ;
#30459=DIRECTION ( 'NONE',  ( -1.000000000000000000, -0.000000000000000000, -0.000000000000000000 ) ) ;
#30479=ADVANCED_FACE ( 'NONE', ( #73649 ), #44354, .T. ) ;
#30533=VERTEX_POINT ( 'NONE', #16516 ) ;
#30535=ADVANCED_FACE ( 'NONE', ( #9385 ), #55256, .T. ) ;
#30544=CARTESIAN_POINT ( 'NONE',  ( 10.00000000000000000, -5.202137450156655518, 37.22597642581156663 ) ) ;
#30545=VECTOR ( 'NONE', #52900, 1000.000000000000000 ) ;
#30551=AXIS2_PLACEMENT_3D ( 'NONE', #2874, #9952, #50163 ) ;
#30554=CARTESIAN_POINT ( 'NONE',  ( 0.000000000000000000, -0.6853352020793173072, 37.58145647212453611 ) ) ;
#30576=DIRECTION ( 'NONE',  ( -1.000000000000000000, -0.000000000000000000, 0.000000000000000000 ) ) ;
#30592=ORIENTED_EDGE ( 'NONE', *, *, #15592, .T. ) ;
#30593=ORIENTED_EDGE ( 'NONE', *, *, #41731, .T. ) ;
#30603=CIRCLE ( 'NONE', #23441, 16.00000000000000355 ) ;
#30620=FACE_OUTER_BOUND ( 'NONE', #34306, .T. ) ;
#30627=FACE_OUTER_BOUND ( 'NONE', #54530, .T. ) ;
#30634=CARTESIAN_POINT ( 'NONE',  ( 10.00000000000000000, -33.17418723428319538, 17.67226234102814431 ) ) ;
#30656=ADVANCED_FACE ( 'NONE', ( #62786 ), #35292, .T. ) ;
#30667=AXIS2_PLACEMENT_3D ( 'NONE', #19302, #52787, #53519 ) ;
#30701=DIRECTION ( 'NONE',  ( 0.000000000000000000, 0.000000000000000000, 1.000000000000000000 ) ) ;
#30702=EDGE_CURVE ( 'NONE', #67105, #15341, #7825, .T. ) ;
#30716=CIRCLE ( 'NONE', #25892, 16.00000000000000000 ) ;
#30737=CYLINDRICAL_SURFACE ( 'NONE', #43258, 42.00000000000000000 ) ;
#30745=DIRECTION ( 'NONE',  ( -1.000000000000000000, 0.000000000000000000, -0.000000000000000000 ) ) ;
#30747=DIRECTION ( 'NONE',  ( 0.000000000000000000, 0.000000000000000000, 1.000000000000000000 ) ) ;
#30751=AXIS2_PLACEMENT_3D ( 'NONE', #8885, #38194, #37473 ) ;
#30801=ORIENTED_EDGE ( 'NONE', *, *, #45498, .F. ) ;
#30804=CIRCLE ( 'NONE', #4383, 16.00000000000000000 ) ;
#30809=CYLINDRICAL_SURFACE ( 'NONE', #12633, 16.00000000000000000 ) ;
#30810=AXIS2_PLACEMENT_3D ( 'NONE', #24900, #35797, #58752 ) ;
#30826=DIRECTION ( 'NONE',  ( 1.000000000000000000, 0.000000000000000000, 0.000000000000000000 ) ) ;
#30847=ORIENTED_EDGE ( 'NONE', *, *, #27683, .T. ) ;
#30859=DIRECTION ( 'NONE',  ( 0.000000000000000000, 0.000000000000000000, 1.000000000000000000 ) ) ;
#30899=DIRECTION ( 'NONE',  ( -1.000000000000000000, -0.000000000000000000, 0.000000000000000000 ) ) ;
#30902=LINE ( 'NONE', #36546, #25093 ) ;
#30903=ORIENTED_EDGE ( 'NONE', *, *, #36345, .T. ) ;
#30949=DIRECTION ( 'NONE',  ( 0.000000000000000000, 0.000000000000000000, 1.000000000000000000 ) ) ;
#30956=ORIENTED_EDGE ( 'NONE', *, *, #457, .F. ) ;
#30974=CIRCLE ( 'NONE', #67043, 37.49900000000000944 ) ;
#31000=EDGE_CURVE ( 'NONE', #61584, #64608, #70725, .T. ) ;
#31003=CYLINDRICAL_SURFACE ( 'NONE', #7488, 42.00000000000000000 ) ;
#31010=LINE ( 'NONE', #6616, #70609 ) ;
#31016=CYLINDRICAL_SURFACE ( 'NONE', #1663, 16.00000000000000000 ) ;
#31035=CIRCLE ( 'NONE', #73057, 42.00000000000000000 ) ;
#31036=ADVANCED_FACE ( 'NONE', ( #31360 ), #59579, .T. ) ;
#31038=CARTESIAN_POINT ( 'NONE',  ( 10.00000000000000000, 30.84782396557218931, 21.32104025579126017 ) ) ;
#31093=CIRCLE ( 'NONE', #53913, 15.99999999999999822 ) ;
#31095=VERTEX_POINT ( 'NONE', #14062 ) ;
#31099=DIRECTION ( 'NONE',  ( -1.000000000000000000, -0.000000000000000000, -0.000000000000000000 ) ) ;
#31102=DIRECTION ( 'NONE',  ( 0.000000000000000000, 0.000000000000000000, 1.000000000000000000 ) ) ;
#31103=CARTESIAN_POINT ( 'NONE',  ( 10.00000000000000000, 0.000000000000000000, 0.000000000000000000 ) ) ;
#31126=EDGE_CURVE ( 'NONE', #4312, #63015, #40815, .T. ) ;
#31134=ORIENTED_EDGE ( 'NONE', *, *, #11388, .T. ) ;
#31144=ORIENTED_EDGE ( 'NONE', *, *, #2783, .F. ) ;
#31149=VECTOR ( 'NONE', #62338, 1000.000000000000000 ) ;
#31154=AXIS2_PLACEMENT_3D ( 'NONE', #68321, #44657, #57405 ) ;
#31161=ORIENTED_EDGE ( 'NONE', *, *, #15009, .T. ) ;
#31177=DIRECTION ( 'NONE',  ( -1.000000000000000000, -0.000000000000000000, -0.000000000000000000 ) ) ;
#31188=CIRCLE ( 'NONE', #9619, 42.00000000000000000 ) ;
#31203=CIRCLE ( 'NONE', #4834, 37.49900000000000944 ) ;
#31221=ADVANCED_FACE ( 'NONE', ( #44133 ), #21561, .T. ) ;
#31236=EDGE_LOOP ( 'NONE', ( #45589, #44953, #15365, #34762 ) ) ;
#31256=VECTOR ( 'NONE', #15447, 1000.000000000000000 ) ;
#31300=EDGE_CURVE ( 'NONE', #50488, #39943, #34796, .T. ) ;
#31306=VECTOR ( 'NONE', #34911, 1000.000000000000000 ) ;
#31309=DIRECTION ( 'NONE',  ( -1.000000000000000000, -0.000000000000000000, -0.000000000000000000 ) ) ;
#31317=ORIENTED_EDGE ( 'NONE', *, *, #59623, .F. ) ;
#31346=DIRECTION ( 'NONE',  ( 0.000000000000000000, 0.000000000000000000, 1.000000000000000000 ) ) ;
#31351=CARTESIAN_POINT ( 'NONE',  ( 10.00000000000000000, 33.80338159004307386, -16.23288003029461279 ) ) ;
#31360=FACE_OUTER_BOUND ( 'NONE', #128, .T. ) ;
#31365=CIRCLE ( 'NONE', #71013, 12.50000000000000000 ) ;
#31413=DIRECTION ( 'NONE',  ( 0.000000000000000000, -0.8090169943749403458, -0.5877852522924830181 ) ) ;
#31431=VERTEX_POINT ( 'NONE', #40669 ) ;
#31451=AXIS2_PLACEMENT_3D ( 'NONE', #8258, #14264, #36455 ) ;
#31452=DIRECTION ( 'NONE',  ( -1.000000000000000000, -0.000000000000000000, -0.000000000000000000 ) ) ;
#31465=ORIENTED_EDGE ( 'NONE', *, *, #37118, .F. ) ;
#31470=AXIS2_PLACEMENT_3D ( 'NONE', #14827, #53956, #43436 ) ;
#31502=DIRECTION ( 'NONE',  ( 0.000000000000000000, 0.7071067811865437980, 0.7071067811865512365 ) ) ;
#31506=ORIENTED_EDGE ( 'NONE', *, *, #17470, .F. ) ;
#31538=CARTESIAN_POINT ( 'NONE',  ( 0.000000000000000000, 0.000000000000000000, 0.000000000000000000 ) ) ;
#31540=ORIENTED_EDGE ( 'NONE', *, *, #16968, .F. ) ;
#31552=ADVANCED_FACE ( 'NONE', ( #12451 ), #24125, .T. ) ;
#31559=SHAPE_REPRESENTATION ( 'small gear_ISO - Spur gear 2M 40T 20PA 10FW ---S40A75H50L20.0N', ( #43395 ), #59053 ) ;
#31583=CARTESIAN_POINT ( 'NONE',  ( 10.00000000000000000, -16.23288003029521320, 33.80338159004277543 ) ) ;
#31586=ORIENTED_EDGE ( 'NONE', *, *, #1341, .T. ) ;
#31587=CARTESIAN_POINT ( 'NONE',  ( 10.00000000000000000, -27.13269053701078448, -25.88420570971428702 ) ) ;
#31589=ORIENTED_EDGE ( 'NONE', *, *, #17479, .T. ) ;
#31598=DIRECTION ( 'NONE',  ( 0.000000000000000000, 0.000000000000000000, -1.000000000000000000 ) ) ;
#31599=ORIENTED_EDGE ( 'NONE', *, *, #34150, .F. ) ;
#31606=DIRECTION ( 'NONE',  ( -1.000000000000000000, 0.000000000000000000, -0.000000000000000000 ) ) ;
#31670=EDGE_CURVE ( 'NONE', #53075, #56256, #36727, .T. ) ;
#31671=AXIS2_PLACEMENT_3D ( 'NONE', #42909, #36509, #30859 ) ;
#31675=DIRECTION ( 'NONE',  ( -1.000000000000000000, 0.000000000000000000, 0.000000000000000000 ) ) ;
#31682=CIRCLE ( 'NONE', #19659, 15.99999999999999822 ) ;
#31694=ORIENTED_EDGE ( 'NONE', *, *, #52022, .F. ) ;
#31704=ORIENTED_EDGE ( 'NONE', *, *, #33536, .F. ) ;
#31733=EDGE_CURVE ( 'NONE', #48642, #30113, #11505, .T. ) ;
#31737=ORIENTED_EDGE ( 'NONE', *, *, #13085, .T. ) ;
#31752=CARTESIAN_POINT ( 'NONE',  ( 0.000000000000000000, 29.81001611431041098, -22.74946021919100403 ) ) ;
#31784=DIRECTION ( 'NONE',  ( -1.000000000000000000, -0.000000000000000000, 0.000000000000000000 ) ) ;
#31806=CARTESIAN_POINT ( 'NONE',  ( 0.000000000000000000, 16.23288003029543347, -33.80338159004267595 ) ) ;
#31809=ORIENTED_EDGE ( 'NONE', *, *, #56706, .F. ) ;
#31822=EDGE_LOOP ( 'NONE', ( #29977, #15480, #29775, #25034 ) ) ;
#31828=VERTEX_POINT ( 'NONE', #22836 ) ;
#31834=EDGE_CURVE ( 'NONE', #14575, #49911, #65789, .T. ) ;
#31857=CIRCLE ( 'NONE', #73878, 16.00000000000000000 ) ;
#31860=ORIENTED_EDGE ( 'NONE', *, *, #17516, .T. ) ;
#31862=DIRECTION ( 'NONE',  ( 0.000000000000000000, 0.000000000000000000, -1.000000000000000000 ) ) ;
#31878=EDGE_CURVE ( 'NONE', #35308, #21754, #3393, .T. ) ;
#31887=DIRECTION ( 'NONE',  ( 0.000000000000000000, 0.000000000000000000, -1.000000000000000000 ) ) ;
#31896=DIRECTION ( 'NONE',  ( 0.000000000000000000, 0.000000000000000000, 1.000000000000000000 ) ) ;
#31901=ORIENTED_EDGE ( 'NONE', *, *, #62059, .T. ) ;
#31909=ORIENTED_EDGE ( 'NONE', *, *, #65343, .F. ) ;
#31929=CARTESIAN_POINT ( 'NONE',  ( 10.00000000000000000, 12.26510123303308752, -35.53030884539072787 ) ) ;
#31936=CARTESIAN_POINT ( 'NONE',  ( 10.00000000000000000, 0.000000000000000000, 0.000000000000000000 ) ) ;
#31978=EDGE_LOOP ( 'NONE', ( #5980, #71031, #30903, #65295 ) ) ;
#31996=CIRCLE ( 'NONE', #40381, 16.00000000000000000 ) ;
#32026=CARTESIAN_POINT ( 'NONE',  ( 10.00000000000000000, 29.81001611431041098, -22.74946021919100403 ) ) ;
#32041=DIRECTION ( 'NONE',  ( -1.000000000000000000, 0.000000000000000000, 0.000000000000000000 ) ) ;
#32043=AXIS2_PLACEMENT_3D ( 'NONE', #44561, #1867, #49806 ) ;
#32049=DIRECTION ( 'NONE',  ( -1.000000000000000000, 0.000000000000000000, 0.000000000000000000 ) ) ;
#32053=EDGE_CURVE ( 'NONE', #49911, #34884, #32522, .T. ) ;
#32066=CARTESIAN_POINT ( 'NONE',  ( 0.000000000000000000, -22.74946021919153694, 29.81001611431000597 ) ) ;
#32071=DIRECTION ( 'NONE',  ( 0.000000000000000000, 0.000000000000000000, 1.000000000000000000 ) ) ;
#32105=AXIS2_PLACEMENT_3D ( 'NONE', #24092, #59402, #64671 ) ;
#32109=CYLINDRICAL_SURFACE ( 'NONE', #49928, 42.00000000000000000 ) ;
#32133=EDGE_CURVE ( 'NONE', #53810, #38967, #26163, .T. ) ;
#32158=ORIENTED_EDGE ( 'NONE', *, *, #66207, .F. ) ;
#32168=CARTESIAN_POINT ( 'NONE',  ( 10.00000000000000000, 0.000000000000000000, 0.000000000000000000 ) ) ;
#32170=ORIENTED_EDGE ( 'NONE', *, *, #39639, .F. ) ;
#32173=ORIENTED_EDGE ( 'NONE', *, *, #40593, .T. ) ;
#32174=FACE_OUTER_BOUND ( 'NONE', #27118, .T. ) ;
#32207=DIRECTION ( 'NONE',  ( -1.000000000000000000, 0.000000000000000000, 0.000000000000000000 ) ) ;
#32209=CARTESIAN_POINT ( 'NONE',  ( 10.00000000000000000, -35.95386929396248377, -10.96151621346525751 ) ) ;
#32210=FACE_OUTER_BOUND ( 'NONE', #21368, .T. ) ;
#32211=DIRECTION ( 'NONE',  ( -1.000000000000000000, -0.000000000000000000, -0.000000000000000000 ) ) ;
#32223=CIRCLE ( 'NONE', #13017, 42.00000000000000000 ) ;
#32243=ORIENTED_EDGE ( 'NONE', *, *, #70365, .T. ) ;
#32249=AXIS2_PLACEMENT_3D ( 'NONE', #6081, #462, #47028 ) ;
#32257=ORIENTED_EDGE ( 'NONE', *, *, #60798, .F. ) ;
#32282=ORIENTED_EDGE ( 'NONE', *, *, #43474, .T. ) ;
#32304=CIRCLE ( 'NONE', #74338, 37.49900000000000233 ) ;
#32314=CIRCLE ( 'NONE', #52721, 42.00000000000000000 ) ;
#32326=AXIS2_PLACEMENT_3D ( 'NONE', #64268, #39862, #6746 ) ;
#32334=EDGE_CURVE ( 'NONE', #54634, #50408, #52631, .T. ) ;
#32346=ORIENTED_EDGE ( 'NONE', *, *, #7201, .F. ) ;
#32351=EDGE_CURVE ( 'NONE', #8457, #30109, #51388, .T. ) ;
#32356=AXIS2_PLACEMENT_3D ( 'NONE', #73435, #10289, #33209 ) ;
#32363=ORIENTED_EDGE ( 'NONE', *, *, #65266, .T. ) ;
#32381=CARTESIAN_POINT ( 'NONE',  ( 4.999999999999999112, -9.188173127307592836, 40.98264845739746676 ) ) ;
#32385=AXIS2_PLACEMENT_3D ( 'NONE', #5877, #74279, #56255 ) ;
#32389=AXIS2_PLACEMENT_3D ( 'NONE', #24388, #35299, #58976 ) ;
#32395=ORIENTED_EDGE ( 'NONE', *, *, #52804, .T. ) ;
#32396=LINE ( 'NONE', #32026, #29366 ) ;
#32421=CARTESIAN_POINT ( 'NONE',  ( 0.000000000000000000, 0.000000000000000000, 0.000000000000000000 ) ) ;
#32425=CYLINDRICAL_SURFACE ( 'NONE', #60411, 42.00000000000000000 ) ;
#32426=ORIENTED_EDGE ( 'NONE', *, *, #49204, .T. ) ;
#32441=CARTESIAN_POINT ( 'NONE',  ( 10.00000000000000000, -4.992566952385247170, 37.16516213103275845 ) ) ;
#32453=DIRECTION ( 'NONE',  ( 1.000000000000000000, -0.000000000000000000, -0.000000000000000000 ) ) ;
#32458=LINE ( 'NONE', #31351, #51469 ) ;
#32481=CARTESIAN_POINT ( 'NONE',  ( 10.00000000000000000, 0.000000000000000000, 0.000000000000000000 ) ) ;
#32485=CARTESIAN_POINT ( 'NONE',  ( 0.000000000000000000, 16.45098606841126454, 33.79645857604518966 ) ) ;
#32489=EDGE_CURVE ( 'NONE', #17385, #24964, #37359, .T. ) ;
#32490=AXIS2_PLACEMENT_3D ( 'NONE', #31929, #9370, #15761 ) ;
#32515=ORIENTED_EDGE ( 'NONE', *, *, #71300, .F. ) ;
#32518=CARTESIAN_POINT ( 'NONE',  ( 4.999999999999999112, -16.65560815589383381, -38.55633173627028754 ) ) ;
#32522=LINE ( 'NONE', #8863, #46573 ) ;
#32536=VERTEX_POINT ( 'NONE', #26429 ) ;
#32546=ORIENTED_EDGE ( 'NONE', *, *, #48734, .T. ) ;
#32562=DIRECTION ( 'NONE',  ( -1.000000000000000000, 0.000000000000000000, 0.000000000000000000 ) ) ;
#32575=ADVANCED_FACE ( 'NONE', ( #42258 ), #36596, .T. ) ;
#32584=CARTESIAN_POINT ( 'NONE',  ( 10.00000000000000000, -30.84782396557233142, 21.32104025579104345 ) ) ;
#32600=CIRCLE ( 'NONE', #8575, 37.49900000000000233 ) ;
#32601=CARTESIAN_POINT ( 'NONE',  ( 0.000000000000000000, -35.47612816024539484, 22.48208911017487921 ) ) ;
#32626=CARTESIAN_POINT ( 'NONE',  ( 0.000000000000000000, 26.08949754953062694, -27.05870788708203989 ) ) ;
#32628=DIRECTION ( 'NONE',  ( -1.000000000000000000, 0.000000000000000000, 0.000000000000000000 ) ) ;
#32632=DIRECTION ( 'NONE',  ( -1.000000000000000000, 0.000000000000000000, 0.000000000000000000 ) ) ;
#32640=ORIENTED_EDGE ( 'NONE', *, *, #28342, .T. ) ;
#32645=CYLINDRICAL_SURFACE ( 'NONE', #8068, 16.00000000000000000 ) ;
#32653=ORIENTED_EDGE ( 'NONE', *, *, #29799, .F. ) ;
#32678=DIRECTION ( 'NONE',  ( 0.000000000000000000, 0.000000000000000000, 1.000000000000000000 ) ) ;
#32697=ORIENTED_EDGE ( 'NONE', *, *, #18849, .T. ) ;
#32735=AXIS2_PLACEMENT_3D ( 'NONE', #72278, #45211, #61760 ) ;
#32754=CARTESIAN_POINT ( 'NONE',  ( 0.000000000000000000, -38.55633173627022359, 16.65560815589396526 ) ) ;
#32760=EDGE_LOOP ( 'NONE', ( #66912, #57402, #22205, #48470 ) ) ;
#32761=EDGE_CURVE ( 'NONE', #43377, #72913, #57612, .T. ) ;
#32775=DIRECTION ( 'NONE',  ( 0.000000000000000000, -0.5877852522924801315, 0.8090169943749421222 ) ) ;
#32792=LINE ( 'NONE', #31038, #39039 ) ;
#32800=ORIENTED_EDGE ( 'NONE', *, *, #8663, .T. ) ;
#32817=EDGE_CURVE ( 'NONE', #74032, #40680, #47068, .T. ) ;
#32841=ORIENTED_EDGE ( 'NONE', *, *, #18997, .F. ) ;
#32843=ADVANCED_FACE ( 'NONE', ( #63988 ), #17373, .T. ) ;
#32845=EDGE_CURVE ( 'NONE', #1093, #12587, #29865, .T. ) ;
#32878=CARTESIAN_POINT ( 'NONE',  ( 10.00000000000000000, -25.88420570971381807, -27.13269053701123212 ) ) ;
#32880=LINE ( 'NONE', #66387, #58466 ) ;
#32887=CARTESIAN_POINT ( 'NONE',  ( 0.000000000000000000, 29.81001611431009479, 22.74946021919143391 ) ) ;
#32909=EDGE_CURVE ( 'NONE', #4807, #38459, #49081, .T. ) ;
#32915=EDGE_LOOP ( 'NONE', ( #34638, #56070, #33438, #66186 ) ) ;
#32918=ORIENTED_EDGE ( 'NONE', *, *, #69124, .F. ) ;
#32936=DIRECTION ( 'NONE',  ( 0.000000000000000000, 0.000000000000000000, 1.000000000000000000 ) ) ;
#32949=FACE_OUTER_BOUND ( 'NONE', #25245, .T. ) ;
#32957=AXIS2_PLACEMENT_3D ( 'NONE', #59473, #35780, #71838 ) ;
#32964=CIRCLE ( 'NONE', #607, 16.00000000000000000 ) ;
#32967=ORIENTED_EDGE ( 'NONE', *, *, #46713, .T. ) ;
#32971=DIRECTION ( 'NONE',  ( -1.000000000000000000, 0.000000000000000000, 0.000000000000000000 ) ) ;
#32995=EDGE_CURVE ( 'NONE', #54409, #26601, #9420, .T. ) ;
#33008=CIRCLE ( 'NONE', #41394, 16.00000000000000000 ) ;
#33009=EDGE_CURVE ( 'NONE', #45064, #68267, #38740, .T. ) ;
#33019=EDGE_LOOP ( 'NONE', ( #10836, #68610, #10901, #21903 ) ) ;
#33033=FACE_OUTER_BOUND ( 'NONE', #55387, .T. ) ;
#33050=FACE_OUTER_BOUND ( 'NONE', #40527, .T. ) ;
#33051=CARTESIAN_POINT ( 'NONE',  ( 10.00000000000000000, 0.000000000000000000, 0.000000000000000000 ) ) ;
#33060=LINE ( 'NONE', #39472, #17409 ) ;
#33068=ADVANCED_FACE ( 'NONE', ( #43649 ), #39488, .T. ) ;
#33071=CIRCLE ( 'NONE', #55905, 15.99999999999999645 ) ;
#33082=( NAMED_UNIT ( * ) PLANE_ANGLE_UNIT ( ) SI_UNIT ( $, .RADIAN. ) );
#33092=LINE ( 'NONE', #16554, #30021 ) ;
#33099=ORIENTED_EDGE ( 'NONE', *, *, #49204, .F. ) ;
#33123=EDGE_LOOP ( 'NONE', ( #12485, #36346, #53558, #40979 ) ) ;
#33136=DIRECTION ( 'NONE',  ( 0.000000000000000000, 0.000000000000000000, -1.000000000000000000 ) ) ;
#33169=ORIENTED_EDGE ( 'NONE', *, *, #57389, .T. ) ;
#33183=EDGE_CURVE ( 'NONE', #74032, #69905, #35937, .T. ) ;
#33186=ORIENTED_EDGE ( 'NONE', *, *, #44913, .F. ) ;
#33189=EDGE_CURVE ( 'NONE', #43729, #20222, #49145, .T. ) ;
#33190=ORIENTED_EDGE ( 'NONE', *, *, #12021, .F. ) ;
#33195=CARTESIAN_POINT ( 'NONE',  ( 10.00000000000000000, 33.80338159004283938, 16.23288003029508886 ) ) ;
#33201=EDGE_CURVE ( 'NONE', #69905, #45064, #3556, .T. ) ;
#33209=DIRECTION ( 'NONE',  ( 0.000000000000000000, 0.7071067811865487940, -0.7071067811865462405 ) ) ;
#33231=CIRCLE ( 'NONE', #30810, 37.49900000000000233 ) ;
#33268=ORIENTED_EDGE ( 'NONE', *, *, #70165, .T. ) ;
#33276=CIRCLE ( 'NONE', #54913, 37.49900000000000233 ) ;
#33286=EDGE_CURVE ( 'NONE', #20440, #20082, #34950, .T. ) ;
#33304=CARTESIAN_POINT ( 'NONE',  ( 10.00000000000000000, 0.8828120875900632436, 37.48860685352291000 ) ) ;
#33305=LINE ( 'NONE', #4783, #48510 ) ;
#33316=DIRECTION ( 'NONE',  ( 0.000000000000000000, 0.000000000000000000, 1.000000000000000000 ) ) ;
#33337=DIRECTION ( 'NONE',  ( 0.000000000000000000, 0.5877852522924744694, -0.8090169943749465631 ) ) ;
#33347=CIRCLE ( 'NONE', #62201, 42.00000000000000000 ) ;
#33349=DIRECTION ( 'NONE',  ( -1.000000000000000000, 0.000000000000000000, -0.000000000000000000 ) ) ;
#33388=AXIS2_PLACEMENT_3D ( 'NONE', #4242, #71147, #19652 ) ;
#33396=DIRECTION ( 'NONE',  ( 1.000000000000000000, 0.000000000000000000, 0.000000000000000000 ) ) ;
#33401=CIRCLE ( 'NONE', #3436, 37.49900000000000944 ) ;
#33404=AXIS2_PLACEMENT_3D ( 'NONE', #9262, #19424, #14530 ) ;
#33438=ORIENTED_EDGE ( 'NONE', *, *, #45196, .T. ) ;
#33455=ORIENTED_EDGE ( 'NONE', *, *, #64686, .T. ) ;
#33475=AXIS2_PLACEMENT_3D ( 'NONE', #50867, #23057, #45248 ) ;
#33477=ADVANCED_FACE ( 'NONE', ( #19858 ), #7848, .T. ) ;
#33479=CARTESIAN_POINT ( 'NONE',  ( 10.00000000000000000, -35.92658777277517856, 10.74501242461269257 ) ) ;
#33502=EDGE_LOOP ( 'NONE', ( #59244, #11093, #11759, #51815 ) ) ;
#33512=DIRECTION ( 'NONE',  ( 1.000000000000000000, -0.000000000000000000, -0.000000000000000000 ) ) ;
#33533=VECTOR ( 'NONE', #74176, 1000.000000000000000 ) ;
#33536=EDGE_CURVE ( 'NONE', #11375, #47114, #70691, .T. ) ;
#33541=CIRCLE ( 'NONE', #23955, 37.49900000000001654 ) ;
#33551=ORIENTED_EDGE ( 'NONE', *, *, #64686, .F. ) ;
#33580=CARTESIAN_POINT ( 'NONE',  ( 10.00000000000000000, 12.42422080174639021, 35.38097989696516521 ) ) ;
#33581=DIRECTION ( 'NONE',  ( 0.000000000000000000, 0.000000000000000000, 1.000000000000000000 ) ) ;
#33589=LINE ( 'NONE', #184, #39485 ) ;
#33644=ORIENTED_EDGE ( 'NONE', *, *, #10890, .F. ) ;
#33650=CARTESIAN_POINT ( 'NONE',  ( 10.00000000000000000, 27.75498641678786527, -31.52238457039571173 ) ) ;
#33668=CARTESIAN_POINT ( 'NONE',  ( 0.000000000000000000, -2.663952781845850826, -41.91543099594819921 ) ) ;
#33669=EDGE_LOOP ( 'NONE', ( #69747, #44109, #39951, #70991 ) ) ;
#33690=AXIS2_PLACEMENT_3D ( 'NONE', #60647, #68024, #19645 ) ;
#33716=CARTESIAN_POINT ( 'NONE',  ( 10.00000000000000000, 0.000000000000000000, 0.000000000000000000 ) ) ;
#33717=ORIENTED_EDGE ( 'NONE', *, *, #41968, .F. ) ;
#33723=EDGE_CURVE ( 'NONE', #63727, #50408, #35505, .T. ) ;
#33730=VECTOR ( 'NONE', #30083, 1000.000000000000000 ) ;
#33748=ORIENTED_EDGE ( 'NONE', *, *, #20394, .T. ) ;
#33749=DIRECTION ( 'NONE',  ( -1.000000000000000000, 0.000000000000000000, -0.000000000000000000 ) ) ;
#33767=VECTOR ( 'NONE', #50212, 1000.000000000000000 ) ;
#33809=EDGE_CURVE ( 'NONE', #37625, #34470, #20053, .T. ) ;
#33810=ADVANCED_FACE ( 'NONE', ( #20799 ), #72301, .T. ) ;
#33811=CARTESIAN_POINT ( 'NONE',  ( 10.00000000000000000, 0.000000000000000000, 0.000000000000000000 ) ) ;
#33819=AXIS2_PLACEMENT_3D ( 'NONE', #39981, #58370, #24171 ) ;
#33833=CARTESIAN_POINT ( 'NONE',  ( 10.00000000000000000, 0.000000000000000000, 0.000000000000000000 ) ) ;
#33834=ORIENTED_EDGE ( 'NONE', *, *, #11797, .F. ) ;
#33883=LINE ( 'NONE', #74099, #12734 ) ;
#33894=EDGE_CURVE ( 'NONE', #25438, #60516, #37370, .T. ) ;
#33902=ORIENTED_EDGE ( 'NONE', *, *, #5707, .T. ) ;
#33910=CARTESIAN_POINT ( 'NONE',  ( -10.00000000000000000, 0.000000000000000000, 0.000000000000000000 ) ) ;
#33914=DIRECTION ( 'NONE',  ( -1.000000000000000000, -0.000000000000000000, -0.000000000000000000 ) ) ;
#33946=CARTESIAN_POINT ( 'NONE',  ( 50.00005079999999680, 12.24744871391589207, -2.499999999999994671 ) ) ;
#33951=CARTESIAN_POINT ( 'NONE',  ( 0.000000000000000000, -36.88895765772637247, 6.736453364083436313 ) ) ;
#33962=CARTESIAN_POINT ( 'NONE',  ( 0.000000000000000000, -10.41901085202050581, -40.68715046381939970 ) ) ;
#33992=AXIS2_PLACEMENT_3D ( 'NONE', #12895, #35824, #63692 ) ;
#34014=EDGE_CURVE ( 'NONE', #16321, #21495, #5754, .T. ) ;
#34025=ORIENTED_EDGE ( 'NONE', *, *, #29091, .T. ) ;
#34044=VERTEX_POINT ( 'NONE', #51223 ) ;
#34052=CYLINDRICAL_SURFACE ( 'NONE', #17938, 16.00000000000000000 ) ;
#34076=CARTESIAN_POINT ( 'NONE',  ( 10.00000000000000000, 33.17418723428307459, 17.67226234102837878 ) ) ;
#34090=CARTESIAN_POINT ( 'NONE',  ( 0.000000000000000000, 0.000000000000000000, 0.000000000000000000 ) ) ;
#34102=CARTESIAN_POINT ( 'NONE',  ( 10.00000000000000000, 10.96151621346487914, 35.95386929396260456 ) ) ;
#34109=CARTESIAN_POINT ( 'NONE',  ( 10.00000000000000000, -12.26510123303234501, -35.53030884539098366 ) ) ;
#34121=CARTESIAN_POINT ( 'NONE',  ( 10.00000000000000000, -6.736453364083292428, -36.88895765772640800 ) ) ;
#34129=AXIS2_PLACEMENT_3D ( 'NONE', #5148, #56260, #45367 ) ;
#34130=ADVANCED_FACE ( 'NONE', ( #53083, #58347 ), #57982, .F. ) ;
#34131=ORIENTED_EDGE ( 'NONE', *, *, #38897, .F. ) ;
#34136=VERTEX_POINT ( 'NONE', #511 ) ;
#34150=EDGE_CURVE ( 'NONE', #54409, #24772, #23043, .T. ) ;
#34152=AXIS2_PLACEMENT_3D ( 'NONE', #13117, #36055, #59000 ) ;
#34158=DIRECTION ( 'NONE',  ( 0.000000000000000000, 0.000000000000000000, 1.000000000000000000 ) ) ;
#34165=CIRCLE ( 'NONE', #53367, 15.99999999999999467 ) ;
#34170=AXIS2_PLACEMENT_3D ( 'NONE', #64688, #41745, #1942 ) ;
#34199=CARTESIAN_POINT ( 'NONE',  ( 0.000000000000000000, 35.95386929396256903, -10.96151621346501237 ) ) ;
#34220=VECTOR ( 'NONE', #73523, 1000.000000000000000 ) ;
#34226=CARTESIAN_POINT ( 'NONE',  ( 10.00000000000000000, -17.80606268964563554, 33.00180498840040855 ) ) ;
#34243=CARTESIAN_POINT ( 'NONE',  ( 10.00000000000000000, 39.04073710021344112, 15.48615015657596317 ) ) ;
#34255=EDGE_LOOP ( 'NONE', ( #10334, #34492, #37546, #4944 ) ) ;
#34274=AXIS2_PLACEMENT_3D ( 'NONE', #12914, #30576, #58796 ) ;
#34289=EDGE_LOOP ( 'NONE', ( #37900, #20628, #48182, #51646 ) ) ;
#34297=EDGE_CURVE ( 'NONE', #49630, #57628, #55259, .T. ) ;
#34298=EDGE_LOOP ( 'NONE', ( #27259, #14159, #2573, #14921 ) ) ;
#34306=EDGE_LOOP ( 'NONE', ( #2526, #60106, #61969, #19519 ) ) ;
#34319=CARTESIAN_POINT ( 'NONE',  ( 10.00000000000000000, 0.000000000000000000, 0.000000000000000000 ) ) ;
#34347=ORIENTED_EDGE ( 'NONE', *, *, #31834, .T. ) ;
#34356=EDGE_CURVE ( 'NONE', #47902, #1611, #36037, .T. ) ;
#34364=DIRECTION ( 'NONE',  ( 0.000000000000000000, -0.5877852522924624790, -0.8090169943749550008 ) ) ;
#34375=ORIENTED_EDGE ( 'NONE', *, *, #56208, .T. ) ;
#34398=DIRECTION ( 'NONE',  ( -1.000000000000000000, 0.000000000000000000, 0.000000000000000000 ) ) ;
#34425=ADVANCED_FACE ( 'NONE', ( #68062 ), #45141, .T. ) ;
#34441=EDGE_CURVE ( 'NONE', #73312, #20472, #33092, .T. ) ;
#34445=AXIS2_PLACEMENT_3D ( 'NONE', #19394, #36688, #59630 ) ;
#34446=EDGE_CURVE ( 'NONE', #7952, #52503, #73222, .T. ) ;
#34470=VERTEX_POINT ( 'NONE', #38379 ) ;
#34473=LINE ( 'NONE', #23943, #10442 ) ;
#34492=ORIENTED_EDGE ( 'NONE', *, *, #69941, .T. ) ;
#34513=DIRECTION ( 'NONE',  ( -1.000000000000000000, -0.000000000000000000, 0.000000000000000000 ) ) ;
#34538=DIRECTION ( 'NONE',  ( 0.000000000000000000, 0.000000000000000000, 1.000000000000000000 ) ) ;
#34558=VERTEX_POINT ( 'NONE', #35684 ) ;
#34567=AXIS2_PLACEMENT_3D ( 'NONE', #8837, #66361, #14089 ) ;
#34568=CIRCLE ( 'NONE', #34749, 37.49900000000000944 ) ;
#34572=ORIENTED_EDGE ( 'NONE', *, *, #64282, .F. ) ;
#34584=DIRECTION ( 'NONE',  ( -1.000000000000000000, 0.000000000000000000, 0.000000000000000000 ) ) ;
#34586=ADVANCED_BREP_SHAPE_REPRESENTATION ( '', ( #62016, #43395 ), #59053 ) ;
#34588=ORIENTED_EDGE ( 'NONE', *, *, #41414, .F. ) ;
#34592=AXIS2_PLACEMENT_3D ( 'NONE', #38179, #8507, #42718 ) ;
#34594=AXIS2_PLACEMENT_3D ( 'NONE', #11209, #44695, #45438 ) ;
#34604=DIRECTION ( 'NONE',  ( 0.000000000000000000, 0.000000000000000000, -1.000000000000000000 ) ) ;
#34607=CARTESIAN_POINT ( 'NONE',  ( 0.000000000000000000, -35.38097989696503021, -12.42422080174676147 ) ) ;
#34614=EDGE_CURVE ( 'NONE', #24962, #49804, #42127, .T. ) ;
#34617=ADVANCED_FACE ( 'NONE', ( #47355 ), #18042, .T. ) ;
#34618=DIRECTION ( 'NONE',  ( 0.000000000000000000, -6.938893903907228378E-15, 1.000000000000000000 ) ) ;
#34619=DIRECTION ( 'NONE',  ( 0.000000000000000000, 0.000000000000000000, 1.000000000000000000 ) ) ;
#34631=DIRECTION ( 'NONE',  ( 0.000000000000000000, 0.8910065241883688980, -0.4539904997395446951 ) ) ;
#34633=FACE_OUTER_BOUND ( 'NONE', #65049, .T. ) ;
#34638=ORIENTED_EDGE ( 'NONE', *, *, #45498, .T. ) ;
#34646=ADVANCED_FACE ( 'NONE', ( #22740 ), #11793, .T. ) ;
#34651=CARTESIAN_POINT ( 'NONE',  ( 0.000000000000000000, 17.67226234102826510, 33.17418723428314564 ) ) ;
#34665=FACE_OUTER_BOUND ( 'NONE', #10608, .T. ) ;
#34678=ORIENTED_EDGE ( 'NONE', *, *, #10154, .F. ) ;
#34684=CARTESIAN_POINT ( 'NONE',  ( 10.00000000000000000, 0.000000000000000000, 0.000000000000000000 ) ) ;
#34685=AXIS2_PLACEMENT_3D ( 'NONE', #24120, #59432, #28998 ) ;
#34709=EDGE_CURVE ( 'NONE', #1535, #4351, #52397, .T. ) ;
#34712=EDGE_CURVE ( 'NONE', #51075, #73312, #28856, .T. ) ;
#34717=CARTESIAN_POINT ( 'NONE',  ( 10.00000000000000000, 0.000000000000000000, 0.000000000000000000 ) ) ;
#34718=CARTESIAN_POINT ( 'NONE',  ( 10.00000000000000000, 21.40280677340372151, 36.13751322684426981 ) ) ;
#34749=AXIS2_PLACEMENT_3D ( 'NONE', #5535, #69398, #29168 ) ;
#34762=ORIENTED_EDGE ( 'NONE', *, *, #68791, .T. ) ;
#34776=CARTESIAN_POINT ( 'NONE',  ( 10.00000000000000000, 27.13269053701096922, 25.88420570971410228 ) ) ;
#34782=CARTESIAN_POINT ( 'NONE',  ( 10.00000000000000000, -10.41901085202050403, -40.68715046381940681 ) ) ;
#34784=ORIENTED_EDGE ( 'NONE', *, *, #1330, .T. ) ;
#34794=DIRECTION ( 'NONE',  ( -1.000000000000000000, 0.000000000000000000, 0.000000000000000000 ) ) ;
#34796=CIRCLE ( 'NONE', #62447, 42.00000000000000000 ) ;
#34799=CARTESIAN_POINT ( 'NONE',  ( 5.000000000000000000, 41.91543099594818500, -2.663952781846291362 ) ) ;
#34806=EDGE_CURVE ( 'NONE', #63739, #53879, #30086, .T. ) ;
#34812=DIRECTION ( 'NONE',  ( 0.000000000000000000, 0.000000000000000000, -1.000000000000000000 ) ) ;
#34821=CARTESIAN_POINT ( 'NONE',  ( 0.000000000000000000, 0.000000000000000000, 0.000000000000000000 ) ) ;
#34829=CARTESIAN_POINT ( 'NONE',  ( 0.000000000000000000, 27.75498641678786527, -31.52238457039571173 ) ) ;
#34868=LINE ( 'NONE', #51042, #25722 ) ;
#34884=VERTEX_POINT ( 'NONE', #13288 ) ;
#34885=CARTESIAN_POINT ( 'NONE',  ( 10.00000000000000000, 37.58145647212453611, 16.68533520207917675 ) ) ;
#34896=ORIENTED_EDGE ( 'NONE', *, *, #71282, .T. ) ;
#34898=FACE_OUTER_BOUND ( 'NONE', #25339, .T. ) ;
#34906=ORIENTED_EDGE ( 'NONE', *, *, #52186, .F. ) ;
#34911=DIRECTION ( 'NONE',  ( -1.000000000000000000, 0.000000000000000000, 0.000000000000000000 ) ) ;
#34918=ADVANCED_FACE ( 'NONE', ( #2432 ), #25321, .T. ) ;
#34926=CARTESIAN_POINT ( 'NONE',  ( 10.00000000000000000, -22.74946021919153694, 29.81001611431000597 ) ) ;
#34934=DIRECTION ( 'NONE',  ( 0.000000000000000000, 0.000000000000000000, 1.000000000000000000 ) ) ;
#34941=ORIENTED_EDGE ( 'NONE', *, *, #7917, .F. ) ;
#34950=LINE ( 'NONE', #57889, #50318 ) ;
#34952=CIRCLE ( 'NONE', #12140, 16.00000000000000000 ) ;
#34955=( LENGTH_UNIT ( ) NAMED_UNIT ( * ) SI_UNIT ( .MILLI., .METRE. ) );
#34959=CARTESIAN_POINT ( 'NONE',  ( 0.000000000000000000, -33.80338159004296017, 16.23288003029484727 ) ) ;
#34969=ORIENTED_EDGE ( 'NONE', *, *, #45269, .T. ) ;
#34976=ORIENTED_EDGE ( 'NONE', *, *, #60380, .T. ) ;
#34979=CIRCLE ( 'NONE', #45842, 37.49900000000000233 ) ;
#35003=CARTESIAN_POINT ( 'NONE',  ( 10.00000000000000000, 22.74946021919175720, -29.81001611430984255 ) ) ;
#35009=AXIS2_PLACEMENT_3D ( 'NONE', #42226, #61265, #38700 ) ;
#35017=AXIS2_PLACEMENT_3D ( 'NONE', #69103, #40520, #46532 ) ;
#35022=DIRECTION ( 'NONE',  ( -1.000000000000000000, -0.000000000000000000, -0.000000000000000000 ) ) ;
#35023=CARTESIAN_POINT ( 'NONE',  ( 10.00000000000000000, -41.81611651403864727, 3.925862922256025289 ) ) ;
#35026=EDGE_LOOP ( 'NONE', ( #74139, #34347, #42470, #51900 ) ) ;
#35037=DIRECTION ( 'NONE',  ( -1.000000000000000000, -0.000000000000000000, 0.000000000000000000 ) ) ;
#35042=EDGE_LOOP ( 'NONE', ( #28484, #43570, #50695, #34025 ) ) ;
#35046=EDGE_LOOP ( 'NONE', ( #24504, #22574, #1003, #36978 ) ) ;
#35048=ORIENTED_EDGE ( 'NONE', *, *, #2162, .T. ) ;
#35060=AXIS2_PLACEMENT_3D ( 'NONE', #31936, #19910, #65795 ) ;
#35061=CYLINDRICAL_SURFACE ( 'NONE', #25785, 16.00000000000000000 ) ;
#35068=AXIS2_PLACEMENT_3D ( 'NONE', #22605, #45550, #69204 ) ;
#35069=ORIENTED_EDGE ( 'NONE', *, *, #15215, .T. ) ;
#35074=DIRECTION ( 'NONE',  ( -1.000000000000000000, 0.000000000000000000, 0.000000000000000000 ) ) ;
#35088=ORIENTED_EDGE ( 'NONE', *, *, #49964, .T. ) ;
#35096=DIRECTION ( 'NONE',  ( -1.000000000000000000, 0.000000000000000000, 0.000000000000000000 ) ) ;
#35116=ORIENTED_EDGE ( 'NONE', *, *, #71633, .T. ) ;
#35118=CARTESIAN_POINT ( 'NONE',  ( 10.00000000000000000, 37.48860685352291000, -0.8828120875901940279 ) ) ;
#35123=EDGE_CURVE ( 'NONE', #28591, #54942, #22537, .T. ) ;
#35149=DIRECTION ( 'NONE',  ( -1.000000000000000000, 0.000000000000000000, 0.000000000000000000 ) ) ;
#35197=CARTESIAN_POINT ( 'NONE',  ( 0.000000000000000000, -26.79245525562738095, 32.34446384429961796 ) ) ;
#35210=ORIENTED_EDGE ( 'NONE', *, *, #12481, .T. ) ;
#35292=CYLINDRICAL_SURFACE ( 'NONE', #63576, 37.49900000000000233 ) ;
#35299=DIRECTION ( 'NONE',  ( -1.000000000000000000, 0.000000000000000000, -0.000000000000000000 ) ) ;
#35301=FACE_OUTER_BOUND ( 'NONE', #2248, .T. ) ;
#35302=VECTOR ( 'NONE', #61039, 1000.000000000000000 ) ;
#35308=VERTEX_POINT ( 'NONE', #59331 ) ;
#35323=CIRCLE ( 'NONE', #41332, 37.49900000000001654 ) ;
#35324=SURFACE_SIDE_STYLE ('',( #36417 ) ) ;
#35358=ORIENTED_EDGE ( 'NONE', *, *, #40609, .T. ) ;
#35374=DIRECTION ( 'NONE',  ( -0.000000000000000000, 0.000000000000000000, 1.000000000000000000 ) ) ;
#35381=CYLINDRICAL_SURFACE ( 'NONE', #10529, 42.00000000000000000 ) ;
#35388=LINE ( 'NONE', #53777, #28745 ) ;
#35401=CARTESIAN_POINT ( 'NONE',  ( 10.00000000000000000, 0.6853352020795618893, -37.58145647212453611 ) ) ;
#35437=CARTESIAN_POINT ( 'NONE',  ( 10.00000000000000000, -29.81001611431024756, 22.74946021919122785 ) ) ;
#35439=CIRCLE ( 'NONE', #17458, 16.00000000000000355 ) ;
#35465=EDGE_CURVE ( 'NONE', #7320, #56343, #16997, .T. ) ;
#35503=EDGE_LOOP ( 'NONE', ( #63354, #27247, #29199, #33748 ) ) ;
#35505=LINE ( 'NONE', #6925, #31149 ) ;
#35508=VERTEX_POINT ( 'NONE', #16428 ) ;
#35516=CARTESIAN_POINT ( 'NONE',  ( 0.000000000000000000, 0.000000000000000000, 0.000000000000000000 ) ) ;
#35538=CARTESIAN_POINT ( 'NONE',  ( 0.000000000000000000, -26.08949754953044220, 27.05870788708222818 ) ) ;
#35543=EDGE_CURVE ( 'NONE', #1166, #52158, #34979, .T. ) ;
#35564=ORIENTED_EDGE ( 'NONE', *, *, #49964, .F. ) ;
#35574=CYLINDRICAL_SURFACE ( 'NONE', #40272, 37.49900000000000233 ) ;
#35587=ORIENTED_EDGE ( 'NONE', *, *, #43238, .F. ) ;
#35630=CARTESIAN_POINT ( 'NONE',  ( 10.00000000000000000, 0.000000000000000000, 0.000000000000000000 ) ) ;
#35631=DIRECTION ( 'NONE',  ( 0.000000000000000000, 0.000000000000000000, 1.000000000000000000 ) ) ;
#35656=EDGE_CURVE ( 'NONE', #51075, #14449, #32600, .T. ) ;
#35684=CARTESIAN_POINT ( 'NONE',  ( 0.000000000000000000, 12.24744871391589207, -2.499999999999994671 ) ) ;
#35692=ORIENTED_EDGE ( 'NONE', *, *, #41952, .T. ) ;
#35708=CYLINDRICAL_SURFACE ( 'NONE', #42257, 37.49900000000000233 ) ;
#35730=CYLINDRICAL_SURFACE ( 'NONE', #17723, 42.00000000000000000 ) ;
#35738=FACE_OUTER_BOUND ( 'NONE', #62314, .T. ) ;
#35740=DIRECTION ( 'NONE',  ( -1.000000000000000000, -0.000000000000000000, 0.000000000000000000 ) ) ;
#35759=ORIENTED_EDGE ( 'NONE', *, *, #34150, .T. ) ;
#35763=AXIS2_PLACEMENT_3D ( 'NONE', #5921, #27332, #73202 ) ;
#35770=ORIENTED_EDGE ( 'NONE', *, *, #29348, .F. ) ;
#35778=CARTESIAN_POINT ( 'NONE',  ( 10.00000000000000000, 10.74501242461282757, 35.92658777277515014 ) ) ;
#35780=DIRECTION ( 'NONE',  ( 1.000000000000000000, 0.000000000000000000, 0.000000000000000000 ) ) ;
#35785=FACE_OUTER_BOUND ( 'NONE', #31978, .T. ) ;
#35797=DIRECTION ( 'NONE',  ( -1.000000000000000000, 0.000000000000000000, 0.000000000000000000 ) ) ;
#35806=AXIS2_PLACEMENT_3D ( 'NONE', #12881, #29801, #41468 ) ;
#35814=CYLINDRICAL_SURFACE ( 'NONE', #56593, 37.49900000000000233 ) ;
#35820=DIRECTION ( 'NONE',  ( 0.000000000000000000, 0.4539904997395414754, 0.8910065241883706744 ) ) ;
#35824=DIRECTION ( 'NONE',  ( -1.000000000000000000, 0.000000000000000000, 0.000000000000000000 ) ) ;
#35828=EDGE_CURVE ( 'NONE', #2059, #19149, #63805, .T. ) ;
#35829=CARTESIAN_POINT ( 'NONE',  ( 10.00000000000000000, -0.8828120875898013420, -37.48860685352291711 ) ) ;
#35838=CARTESIAN_POINT ( 'NONE',  ( 0.000000000000000000, 0.000000000000000000, 0.000000000000000000 ) ) ;
#35863=VECTOR ( 'NONE', #46003, 1000.000000000000000 ) ;
#35879=CARTESIAN_POINT ( 'NONE',  ( 10.00000000000000000, 37.01155633439068282, -6.555932627142014191 ) ) ;
#35937=CIRCLE ( 'NONE', #21491, 37.49900000000000944 ) ;
#35942=ORIENTED_EDGE ( 'NONE', *, *, #22883, .F. ) ;
#35944=CARTESIAN_POINT ( 'NONE',  ( 10.00000000000000000, 26.08949754953024325, 27.05870788708241648 ) ) ;
#35966=AXIS2_PLACEMENT_3D ( 'NONE', #10305, #16691, #38879 ) ;
#35982=DIRECTION ( 'NONE',  ( -1.000000000000000000, 0.000000000000000000, 0.000000000000000000 ) ) ;
#35988=CIRCLE ( 'NONE', #32385, 16.00000000000000355 ) ;
#36037=CIRCLE ( 'NONE', #12001, 16.00000000000000000 ) ;
#36055=DIRECTION ( 'NONE',  ( -1.000000000000000000, 0.000000000000000000, -0.000000000000000000 ) ) ;
#36063=DIRECTION ( 'NONE',  ( 0.000000000000000000, 0.000000000000000000, -1.000000000000000000 ) ) ;
#36068=ORIENTED_EDGE ( 'NONE', *, *, #62145, .F. ) ;
#36076=ORIENTED_EDGE ( 'NONE', *, *, #70842, .T. ) ;
#36078=EDGE_CURVE ( 'NONE', #63015, #61302, #28722, .T. ) ;
#36085=ORIENTED_EDGE ( 'NONE', *, *, #66207, .T. ) ;
#36104=AXIS2_PLACEMENT_3D ( 'NONE', #52029, #62977, #45682 ) ;
#36126=ORIENTED_EDGE ( 'NONE', *, *, #11058, .F. ) ;
#36135=AXIS2_PLACEMENT_3D ( 'NONE', #16883, #23627, #36747 ) ;
#36158=ORIENTED_EDGE ( 'NONE', *, *, #45785, .T. ) ;
#36165=DIRECTION ( 'NONE',  ( -1.000000000000000000, -0.000000000000000000, -0.000000000000000000 ) ) ;
#36185=LINE ( 'NONE', #29065, #46845 ) ;
#36197=CARTESIAN_POINT ( 'NONE',  ( 10.00000000000000000, -36.88895765772628010, -6.736453364083947015 ) ) ;
#36199=VERTEX_POINT ( 'NONE', #46770 ) ;
#36208=CYLINDRICAL_SURFACE ( 'NONE', #56957, 42.00000000000000000 ) ;
#36216=CARTESIAN_POINT ( 'NONE',  ( 10.00000000000000000, -33.17418723428294669, -17.67226234102862747 ) ) ;
#36224=EDGE_CURVE ( 'NONE', #14549, #44827, #30242, .T. ) ;
#36228=CIRCLE ( 'NONE', #14653, 16.00000000000000000 ) ;
#36231=ORIENTED_EDGE ( 'NONE', *, *, #69124, .T. ) ;
#36236=ORIENTED_EDGE ( 'NONE', *, *, #56990, .T. ) ;
#36237=CIRCLE ( 'NONE', #18271, 42.00000000000000000 ) ;
#36255=CARTESIAN_POINT ( 'NONE',  ( 10.00000000000000000, 27.13269053701132094, -25.88420570971372570 ) ) ;
#36269=CARTESIAN_POINT ( 'NONE',  ( 0.000000000000000000, 21.40280677340371795, 36.13751322684426270 ) ) ;
#36271=LINE ( 'NONE', #8449, #19437 ) ;
#36273=ORIENTED_EDGE ( 'NONE', *, *, #2942, .T. ) ;
#36281=CARTESIAN_POINT ( 'NONE',  ( 10.00000000000000000, -41.91543099594819921, 2.663952781846001816 ) ) ;
#36300=DIRECTION ( 'NONE',  ( -1.000000000000000000, 0.000000000000000000, -0.000000000000000000 ) ) ;
#36301=VERTEX_POINT ( 'NONE', #66642 ) ;
#36310=EDGE_CURVE ( 'NONE', #63369, #73482, #49697, .T. ) ;
#36325=ADVANCED_FACE ( 'NONE', ( #9118 ), #54618, .T. ) ;
#36345=EDGE_CURVE ( 'NONE', #46234, #305, #57376, .T. ) ;
#36346=ORIENTED_EDGE ( 'NONE', *, *, #49798, .T. ) ;
#36395=CIRCLE ( 'NONE', #4023, 37.49900000000000233 ) ;
#36416=CARTESIAN_POINT ( 'NONE',  ( 10.00000000000000000, -21.40280677340398441, 36.13751322684410638 ) ) ;
#36417=SURFACE_STYLE_FILL_AREA ( #7119 ) ;
#36429=VERTEX_POINT ( 'NONE', #68871 ) ;
#36437=VERTEX_POINT ( 'NONE', #39932 ) ;
#36455=DIRECTION ( 'NONE',  ( 0.000000000000000000, 0.000000000000000000, 1.000000000000000000 ) ) ;
#36465=CYLINDRICAL_SURFACE ( 'NONE', #6843, 37.49900000000000233 ) ;
#36485=DIRECTION ( 'NONE',  ( -1.000000000000000000, -0.000000000000000000, 0.000000000000000000 ) ) ;
#36490=DIRECTION ( 'NONE',  ( 1.000000000000000000, -0.000000000000000000, -0.000000000000000000 ) ) ;
#36492=ORIENTED_EDGE ( 'NONE', *, *, #20394, .F. ) ;
#36498=CARTESIAN_POINT ( 'NONE',  ( 10.00000000000000000, 26.79245525562761188, -32.34446384429941901 ) ) ;
#36503=ADVANCED_FACE ( 'NONE', ( #63235 ), #45200, .T. ) ;
#36509=DIRECTION ( 'NONE',  ( -1.000000000000000000, 0.000000000000000000, 0.000000000000000000 ) ) ;
#36520=VECTOR ( 'NONE', #57259, 1000.000000000000000 ) ;
#36541=CARTESIAN_POINT ( 'NONE',  ( 0.000000000000000000, -37.58145647212455032, 0.6853352020789044152 ) ) ;
#36546=CARTESIAN_POINT ( 'NONE',  ( 10.00000000000000000, -33.80338159004273280, -16.23288003029533044 ) ) ;
#36550=DIRECTION ( 'NONE',  ( 0.000000000000000000, 0.5877852522924741363, -0.8090169943749465631 ) ) ;
#36557=AXIS2_PLACEMENT_3D ( 'NONE', #6308, #29211, #64550 ) ;
#36580=ORIENTED_EDGE ( 'NONE', *, *, #27466, .F. ) ;
#36582=DIRECTION ( 'NONE',  ( 0.000000000000000000, -8.881784197001252323E-16, 1.000000000000000000 ) ) ;
#36596=CYLINDRICAL_SURFACE ( 'NONE', #8189, 37.49900000000000233 ) ;
#36597=EDGE_CURVE ( 'NONE', #43117, #52875, #3399, .T. ) ;
#36613=VERTEX_POINT ( 'NONE', #64705 ) ;
#36630=ORIENTED_EDGE ( 'NONE', *, *, #44194, .F. ) ;
#36647=CARTESIAN_POINT ( 'NONE',  ( 50.00005079999999680, 0.000000000000000000, 0.000000000000000000 ) ) ;
#36649=EDGE_CURVE ( 'NONE', #31828, #73312, #39389, .T. ) ;
#36650=CYLINDRICAL_SURFACE ( 'NONE', #60370, 12.50000000000000000 ) ;
#36657=CIRCLE ( 'NONE', #12661, 42.00000000000000000 ) ;
#36664=DIRECTION ( 'NONE',  ( 0.000000000000000000, 0.000000000000000000, 1.000000000000000000 ) ) ;
#36677=CIRCLE ( 'NONE', #64332, 16.00000000000000000 ) ;
#36688=DIRECTION ( 'NONE',  ( -1.000000000000000000, -0.000000000000000000, -0.000000000000000000 ) ) ;
#36702=ORIENTED_EDGE ( 'NONE', *, *, #17479, .F. ) ;
#36703=ORIENTED_EDGE ( 'NONE', *, *, #66704, .F. ) ;
#36704=LINE ( 'NONE', #8130, #21399 ) ;
#36711=EDGE_CURVE ( 'NONE', #12130, #22476, #65454, .T. ) ;
#36727=CIRCLE ( 'NONE', #55939, 37.49900000000000233 ) ;
#36747=DIRECTION ( 'NONE',  ( 0.000000000000000000, 0.000000000000000000, 1.000000000000000000 ) ) ;
#36756=DIRECTION ( 'NONE',  ( -1.000000000000000000, -0.000000000000000000, -0.000000000000000000 ) ) ;
#36774=ORIENTED_EDGE ( 'NONE', *, *, #66560, .T. ) ;
#36792=CARTESIAN_POINT ( 'NONE',  ( 10.00000000000000000, 10.96151621346540317, -35.95386929396244113 ) ) ;
#36819=ORIENTED_EDGE ( 'NONE', *, *, #25985, .F. ) ;
#36822=ORIENTED_EDGE ( 'NONE', *, *, #54428, .F. ) ;
#36840=CYLINDRICAL_SURFACE ( 'NONE', #39850, 42.00000000000000000 ) ;
#36858=CYLINDRICAL_SURFACE ( 'NONE', #51563, 16.00000000000000000 ) ;
#36864=DIRECTION ( 'NONE',  ( -1.000000000000000000, -0.000000000000000000, -0.000000000000000000 ) ) ;
#36879=ORIENTED_EDGE ( 'NONE', *, *, #60469, .F. ) ;
#36891=EDGE_CURVE ( 'NONE', #35508, #19685, #32223, .T. ) ;
#36895=CARTESIAN_POINT ( 'NONE',  ( 0.000000000000000000, 27.75498641678742473, 31.52238457039609187 ) ) ;
#36897=ORIENTED_EDGE ( 'NONE', *, *, #29596, .F. ) ;
#36902=CYLINDRICAL_SURFACE ( 'NONE', #73761, 37.49900000000000233 ) ;
#36909=AXIS2_PLACEMENT_3D ( 'NONE', #44107, #56515, #21531 ) ;
#36918=DIRECTION ( 'NONE',  ( 0.000000000000000000, 0.000000000000000000, 1.000000000000000000 ) ) ;
#36927=DIRECTION ( 'NONE',  ( -1.000000000000000000, 0.000000000000000000, -0.000000000000000000 ) ) ;
#36936=ADVANCED_FACE ( 'NONE', ( #14109 ), #46580, .T. ) ;
#36944=VECTOR ( 'NONE', #68756, 1000.000000000000000 ) ;
#36954=CYLINDRICAL_SURFACE ( 'NONE', #40657, 16.00000000000000000 ) ;
#36961=CIRCLE ( 'NONE', #4565, 15.99999999999999822 ) ;
#36978=ORIENTED_EDGE ( 'NONE', *, *, #1585, .T. ) ;
#36984=AXIS2_PLACEMENT_3D ( 'NONE', #41942, #7723, #64879 ) ;
#36988=ADVANCED_FACE ( 'NONE', ( #35301 ), #54356, .T. ) ;
#36999=DIRECTION ( 'NONE',  ( -1.000000000000000000, 0.000000000000000000, 0.000000000000000000 ) ) ;
#37017=ORIENTED_EDGE ( 'NONE', *, *, #39556, .F. ) ;
#37032=ORIENTED_EDGE ( 'NONE', *, *, #14459, .F. ) ;
#37056=VECTOR ( 'NONE', #42508, 1000.000000000000000 ) ;
#37067=FACE_OUTER_BOUND ( 'NONE', #67052, .T. ) ;
#37071=LINE ( 'NONE', #70899, #52016 ) ;
#37075=DIRECTION ( 'NONE',  ( 0.000000000000000000, 0.000000000000000000, 1.000000000000000000 ) ) ;
#37092=VERTEX_POINT ( 'NONE', #21609 ) ;
#37108=DIRECTION ( 'NONE',  ( 0.000000000000000000, 0.000000000000000000, 1.000000000000000000 ) ) ;
#37118=EDGE_CURVE ( 'NONE', #67395, #8860, #26132, .T. ) ;
#37153=DIRECTION ( 'NONE',  ( 1.000000000000000000, -0.000000000000000000, -0.000000000000000000 ) ) ;
#37165=EDGE_CURVE ( 'NONE', #24000, #62600, #23885, .T. ) ;
#37181=VECTOR ( 'NONE', #44491, 1000.000000000000000 ) ;
#37197=ORIENTED_EDGE ( 'NONE', *, *, #44073, .F. ) ;
#37200=ORIENTED_EDGE ( 'NONE', *, *, #17382, .T. ) ;
#37267=ORIENTED_EDGE ( 'NONE', *, *, #32334, .T. ) ;
#37272=CIRCLE ( 'NONE', #51655, 37.49900000000000944 ) ;
#37274=ORIENTED_EDGE ( 'NONE', *, *, #32909, .T. ) ;
#37277=VERTEX_POINT ( 'NONE', #11439 ) ;
#37279=ORIENTED_EDGE ( 'NONE', *, *, #64443, .F. ) ;
#37286=CIRCLE ( 'NONE', #50420, 42.00000000000000000 ) ;
#37289=LINE ( 'NONE', #70351, #13672 ) ;
#37305=ORIENTED_EDGE ( 'NONE', *, *, #39739, .T. ) ;
#37306=CARTESIAN_POINT ( 'NONE',  ( 0.000000000000000000, 33.80338159004307386, -16.23288003029461279 ) ) ;
#37317=CARTESIAN_POINT ( 'NONE',  ( 0.000000000000000000, 0.000000000000000000, 0.000000000000000000 ) ) ;
#37324=VERTEX_POINT ( 'NONE', #40771 ) ;
#37348=VECTOR ( 'NONE', #46945, 1000.000000000000000 ) ;
#37357=ORIENTED_EDGE ( 'NONE', *, *, #69450, .F. ) ;
#37359=LINE ( 'NONE', #19672, #12965 ) ;
#37368=VERTEX_POINT ( 'NONE', #35118 ) ;
#37370=LINE ( 'NONE', #60309, #2399 ) ;
#37373=ORIENTED_EDGE ( 'NONE', *, *, #43722, .F. ) ;
#37380=ORIENTED_EDGE ( 'NONE', *, *, #57036, .T. ) ;
#37382=CARTESIAN_POINT ( 'NONE',  ( 10.00000000000000000, -37.22597642581153821, -5.202137450156795850 ) ) ;
#37399=DIRECTION ( 'NONE',  ( 0.000000000000000000, 0.8910065241883688980, -0.4539904997395445840 ) ) ;
#37411=AXIS2_PLACEMENT_3D ( 'NONE', #21688, #49518, #16055 ) ;
#37413=DIRECTION ( 'NONE',  ( 0.000000000000000000, 0.000000000000000000, 1.000000000000000000 ) ) ;
#37414=CARTESIAN_POINT ( 'NONE',  ( 0.000000000000000000, -37.22597642581153821, 10.79786254984320415 ) ) ;
#37421=DIRECTION ( 'NONE',  ( 0.000000000000000000, 0.8090169943749445647, 0.5877852522924771339 ) ) ;
#37438=ADVANCED_FACE ( 'NONE', ( #7658 ), #19666, .T. ) ;
#37439=FACE_OUTER_BOUND ( 'NONE', #51799, .T. ) ;
#37442=EDGE_CURVE ( 'NONE', #16864, #24357, #736, .T. ) ;
#37446=ORIENTED_EDGE ( 'NONE', *, *, #20110, .T. ) ;
#37454=EDGE_CURVE ( 'NONE', #37974, #57971, #2058, .T. ) ;
#37459=DIRECTION ( 'NONE',  ( -1.000000000000000000, -0.000000000000000000, -0.000000000000000000 ) ) ;
#37473=DIRECTION ( 'NONE',  ( 0.000000000000000000, 1.000000000000000000, 3.469446951953614189E-15 ) ) ;
#37482=DIRECTION ( 'NONE',  ( -1.000000000000000000, 0.000000000000000000, 0.000000000000000000 ) ) ;
#37523=EDGE_CURVE ( 'NONE', #23039, #65417, #24669, .T. ) ;
#37524=DIRECTION ( 'NONE',  ( 1.000000000000000000, 0.000000000000000000, 0.000000000000000000 ) ) ;
#37546=ORIENTED_EDGE ( 'NONE', *, *, #71173, .T. ) ;
#37552=ADVANCED_FACE ( 'NONE', ( #66652 ), #15132, .T. ) ;
#37558=VERTEX_POINT ( 'NONE', #21506 ) ;
#37560=CARTESIAN_POINT ( 'NONE',  ( 10.00000000000000000, -16.65560815589439159, 38.55633173627004595 ) ) ;
#37579=CARTESIAN_POINT ( 'NONE',  ( 10.00000000000000000, 21.53537804866081373, 30.80686688397018358 ) ) ;
#37605=UNCERTAINTY_MEASURE_WITH_UNIT (LENGTH_MEASURE( 1.000000000000000082E-05 ), #34955, 'distance_accuracy_value', 'NONE');
#37615=EDGE_CURVE ( 'NONE', #26264, #5742, #22324, .T. ) ;
#37625=VERTEX_POINT ( 'NONE', #10989 ) ;
#37645=VERTEX_POINT ( 'NONE', #23021 ) ;
#37650=AXIS2_PLACEMENT_3D ( 'NONE', #14557, #48769, #31102 ) ;
#37666=VERTEX_POINT ( 'NONE', #23385 ) ;
#37673=CARTESIAN_POINT ( 'NONE',  ( 0.000000000000000000, 33.79645857604513992, 16.45098606841138178 ) ) ;
#37677=CARTESIAN_POINT ( 'NONE',  ( 0.000000000000000000, -35.53030884539094103, 12.26510123303246935 ) ) ;
#37698=DIRECTION ( 'NONE',  ( 0.000000000000000000, 0.000000000000000000, 1.000000000000000000 ) ) ;
#37707=CARTESIAN_POINT ( 'NONE',  ( 10.00000000000000000, -0.6853352020787742971, -37.58145647212455032 ) ) ;
#37715=CIRCLE ( 'NONE', #61692, 16.00000000000000000 ) ;
#37746=CARTESIAN_POINT ( 'NONE',  ( 10.00000000000000000, 0.000000000000000000, 0.000000000000000000 ) ) ;
#37753=EDGE_LOOP ( 'NONE', ( #13403, #56018, #18885, #43282 ) ) ;
#37773=CIRCLE ( 'NONE', #1788, 42.00000000000000000 ) ;
#37779=FACE_OUTER_BOUND ( 'NONE', #52145, .T. ) ;
#37795=ADVANCED_FACE ( 'NONE', ( #52684 ), #47060, .T. ) ;
#37807=ORIENTED_EDGE ( 'NONE', *, *, #46423, .T. ) ;
#37831=DIRECTION ( 'NONE',  ( 1.000000000000000000, 0.000000000000000000, 0.000000000000000000 ) ) ;
#37837=DIRECTION ( 'NONE',  ( 0.000000000000000000, 1.000000000000000000, 3.469446951953614189E-15 ) ) ;
#37841=CYLINDRICAL_SURFACE ( 'NONE', #59024, 16.00000000000000000 ) ;
#37846=CARTESIAN_POINT ( 'NONE',  ( 0.000000000000000000, -37.22597642581161637, 5.202137450156258502 ) ) ;
#37869=DIRECTION ( 'NONE',  ( 0.000000000000000000, 0.9510565162951544194, -0.3090169943749447867 ) ) ;
#37878=CARTESIAN_POINT ( 'NONE',  ( 0.000000000000000000, 0.000000000000000000, 0.000000000000000000 ) ) ;
#37896=CARTESIAN_POINT ( 'NONE',  ( 0.000000000000000000, 0.000000000000000000, 0.000000000000000000 ) ) ;
#37897=DIRECTION ( 'NONE',  ( 0.000000000000000000, 0.000000000000000000, -1.000000000000000000 ) ) ;
#37900=ORIENTED_EDGE ( 'NONE', *, *, #60951, .T. ) ;
#37921=CARTESIAN_POINT ( 'NONE',  ( 0.000000000000000000, 0.000000000000000000, 0.000000000000000000 ) ) ;
#37922=CARTESIAN_POINT ( 'NONE',  ( 10.00000000000000000, 4.992566952384984269, 37.16516213103279398 ) ) ;
#37944=EDGE_CURVE ( 'NONE', #72597, #43377, #15115, .T. ) ;
#37974=VERTEX_POINT ( 'NONE', #9783 ) ;
#37979=AXIS2_PLACEMENT_3D ( 'NONE', #72907, #36864, #66200 ) ;
#37981=ORIENTED_EDGE ( 'NONE', *, *, #63413, .T. ) ;
#37982=LINE ( 'NONE', #4158, #13116 ) ;
#37989=VERTEX_POINT ( 'NONE', #55641 ) ;
#37995=VERTEX_POINT ( 'NONE', #4160 ) ;
#38009=ORIENTED_EDGE ( 'NONE', *, *, #64429, .F. ) ;
#38022=EDGE_LOOP ( 'NONE', ( #20890, #49713, #61782, #56444 ) ) ;
#38034=LINE ( 'NONE', #32381, #54718 ) ;
#38041=EDGE_CURVE ( 'NONE', #24429, #63558, #42812, .T. ) ;
#38058=AXIS2_PLACEMENT_3D ( 'NONE', #3753, #26655, #38317 ) ;
#38085=VERTEX_POINT ( 'NONE', #4533 ) ;
#38093=CARTESIAN_POINT ( 'NONE',  ( 10.00000000000000000, 37.22597642581150268, 5.202137450157037435 ) ) ;
#38161=ORIENTED_EDGE ( 'NONE', *, *, #37615, .F. ) ;
#38163=DIRECTION ( 'NONE',  ( -1.000000000000000000, 0.000000000000000000, 0.000000000000000000 ) ) ;
#38179=CARTESIAN_POINT ( 'NONE',  ( 0.000000000000000000, 26.08949754953024325, 27.05870788708241648 ) ) ;
#38194=DIRECTION ( 'NONE',  ( -1.000000000000000000, 0.000000000000000000, 0.000000000000000000 ) ) ;
#38195=CIRCLE ( 'NONE', #28582, 16.00000000000000000 ) ;
#38199=DIRECTION ( 'NONE',  ( -1.000000000000000000, 0.000000000000000000, 0.000000000000000000 ) ) ;
#38225=CIRCLE ( 'NONE', #34567, 37.49900000000001654 ) ;
#38232=CIRCLE ( 'NONE', #33388, 16.00000000000000000 ) ;
#38253=CARTESIAN_POINT ( 'NONE',  ( 10.00000000000000000, 0.000000000000000000, 0.000000000000000000 ) ) ;
#38301=EDGE_CURVE ( 'NONE', #70504, #66872, #16416, .T. ) ;
#38317=DIRECTION ( 'NONE',  ( 0.000000000000000000, 0.000000000000000000, 1.000000000000000000 ) ) ;
#38318=CYLINDRICAL_SURFACE ( 'NONE', #29728, 42.00000000000000000 ) ;
#38334=CIRCLE ( 'NONE', #71908, 16.00000000000000000 ) ;
#38337=FACE_OUTER_BOUND ( 'NONE', #4650, .T. ) ;
#38338=VECTOR ( 'NONE', #63873, 1000.000000000000000 ) ;
#38348=AXIS2_PLACEMENT_3D ( 'NONE', #8438, #36999, #8798 ) ;
#38359=ORIENTED_EDGE ( 'NONE', *, *, #20009, .T. ) ;
#38379=CARTESIAN_POINT ( 'NONE',  ( 0.000000000000000000, -15.48615015657556171, -39.04073710021360455 ) ) ;
#38385=VERTEX_POINT ( 'NONE', #14586 ) ;
#38423=ORIENTED_EDGE ( 'NONE', *, *, #37454, .T. ) ;
#38424=CARTESIAN_POINT ( 'NONE',  ( 10.00000000000000000, 22.48208911017500355, 35.47612816024531668 ) ) ;
#38425=DIRECTION ( 'NONE',  ( -1.000000000000000000, 0.000000000000000000, 0.000000000000000000 ) ) ;
#38436=DIRECTION ( 'NONE',  ( -1.000000000000000000, 0.000000000000000000, 0.000000000000000000 ) ) ;
#38449=EDGE_CURVE ( 'NONE', #63015, #57727, #72834, .T. ) ;
#38455=ORIENTED_EDGE ( 'NONE', *, *, #34614, .F. ) ;
#38459=VERTEX_POINT ( 'NONE', #57052 ) ;
#38483=DIRECTION ( 'NONE',  ( 0.000000000000000000, -0.9510565162951500895, -0.3090169943749583314 ) ) ;
#38486=DIRECTION ( 'NONE',  ( 0.000000000000000000, -0.5877852522924802425, 0.8090169943749422332 ) ) ;
#38509=LINE ( 'NONE', #27594, #47154 ) ;
#38523=EDGE_CURVE ( 'NONE', #16853, #26601, #38644, .T. ) ;
#38541=CARTESIAN_POINT ( 'NONE',  ( 0.000000000000000000, 0.000000000000000000, 0.000000000000000000 ) ) ;
#38543=EDGE_CURVE ( 'NONE', #52056, #14449, #34473, .T. ) ;
#38556=CARTESIAN_POINT ( 'NONE',  ( 0.000000000000000000, -27.75498641678720446, -31.52238457039628727 ) ) ;
#38559=ADVANCED_FACE ( 'NONE', ( #69426 ), #318, .T. ) ;
#38575=DIRECTION ( 'NONE',  ( -1.000000000000000000, -0.000000000000000000, -0.000000000000000000 ) ) ;
#38589=FACE_OUTER_BOUND ( 'NONE', #63715, .T. ) ;
#38597=PRODUCT_DEFINITION_SHAPE ( 'NONE', 'NONE',  #8124 ) ;
#38602=EDGE_LOOP ( 'NONE', ( #8876, #45930, #59171, #13577 ) ) ;
#38610=CARTESIAN_POINT ( 'NONE',  ( 10.00000000000000000, 35.53030884539102630, -12.26510123303222599 ) ) ;
#38617=LINE ( 'NONE', #56281, #17237 ) ;
#38633=VERTEX_POINT ( 'NONE', #19027 ) ;
#38644=LINE ( 'NONE', #17192, #62091 ) ;
#38666=CARTESIAN_POINT ( 'NONE',  ( 0.000000000000000000, -36.88895765772628010, -6.736453364083947015 ) ) ;
#38667=ORIENTED_EDGE ( 'NONE', *, *, #15215, .F. ) ;
#38695=LINE ( 'NONE', #27022, #45071 ) ;
#38700=DIRECTION ( 'NONE',  ( 0.000000000000000000, 0.000000000000000000, 1.000000000000000000 ) ) ;
#38705=DIRECTION ( 'NONE',  ( 1.000000000000000000, 0.000000000000000000, 0.000000000000000000 ) ) ;
#38724=AXIS2_PLACEMENT_3D ( 'NONE', #71262, #13396, #54366 ) ;
#38725=ADVANCED_FACE ( 'NONE', ( #14497 ), #60019, .T. ) ;
#38733=EDGE_LOOP ( 'NONE', ( #22637, #72630, #67528, #48623 ) ) ;
#38740=LINE ( 'NONE', #49266, #2283 ) ;
#38761=ORIENTED_EDGE ( 'NONE', *, *, #17060, .T. ) ;
#38767=AXIS2_PLACEMENT_3D ( 'NONE', #68655, #39712, #52084 ) ;
#38781=ORIENTED_EDGE ( 'NONE', *, *, #61604, .F. ) ;
#38829=CIRCLE ( 'NONE', #20848, 37.49900000000000233 ) ;
#38874=ORIENTED_EDGE ( 'NONE', *, *, #4790, .F. ) ;
#38877=CARTESIAN_POINT ( 'NONE',  ( 10.00000000000000000, -21.53537804866103045, 30.80686688397002371 ) ) ;
#38879=DIRECTION ( 'NONE',  ( 0.000000000000000000, -0.8090169943749403458, -0.5877852522924830181 ) ) ;
#38884=ADVANCED_FACE ( 'NONE', ( #34665 ), #61119, .T. ) ;
#38897=EDGE_CURVE ( 'NONE', #16169, #25977, #29021, .T. ) ;
#38929=AXIS2_PLACEMENT_3D ( 'NONE', #3877, #21130, #44082 ) ;
#38957=CARTESIAN_POINT ( 'NONE',  ( 0.000000000000000000, 12.42422080174688404, -35.38097989696498047 ) ) ;
#38959=EDGE_CURVE ( 'NONE', #54442, #9139, #56119, .T. ) ;
#38967=VERTEX_POINT ( 'NONE', #142 ) ;
#38978=ORIENTED_EDGE ( 'NONE', *, *, #12730, .T. ) ;
#38982=DIRECTION ( 'NONE',  ( -1.000000000000000000, 0.000000000000000000, 0.000000000000000000 ) ) ;
#38985=CARTESIAN_POINT ( 'NONE',  ( 0.000000000000000000, 0.000000000000000000, 0.000000000000000000 ) ) ;
#39006=DIRECTION ( 'NONE',  ( 0.000000000000000000, 0.5877852522924685852, 0.8090169943749508930 ) ) ;
#39021=ORIENTED_EDGE ( 'NONE', *, *, #10682, .T. ) ;
#39026=EDGE_CURVE ( 'NONE', #39661, #6755, #15326, .T. ) ;
#39039=VECTOR ( 'NONE', #4633, 1000.000000000000000 ) ;
#39047=DIRECTION ( 'NONE',  ( 0.000000000000000000, -0.9510565162951565288, 0.3090169943749382364 ) ) ;
#39064=DIRECTION ( 'NONE',  ( 0.000000000000000000, 0.7071067811865486830, -0.7071067811865463515 ) ) ;
#39084=CARTESIAN_POINT ( 'NONE',  ( 0.000000000000000000, 0.000000000000000000, 0.000000000000000000 ) ) ;
#39086=DIRECTION ( 'NONE',  ( 0.000000000000000000, 0.000000000000000000, 1.000000000000000000 ) ) ;
#39088=CARTESIAN_POINT ( 'NONE',  ( 10.00000000000000000, 33.79645857604513992, -16.45098606841138178 ) ) ;
#39092=CARTESIAN_POINT ( 'NONE',  ( 10.00000000000000000, 0.9569279952884607310, 2.500000000000015543 ) ) ;
#39113=VECTOR ( 'NONE', #18196, 1000.000000000000000 ) ;
#39116=ADVANCED_FACE ( 'NONE', ( #49542 ), #67212, .T. ) ;
#39120=ADVANCED_FACE ( 'NONE', ( #4448 ), #74336, .T. ) ;
#39123=ORIENTED_EDGE ( 'NONE', *, *, #667, .T. ) ;
#39133=ORIENTED_EDGE ( 'NONE', *, *, #30702, .T. ) ;
#39136=FACE_OUTER_BOUND ( 'NONE', #69774, .T. ) ;
#39139=ADVANCED_FACE ( 'NONE', ( #68337 ), #323, .T. ) ;
#39167=ORIENTED_EDGE ( 'NONE', *, *, #63814, .T. ) ;
#39187=ORIENTED_EDGE ( 'NONE', *, *, #62686, .T. ) ;
#39190=ORIENTED_EDGE ( 'NONE', *, *, #13826, .F. ) ;
#39192=CARTESIAN_POINT ( 'NONE',  ( 0.000000000000000000, 39.04073710021366139, -15.48615015657542315 ) ) ;
#39209=CYLINDRICAL_SURFACE ( 'NONE', #52771, 16.00000000000000000 ) ;
#39215=CARTESIAN_POINT ( 'NONE',  ( 10.00000000000000000, 36.88895765772642932, -6.736453364083163642 ) ) ;
#39220=ORIENTED_EDGE ( 'NONE', *, *, #9761, .F. ) ;
#39229=CARTESIAN_POINT ( 'NONE',  ( 10.00000000000000000, -37.16516213103273714, -4.992566952385376844 ) ) ;
#39257=DIRECTION ( 'NONE',  ( 0.000000000000000000, 0.000000000000000000, -1.000000000000000000 ) ) ;
#39294=ORIENTED_EDGE ( 'NONE', *, *, #23276, .T. ) ;
#39298=EDGE_CURVE ( 'NONE', #57179, #10428, #18973, .T. ) ;
#39334=ORIENTED_EDGE ( 'NONE', *, *, #8387, .F. ) ;
#39342=ORIENTED_EDGE ( 'NONE', *, *, #26552, .F. ) ;
#39389=CIRCLE ( 'NONE', #6971, 42.00000000000000000 ) ;
#39405=VERTEX_POINT ( 'NONE', #41984 ) ;
#39446=DIRECTION ( 'NONE',  ( -1.000000000000000000, 0.000000000000000000, -0.000000000000000000 ) ) ;
#39457=LINE ( 'NONE', #62400, #70806 ) ;
#39458=ADVANCED_FACE ( 'NONE', ( #29197 ), #46886, .T. ) ;
#39460=DIRECTION ( 'NONE',  ( -1.000000000000000000, 0.000000000000000000, 0.000000000000000000 ) ) ;
#39472=CARTESIAN_POINT ( 'NONE',  ( 5.000000000000000000, 31.52238457039637609, -27.75498641678709788 ) ) ;
#39485=VECTOR ( 'NONE', #63297, 1000.000000000000000 ) ;
#39488=CYLINDRICAL_SURFACE ( 'NONE', #13075, 37.49900000000000233 ) ;
#39492=AXIS2_PLACEMENT_3D ( 'NONE', #65749, #21342, #31896 ) ;
#39532=DIRECTION ( 'NONE',  ( -1.000000000000000000, 0.000000000000000000, 0.000000000000000000 ) ) ;
#39535=FACE_OUTER_BOUND ( 'NONE', #64436, .T. ) ;
#39536=CARTESIAN_POINT ( 'NONE',  ( 0.000000000000000000, 32.34446384429971033, 26.79245525562726371 ) ) ;
#39539=EDGE_CURVE ( 'NONE', #1166, #66590, #70902, .T. ) ;
#39556=EDGE_CURVE ( 'NONE', #49804, #26693, #10546, .T. ) ;
#39566=DIRECTION ( 'NONE',  ( 0.000000000000000000, 0.000000000000000000, 1.000000000000000000 ) ) ;
#39577=VECTOR ( 'NONE', #63427, 1000.000000000000000 ) ;
#39582=ADVANCED_FACE ( 'NONE', ( #59639 ), #48350, .T. ) ;
#39589=ORIENTED_EDGE ( 'NONE', *, *, #27391, .F. ) ;
#39604=CIRCLE ( 'NONE', #13186, 16.00000000000000355 ) ;
#39613=CARTESIAN_POINT ( 'NONE',  ( 10.00000000000000000, -40.98264845739743834, -9.188173127307738497 ) ) ;
#39630=DIRECTION ( 'NONE',  ( 0.000000000000000000, 0.000000000000000000, -1.000000000000000000 ) ) ;
#39639=EDGE_CURVE ( 'NONE', #52892, #21663, #40561, .T. ) ;
#39661=VERTEX_POINT ( 'NONE', #33650 ) ;
#39687=ORIENTED_EDGE ( 'NONE', *, *, #44035, .T. ) ;
#39692=LINE ( 'NONE', #56614, #11033 ) ;
#39699=ORIENTED_EDGE ( 'NONE', *, *, #8159, .T. ) ;
#39712=DIRECTION ( 'NONE',  ( -1.000000000000000000, -0.000000000000000000, 0.000000000000000000 ) ) ;
#39716=AXIS2_PLACEMENT_3D ( 'NONE', #42472, #48835, #48105 ) ;
#39733=CARTESIAN_POINT ( 'NONE',  ( 10.00000000000000000, -21.53537804866058991, -30.80686688397033635 ) ) ;
#39739=EDGE_CURVE ( 'NONE', #44128, #44780, #9415, .T. ) ;
#39754=DIRECTION ( 'NONE',  ( -1.000000000000000000, 0.000000000000000000, -0.000000000000000000 ) ) ;
#39757=ADVANCED_FACE ( 'NONE', ( #64367 ), #70341, .T. ) ;
#39767=DIRECTION ( 'NONE',  ( 0.000000000000000000, 0.000000000000000000, 1.000000000000000000 ) ) ;
#39792=FACE_OUTER_BOUND ( 'NONE', #33502, .T. ) ;
#39799=EDGE_LOOP ( 'NONE', ( #60866, #11262, #27152, #14540 ) ) ;
#39803=DIRECTION ( 'NONE',  ( 0.000000000000000000, 0.000000000000000000, 1.000000000000000000 ) ) ;
#39812=CARTESIAN_POINT ( 'NONE',  ( 10.00000000000000000, 0.8828120875900632436, 37.48860685352291000 ) ) ;
#39822=DIRECTION ( 'NONE',  ( -1.000000000000000000, -0.000000000000000000, -0.000000000000000000 ) ) ;
#39850=AXIS2_PLACEMENT_3D ( 'NONE', #59415, #41744, #20286 ) ;
#39851=ORIENTED_EDGE ( 'NONE', *, *, #1060, .F. ) ;
#39862=DIRECTION ( 'NONE',  ( -1.000000000000000000, -0.000000000000000000, -0.000000000000000000 ) ) ;
#39899=CYLINDRICAL_SURFACE ( 'NONE', #32105, 37.49900000000000233 ) ;
#39911=VECTOR ( 'NONE', #44333, 1000.000000000000000 ) ;
#39913=CYLINDRICAL_SURFACE ( 'NONE', #69467, 37.49900000000000233 ) ;
#39919=CIRCLE ( 'NONE', #31470, 42.00000000000000000 ) ;
#39932=CARTESIAN_POINT ( 'NONE',  ( 10.00000000000000000, 4.992566952385523393, -37.16516213103272293 ) ) ;
#39938=ORIENTED_EDGE ( 'NONE', *, *, #19583, .T. ) ;
#39943=VERTEX_POINT ( 'NONE', #72566 ) ;
#39951=ORIENTED_EDGE ( 'NONE', *, *, #64526, .T. ) ;
#39967=CARTESIAN_POINT ( 'NONE',  ( 0.000000000000000000, 0.000000000000000000, 0.000000000000000000 ) ) ;
#39981=CARTESIAN_POINT ( 'NONE',  ( 0.000000000000000000, 0.000000000000000000, 0.000000000000000000 ) ) ;
#39995=DIRECTION ( 'NONE',  ( 0.000000000000000000, 0.000000000000000000, 1.000000000000000000 ) ) ;
#39999=DIRECTION ( 'NONE',  ( -1.000000000000000000, -0.000000000000000000, -0.000000000000000000 ) ) ;
#40000=EDGE_CURVE ( 'NONE', #37989, #36437, #25038, .T. ) ;
#40023=AXIS2_PLACEMENT_3D ( 'NONE', #9470, #66982, #33136 ) ;
#40034=ORIENTED_EDGE ( 'NONE', *, *, #64282, .T. ) ;
#40050=DIRECTION ( 'NONE',  ( -1.000000000000000000, -0.000000000000000000, -0.000000000000000000 ) ) ;
#40057=EDGE_CURVE ( 'NONE', #66589, #24429, #33401, .T. ) ;
#40072=CARTESIAN_POINT ( 'NONE',  ( 5.000000000000000000, 41.91543099594818500, 2.663952781846291362 ) ) ;
#40092=DIRECTION ( 'NONE',  ( 0.000000000000000000, 0.3090169943749411230, 0.9510565162951555296 ) ) ;
#40096=CARTESIAN_POINT ( 'NONE',  ( 5.000000000000000000, 21.40280677340421889, -36.13751322684397138 ) ) ;
#40119=AXIS2_PLACEMENT_3D ( 'NONE', #26757, #38425, #21484 ) ;
#40128=DIRECTION ( 'NONE',  ( -1.000000000000000000, 0.000000000000000000, 0.000000000000000000 ) ) ;
#40170=CYLINDRICAL_SURFACE ( 'NONE', #7730, 37.49900000000000233 ) ;
#40233=ORIENTED_EDGE ( 'NONE', *, *, #29177, .F. ) ;
#40240=DIRECTION ( 'NONE',  ( 0.000000000000000000, 0.8090169943749486725, -0.5877852522924714718 ) ) ;
#40242=ORIENTED_EDGE ( 'NONE', *, *, #49916, .T. ) ;
#40247=DIRECTION ( 'NONE',  ( -1.000000000000000000, 0.000000000000000000, 0.000000000000000000 ) ) ;
#40248=EDGE_CURVE ( 'NONE', #13679, #51673, #58692, .T. ) ;
#40253=VERTEX_POINT ( 'NONE', #53721 ) ;
#40272=AXIS2_PLACEMENT_3D ( 'NONE', #52131, #63803, #12273 ) ;
#40277=LINE ( 'NONE', #74109, #20895 ) ;
#40299=FACE_OUTER_BOUND ( 'NONE', #16354, .T. ) ;
#40304=VERTEX_POINT ( 'NONE', #64640 ) ;
#40319=AXIS2_PLACEMENT_3D ( 'NONE', #14444, #71579, #37399 ) ;
#40344=LINE ( 'NONE', #5775, #33533 ) ;
#40357=DIRECTION ( 'NONE',  ( -1.000000000000000000, -0.000000000000000000, 0.000000000000000000 ) ) ;
#40358=CYLINDRICAL_SURFACE ( 'NONE', #47774, 37.49900000000000233 ) ;
#40367=CARTESIAN_POINT ( 'NONE',  ( 10.00000000000000000, 0.000000000000000000, 0.000000000000000000 ) ) ;
#40376=DIRECTION ( 'NONE',  ( 0.000000000000000000, 0.000000000000000000, 1.000000000000000000 ) ) ;
#40381=AXIS2_PLACEMENT_3D ( 'NONE', #20902, #26164, #37837 ) ;
#40427=EDGE_CURVE ( 'NONE', #42621, #26528, #74314, .T. ) ;
#40472=ADVANCED_FACE ( 'NONE', ( #9332 ), #14979, .T. ) ;
#40477=DIRECTION ( 'NONE',  ( 0.000000000000000000, 0.000000000000000000, 1.000000000000000000 ) ) ;
#40488=DIRECTION ( 'NONE',  ( -1.000000000000000000, 0.000000000000000000, 0.000000000000000000 ) ) ;
#40493=EDGE_CURVE ( 'NONE', #73031, #73482, #59891, .T. ) ;
#40494=CARTESIAN_POINT ( 'NONE',  ( 0.000000000000000000, -16.45098606841149902, 33.79645857604508308 ) ) ;
#40510=ORIENTED_EDGE ( 'NONE', *, *, #32845, .F. ) ;
#40520=DIRECTION ( 'NONE',  ( -1.000000000000000000, -0.000000000000000000, 0.000000000000000000 ) ) ;
#40527=EDGE_LOOP ( 'NONE', ( #13067, #14779, #19517, #50771 ) ) ;
#40535=CARTESIAN_POINT ( 'NONE',  ( 10.00000000000000000, 33.17418723428333749, -17.67226234102790272 ) ) ;
#40547=CARTESIAN_POINT ( 'NONE',  ( 0.000000000000000000, 12.42422080174638310, 35.38097989696515810 ) ) ;
#40561=CIRCLE ( 'NONE', #46572, 16.00000000000000000 ) ;
#40569=DIRECTION ( 'NONE',  ( -1.000000000000000000, 0.000000000000000000, 0.000000000000000000 ) ) ;
#40572=DIRECTION ( 'NONE',  ( -1.000000000000000000, -0.000000000000000000, 0.000000000000000000 ) ) ;
#40593=EDGE_CURVE ( 'NONE', #14702, #44780, #62352, .T. ) ;
#40609=EDGE_CURVE ( 'NONE', #34470, #58261, #41963, .T. ) ;
#40654=DIRECTION ( 'NONE',  ( -1.000000000000000000, -0.000000000000000000, -0.000000000000000000 ) ) ;
#40657=AXIS2_PLACEMENT_3D ( 'NONE', #8388, #60277, #22257 ) ;
#40669=CARTESIAN_POINT ( 'NONE',  ( 10.00000000000000000, -27.75498641678764855, 31.52238457039589647 ) ) ;
#40673=DIRECTION ( 'NONE',  ( 1.000000000000000000, 0.000000000000000000, 0.000000000000000000 ) ) ;
#40680=VERTEX_POINT ( 'NONE', #73598 ) ;
#40697=AXIS2_PLACEMENT_3D ( 'NONE', #35401, #58330, #23389 ) ;
#40716=ORIENTED_EDGE ( 'NONE', *, *, #14459, .T. ) ;
#40724=CARTESIAN_POINT ( 'NONE',  ( 10.00000000000000000, 35.47612816024556537, -22.48208911017461631 ) ) ;
#40771=CARTESIAN_POINT ( 'NONE',  ( 10.00000000000000178, 0.000000000000000000, 12.50000000000000000 ) ) ;
#40780=VECTOR ( 'NONE', #13706, 1000.000000000000000 ) ;
#40788=ORIENTED_EDGE ( 'NONE', *, *, #2853, .T. ) ;
#40800=DIRECTION ( 'NONE',  ( 0.000000000000000000, -0.4539904997395540764, 0.8910065241883642351 ) ) ;
#40814=DIRECTION ( 'NONE',  ( -1.000000000000000000, 0.000000000000000000, 0.000000000000000000 ) ) ;
#40815=CIRCLE ( 'NONE', #32356, 37.49900000000000944 ) ;
#40839=CARTESIAN_POINT ( 'NONE',  ( 0.000000000000000000, 16.65560815589411092, 38.55633173627015253 ) ) ;
#40876=DIRECTION ( 'NONE',  ( 0.000000000000000000, 0.000000000000000000, -1.000000000000000000 ) ) ;
#40892=EDGE_CURVE ( 'NONE', #11760, #9413, #27506, .T. ) ;
#40914=DIRECTION ( 'NONE',  ( -1.000000000000000000, -0.000000000000000000, 0.000000000000000000 ) ) ;
#40927=VECTOR ( 'NONE', #52756, 1000.000000000000000 ) ;
#40935=CARTESIAN_POINT ( 'NONE',  ( 10.00000000000000000, -12.42422080174614862, -35.38097989696524337 ) ) ;
#40938=DIRECTION ( 'NONE',  ( 0.000000000000000000, -0.1564344650402170744, -0.9876883405951398798 ) ) ;
#40944=AXIS2_PLACEMENT_3D ( 'NONE', #50774, #50021, #55682 ) ;
#40949=ORIENTED_EDGE ( 'NONE', *, *, #34014, .T. ) ;
#40970=AXIS2_PLACEMENT_3D ( 'NONE', #31103, #24006, #70208 ) ;
#40973=PRESENTATION_STYLE_ASSIGNMENT (( #48081 ) ) ;
#40979=ORIENTED_EDGE ( 'NONE', *, *, #723, .F. ) ;
#40985=ORIENTED_EDGE ( 'NONE', *, *, #41310, .T. ) ;
#41014=DIRECTION ( 'NONE',  ( 0.000000000000000000, 0.000000000000000000, -1.000000000000000000 ) ) ;
#41025=CARTESIAN_POINT ( 'NONE',  ( 10.00000000000000000, 10.41901085202135668, -40.68715046381917944 ) ) ;
#41026=COLOUR_RGB ( '', 0.72549020, 0.75294118, 0.79215686) ;
#41030=CARTESIAN_POINT ( 'NONE',  ( 10.00000000000000000, -35.53030884539077050, -12.26510123303296851 ) ) ;
#41042=CARTESIAN_POINT ( 'NONE',  ( 10.00000000000000000, -27.13269053701114331, 25.88420570971391754 ) ) ;
#41052=CYLINDRICAL_SURFACE ( 'NONE', #44350, 42.00000000000000000 ) ;
#41054=CARTESIAN_POINT ( 'NONE',  ( 0.000000000000000000, -26.08949754953005495, -27.05870788708258701 ) ) ;
#41070=VERTEX_POINT ( 'NONE', #67907 ) ;
#41085=EDGE_CURVE ( 'NONE', #19782, #63727, #35988, .T. ) ;
#41112=LINE ( 'NONE', #36197, #40927 ) ;
#41118=ADVANCED_FACE ( 'NONE', ( #46090 ), #17507, .T. ) ;
#41142=DIRECTION ( 'NONE',  ( 0.000000000000000000, 0.000000000000000000, 1.000000000000000000 ) ) ;
#41151=EDGE_LOOP ( 'NONE', ( #30158, #12019, #23476, #24952 ) ) ;
#41166=CARTESIAN_POINT ( 'NONE',  ( 0.000000000000000000, -22.48208911017525580, 35.47612816024516036 ) ) ;
#41173=APPLICATION_CONTEXT ( 'automotive_design' ) ;
#41209=CARTESIAN_POINT ( 'NONE',  ( 10.00000000000000000, -6.736453364083817341, 36.88895765772630142 ) ) ;
#41230=LINE ( 'NONE', #63439, #62791 ) ;
#41241=EDGE_LOOP ( 'NONE', ( #71811, #46411, #48643, #31589 ) ) ;
#41250=FACE_OUTER_BOUND ( 'NONE', #15979, .T. ) ;
#41266=CARTESIAN_POINT ( 'NONE',  ( 10.00000000000000000, -22.48208911017474065, -35.47612816024548721 ) ) ;
#41284=ORIENTED_EDGE ( 'NONE', *, *, #70581, .F. ) ;
#41285=CIRCLE ( 'NONE', #7676, 15.99999999999999822 ) ;
#41310=EDGE_CURVE ( 'NONE', #49532, #24421, #17875, .T. ) ;
#41332=AXIS2_PLACEMENT_3D ( 'NONE', #27073, #31606, #66218 ) ;
#41338=ORIENTED_EDGE ( 'NONE', *, *, #52432, .F. ) ;
#41394=AXIS2_PLACEMENT_3D ( 'NONE', #17640, #40572, #57133 ) ;
#41414=EDGE_CURVE ( 'NONE', #36301, #31828, #72683, .T. ) ;
#41433=ORIENTED_EDGE ( 'NONE', *, *, #2897, .F. ) ;
#41459=DIRECTION ( 'NONE',  ( 1.000000000000000000, -0.000000000000000000, -0.000000000000000000 ) ) ;
#41468=DIRECTION ( 'NONE',  ( 0.000000000000000000, 0.000000000000000000, 1.000000000000000000 ) ) ;
#41469=FACE_OUTER_BOUND ( 'NONE', #70175, .T. ) ;
#41492=EDGE_CURVE ( 'NONE', #633, #60365, #64877, .T. ) ;
#41498=CARTESIAN_POINT ( 'NONE',  ( 0.000000000000000000, 31.52238457039637609, -27.75498641678709788 ) ) ;
#41502=DIRECTION ( 'NONE',  ( -1.000000000000000000, -0.000000000000000000, 0.000000000000000000 ) ) ;
#41503=AXIS2_PLACEMENT_3D ( 'NONE', #50955, #10736, #4368 ) ;
#41504=ORIENTED_EDGE ( 'NONE', *, *, #32133, .F. ) ;
#41534=EDGE_CURVE ( 'NONE', #62549, #63558, #33589, .T. ) ;
#41539=ORIENTED_EDGE ( 'NONE', *, *, #3087, .F. ) ;
#41550=ORIENTED_EDGE ( 'NONE', *, *, #1567, .T. ) ;
#41579=EDGE_CURVE ( 'NONE', #45314, #36429, #68478, .T. ) ;
#41593=CARTESIAN_POINT ( 'NONE',  ( 10.00000000000000000, 35.53030884539102630, -12.26510123303222599 ) ) ;
#41626=CARTESIAN_POINT ( 'NONE',  ( 0.000000000000000000, 0.000000000000000000, 12.50000000000000000 ) ) ;
#41627=CARTESIAN_POINT ( 'NONE',  ( 0.000000000000000000, 35.92658777277510040, 10.74501242461294659 ) ) ;
#41634=CARTESIAN_POINT ( 'NONE',  ( 10.00000000000000000, 30.80686688397041451, -21.53537804866048688 ) ) ;
#41656=EDGE_CURVE ( 'NONE', #16746, #47938, #5787, .T. ) ;
#41663=AXIS2_PLACEMENT_3D ( 'NONE', #35879, #59197, #6942 ) ;
#41687=ORIENTED_EDGE ( 'NONE', *, *, #21437, .T. ) ;
#41699=ORIENTED_EDGE ( 'NONE', *, *, #25951, .F. ) ;
#41701=CYLINDRICAL_SURFACE ( 'NONE', #68147, 16.00000000000000000 ) ;
#41729=DIRECTION ( 'NONE',  ( -1.000000000000000000, 0.000000000000000000, 0.000000000000000000 ) ) ;
#41731=EDGE_CURVE ( 'NONE', #3104, #56774, #540, .T. ) ;
#41744=DIRECTION ( 'NONE',  ( -1.000000000000000000, -0.000000000000000000, -0.000000000000000000 ) ) ;
#41745=DIRECTION ( 'NONE',  ( -1.000000000000000000, 0.000000000000000000, 0.000000000000000000 ) ) ;
#41767=EDGE_CURVE ( 'NONE', #52143, #42621, #36185, .T. ) ;
#41768=CARTESIAN_POINT ( 'NONE',  ( 10.00000000000000000, 36.88895765772633695, 6.736453364083687667 ) ) ;
#41804=DIRECTION ( 'NONE',  ( 0.000000000000000000, 1.000000000000000000, 3.491481338843133750E-15 ) ) ;
#41827=CIRCLE ( 'NONE', #35806, 42.00000000000000000 ) ;
#41829=VECTOR ( 'NONE', #46478, 1000.000000000000000 ) ;
#41833=CYLINDRICAL_SURFACE ( 'NONE', #11514, 16.00000000000000000 ) ;
#41837=FACE_OUTER_BOUND ( 'NONE', #12368, .T. ) ;
#41847=DIRECTION ( 'NONE',  ( 0.000000000000000000, 0.8910065241883657894, 0.4539904997395509678 ) ) ;
#41851=AXIS2_PLACEMENT_3D ( 'NONE', #30094, #30459, #53408 ) ;
#41854=FACE_OUTER_BOUND ( 'NONE', #2344, .T. ) ;
#41867=EDGE_CURVE ( 'NONE', #21615, #30533, #20246, .T. ) ;
#41870=ORIENTED_EDGE ( 'NONE', *, *, #26830, .T. ) ;
#41872=DIRECTION ( 'NONE',  ( -1.000000000000000000, -0.000000000000000000, -0.000000000000000000 ) ) ;
#41887=CARTESIAN_POINT ( 'NONE',  ( 0.000000000000000000, 4.992566952385522505, -37.16516213103271582 ) ) ;
#41890=AXIS2_PLACEMENT_3D ( 'NONE', #26412, #32041, #71525 ) ;
#41902=CARTESIAN_POINT ( 'NONE',  ( 4.999999999999999112, 10.41901085202078292, 40.68715046381932865 ) ) ;
#41911=AXIS2_PLACEMENT_3D ( 'NONE', #29275, #71245, #23648 ) ;
#41915=FACE_OUTER_BOUND ( 'NONE', #27441, .T. ) ;
#41923=ORIENTED_EDGE ( 'NONE', *, *, #57711, .T. ) ;
#41942=CARTESIAN_POINT ( 'NONE',  ( 10.00000000000000000, 0.000000000000000000, 0.000000000000000000 ) ) ;
#41952=EDGE_CURVE ( 'NONE', #47114, #24429, #30902, .T. ) ;
#41957=ORIENTED_EDGE ( 'NONE', *, *, #13046, .F. ) ;
#41963=CIRCLE ( 'NONE', #47968, 42.00000000000000000 ) ;
#41968=EDGE_CURVE ( 'NONE', #66872, #31431, #31093, .T. ) ;
#41974=ORIENTED_EDGE ( 'NONE', *, *, #27922, .T. ) ;
#41984=CARTESIAN_POINT ( 'NONE',  ( 10.00000000000000000, -17.80606268964516659, -33.00180498840066434 ) ) ;
#42024=DIRECTION ( 'NONE',  ( -1.000000000000000000, -0.000000000000000000, -0.000000000000000000 ) ) ;
#42033=DIRECTION ( 'NONE',  ( -1.000000000000000000, -0.000000000000000000, -0.000000000000000000 ) ) ;
#42041=CARTESIAN_POINT ( 'NONE',  ( 0.000000000000000000, -27.05870788708213226, -26.08949754953053102 ) ) ;
#42043=CIRCLE ( 'NONE', #74283, 42.00000000000000000 ) ;
#42049=EDGE_CURVE ( 'NONE', #46234, #23039, #4961, .T. ) ;
#42062=CIRCLE ( 'NONE', #1264, 15.99999999999999822 ) ;
#42064=ORIENTED_EDGE ( 'NONE', *, *, #36649, .F. ) ;
#42104=ORIENTED_EDGE ( 'NONE', *, *, #56373, .F. ) ;
#42120=CARTESIAN_POINT ( 'NONE',  ( 10.00000000000000000, 5.202137450156389953, 37.22597642581160216 ) ) ;
#42121=AXIS2_PLACEMENT_3D ( 'NONE', #29336, #456, #52281 ) ;
#42122=CARTESIAN_POINT ( 'NONE',  ( 0.000000000000000000, 21.53537804866126137, -30.80686688396986028 ) ) ;
#42127=CIRCLE ( 'NONE', #63706, 37.49900000000001654 ) ;
#42134=CARTESIAN_POINT ( 'NONE',  ( 10.00000000000000000, 17.67226234102826510, 33.17418723428314564 ) ) ;
#42137=DIRECTION ( 'NONE',  ( -1.000000000000000000, -0.000000000000000000, 0.000000000000000000 ) ) ;
#42148=DIRECTION ( 'NONE',  ( -1.000000000000000000, 0.000000000000000000, 0.000000000000000000 ) ) ;
#42186=VERTEX_POINT ( 'NONE', #40839 ) ;
#42222=EDGE_CURVE ( 'NONE', #72132, #21615, #6260, .T. ) ;
#42226=CARTESIAN_POINT ( 'NONE',  ( 0.000000000000000000, 0.000000000000000000, 0.000000000000000000 ) ) ;
#42238=CARTESIAN_POINT ( 'NONE',  ( 0.000000000000000000, 38.55633173627034438, -16.65560815589369881 ) ) ;
#42239=DIRECTION ( 'NONE',  ( -1.000000000000000000, -0.000000000000000000, -0.000000000000000000 ) ) ;
#42257=AXIS2_PLACEMENT_3D ( 'NONE', #52643, #69201, #28972 ) ;
#42258=FACE_OUTER_BOUND ( 'NONE', #72821, .T. ) ;
#42302=DIRECTION ( 'NONE',  ( 0.000000000000000000, 0.000000000000000000, -1.000000000000000000 ) ) ;
#42315=DIRECTION ( 'NONE',  ( 0.000000000000000000, 0.000000000000000000, 1.000000000000000000 ) ) ;
#42317=AXIS2_PLACEMENT_3D ( 'NONE', #45848, #17992, #17 ) ;
#42330=CARTESIAN_POINT ( 'NONE',  ( 10.00000000000000000, -26.79245525562691199, -32.34446384430000876 ) ) ;
#42347=CARTESIAN_POINT ( 'NONE',  ( -10.00000000000000000, 0.000000000000000000, 0.000000000000000000 ) ) ;
#42349=DIRECTION ( 'NONE',  ( 0.000000000000000000, 0.000000000000000000, 1.000000000000000000 ) ) ;
#42370=ORIENTED_EDGE ( 'NONE', *, *, #27466, .T. ) ;
#42397=DIRECTION ( 'NONE',  ( 1.000000000000000000, -0.000000000000000000, -0.000000000000000000 ) ) ;
#42407=PRODUCT_DEFINITION_CONTEXT ( 'detailed design', #70024, 'design' ) ;
#42447=CARTESIAN_POINT ( 'NONE',  ( 0.000000000000000000, 9.188173127307898369, -40.98264845739739570 ) ) ;
#42462=CARTESIAN_POINT ( 'NONE',  ( 0.000000000000000000, -27.13269053701078448, -25.88420570971428702 ) ) ;
#42470=ORIENTED_EDGE ( 'NONE', *, *, #32053, .T. ) ;
#42472=CARTESIAN_POINT ( 'NONE',  ( 0.000000000000000000, -0.6853352020787742971, -37.58145647212455032 ) ) ;
#42484=DIRECTION ( 'NONE',  ( 0.000000000000000000, 0.000000000000000000, 1.000000000000000000 ) ) ;
#42493=DIRECTION ( 'NONE',  ( 0.000000000000000000, 0.000000000000000000, 1.000000000000000000 ) ) ;
#42499=CARTESIAN_POINT ( 'NONE',  ( 0.000000000000000000, 30.80686688397041451, -21.53537804866048688 ) ) ;
#42505=AXIS2_PLACEMENT_3D ( 'NONE', #67539, #17514, #32936 ) ;
#42508=DIRECTION ( 'NONE',  ( 1.000000000000000000, -0.000000000000000000, 0.000000000000000000 ) ) ;
#42524=EDGE_LOOP ( 'NONE', ( #141, #31694, #23788, #4095 ) ) ;
#42571=CARTESIAN_POINT ( 'NONE',  ( -10.00000000000000000, 0.000000000000000000, 0.000000000000000000 ) ) ;
#42577=DIRECTION ( 'NONE',  ( 0.000000000000000000, 0.000000000000000000, 1.000000000000000000 ) ) ;
#42588=DIRECTION ( 'NONE',  ( 0.000000000000000000, 0.000000000000000000, 1.000000000000000000 ) ) ;
#42596=CARTESIAN_POINT ( 'NONE',  ( 10.00000000000000000, -38.55633173627023069, 16.65560815589396526 ) ) ;
#42598=CARTESIAN_POINT ( 'NONE',  ( 10.00000000000000000, -40.98264845739755913, 9.188173127307164734 ) ) ;
#42621=VERTEX_POINT ( 'NONE', #15584 ) ;
#42623=EDGE_LOOP ( 'NONE', ( #11265, #33455, #50543, #11090 ) ) ;
#42626=EDGE_CURVE ( 'NONE', #71453, #57971, #31857, .T. ) ;
#42641=FACE_OUTER_BOUND ( 'NONE', #37753, .T. ) ;
#42656=CARTESIAN_POINT ( 'NONE',  ( 10.00000000000000000, 33.80338159004307386, -16.23288003029461279 ) ) ;
#42669=CARTESIAN_POINT ( 'NONE',  ( -10.00000000000000000, 0.000000000000000000, 0.000000000000000000 ) ) ;
#42692=ORIENTED_EDGE ( 'NONE', *, *, #37442, .F. ) ;
#42695=CYLINDRICAL_SURFACE ( 'NONE', #16131, 16.00000000000000000 ) ;
#42709=DIRECTION ( 'NONE',  ( 0.000000000000000000, 0.000000000000000000, 1.000000000000000000 ) ) ;
#42718=DIRECTION ( 'NONE',  ( 0.000000000000000000, 0.9510565162951544194, -0.3090169943749447867 ) ) ;
#42740=DIRECTION ( 'NONE',  ( 0.000000000000000000, -0.9510565162951500895, -0.3090169943749583314 ) ) ;
#42744=ORIENTED_EDGE ( 'NONE', *, *, #72032, .F. ) ;
#42745=CARTESIAN_POINT ( 'NONE',  ( 10.00000000000000000, -26.08949754953044220, 27.05870788708222818 ) ) ;
#42776=CARTESIAN_POINT ( 'NONE',  ( 10.00000000000000000, 0.000000000000000000, 0.000000000000000000 ) ) ;
#42787=CARTESIAN_POINT ( 'NONE',  ( 10.00000000000000000, -0.8828120875903202602, 37.48860685352291000 ) ) ;
#42788=EDGE_CURVE ( 'NONE', #42186, #46015, #29436, .T. ) ;
#42790=CYLINDRICAL_SURFACE ( 'NONE', #43138, 37.49900000000000233 ) ;
#42801=CARTESIAN_POINT ( 'NONE',  ( 10.00000000000000000, 31.52238457039638320, -27.75498641678709788 ) ) ;
#42809=ORIENTED_EDGE ( 'NONE', *, *, #31878, .T. ) ;
#42812=CIRCLE ( 'NONE', #2020, 15.99999999999999822 ) ;
#42855=AXIS2_PLACEMENT_3D ( 'NONE', #59489, #7980, #2388 ) ;
#42858=VECTOR ( 'NONE', #23874, 1000.000000000000000 ) ;
#42860=EDGE_CURVE ( 'NONE', #65939, #4011, #38195, .T. ) ;
#42864=DIRECTION ( 'NONE',  ( 0.000000000000000000, 0.000000000000000000, 1.000000000000000000 ) ) ;
#42873=UNCERTAINTY_MEASURE_WITH_UNIT (LENGTH_MEASURE( 1.000000000000000082E-05 ), #64632, 'distance_accuracy_value', 'NONE');
#42884=ORIENTED_EDGE ( 'NONE', *, *, #13310, .T. ) ;
#42909=CARTESIAN_POINT ( 'NONE',  ( 10.00000000000000000, 0.000000000000000000, 0.000000000000000000 ) ) ;
#42932=CARTESIAN_POINT ( 'NONE',  ( 0.000000000000000000, 21.32104025579114648, 30.84782396557224970 ) ) ;
#42950=EDGE_CURVE ( 'NONE', #44755, #25438, #70588, .T. ) ;
#42962=ORIENTED_EDGE ( 'NONE', *, *, #73074, .T. ) ;
#42967=AXIS2_PLACEMENT_3D ( 'NONE', #27777, #1745, #16127 ) ;
#42978=ORIENTED_EDGE ( 'NONE', *, *, #8601, .F. ) ;
#42980=FACE_OUTER_BOUND ( 'NONE', #38733, .T. ) ;
#42985=AXIS2_PLACEMENT_3D ( 'NONE', #34102, #57046, #5555 ) ;
#42990=AXIS2_PLACEMENT_3D ( 'NONE', #64415, #12891, #42588 ) ;
#42992=ORIENTED_EDGE ( 'NONE', *, *, #65401, .F. ) ;
#42999=VERTEX_POINT ( 'NONE', #29809 ) ;
#43007=VECTOR ( 'NONE', #18622, 1000.000000000000000 ) ;
#43019=AXIS2_PLACEMENT_3D ( 'NONE', #6272, #56668, #62302 ) ;
#43022=LINE ( 'NONE', #65961, #58835 ) ;
#43032=DIRECTION ( 'NONE',  ( 0.000000000000000000, 0.000000000000000000, 1.000000000000000000 ) ) ;
#43049=DIRECTION ( 'NONE',  ( -1.000000000000000000, 0.000000000000000000, 0.000000000000000000 ) ) ;
#43057=CYLINDRICAL_SURFACE ( 'NONE', #10275, 42.00000000000000000 ) ;
#43069=CIRCLE ( 'NONE', #23902, 16.00000000000000000 ) ;
#43082=CIRCLE ( 'NONE', #34685, 16.00000000000000000 ) ;
#43087=ORIENTED_EDGE ( 'NONE', *, *, #19577, .F. ) ;
#43103=ORIENTED_EDGE ( 'NONE', *, *, #14319, .T. ) ;
#43113=ADVANCED_FACE ( 'NONE', ( #60265 ), #60982, .T. ) ;
#43117=VERTEX_POINT ( 'NONE', #21486 ) ;
#43118=FACE_OUTER_BOUND ( 'NONE', #7142, .T. ) ;
#43138=AXIS2_PLACEMENT_3D ( 'NONE', #55175, #48424, #30747 ) ;
#43146=ORIENTED_EDGE ( 'NONE', *, *, #58317, .T. ) ;
#43150=AXIS2_PLACEMENT_3D ( 'NONE', #3061, #48883, #20318 ) ;
#43160=DIRECTION ( 'NONE',  ( 0.000000000000000000, 0.000000000000000000, 1.000000000000000000 ) ) ;
#43165=AXIS2_PLACEMENT_3D ( 'NONE', #25418, #60013, #31413 ) ;
#43174=ORIENTED_EDGE ( 'NONE', *, *, #22323, .F. ) ;
#43187=DIRECTION ( 'NONE',  ( -1.000000000000000000, 0.000000000000000000, 0.000000000000000000 ) ) ;
#43199=VECTOR ( 'NONE', #35149, 1000.000000000000000 ) ;
#43209=EDGE_LOOP ( 'NONE', ( #32173, #15618, #37981, #21276 ) ) ;
#43212=ORIENTED_EDGE ( 'NONE', *, *, #46293, .F. ) ;
#43238=EDGE_CURVE ( 'NONE', #50408, #59461, #33347, .T. ) ;
#43239=CARTESIAN_POINT ( 'NONE',  ( 0.000000000000000000, 27.13269053701096922, 25.88420570971410228 ) ) ;
#43240=DIRECTION ( 'NONE',  ( 0.000000000000000000, -0.5877852522924801315, 0.8090169943749421222 ) ) ;
#43258=AXIS2_PLACEMENT_3D ( 'NONE', #53680, #20198, #55539 ) ;
#43271=CARTESIAN_POINT ( 'NONE',  ( 10.00000000000000000, -21.32104025579091910, -30.84782396557241313 ) ) ;
#43276=CARTESIAN_POINT ( 'NONE',  ( 0.000000000000000000, 0.000000000000000000, 0.000000000000000000 ) ) ;
#43282=ORIENTED_EDGE ( 'NONE', *, *, #39639, .T. ) ;
#43294=EDGE_CURVE ( 'NONE', #46015, #45314, #69424, .T. ) ;
#43329=DIRECTION ( 'NONE',  ( 0.000000000000000000, 0.4539904997395477482, -0.8910065241883673437 ) ) ;
#43335=ORIENTED_EDGE ( 'NONE', *, *, #36891, .F. ) ;
#43351=DIRECTION ( 'NONE',  ( -1.000000000000000000, -0.000000000000000000, -0.000000000000000000 ) ) ;
#43371=DIRECTION ( 'NONE',  ( 0.000000000000000000, 0.000000000000000000, -1.000000000000000000 ) ) ;
#43377=VERTEX_POINT ( 'NONE', #23722 ) ;
#43380=ORIENTED_EDGE ( 'NONE', *, *, #4043, .F. ) ;
#43395=AXIS2_PLACEMENT_3D ( 'NONE', #48320, #71232, #19735 ) ;
#43416=ORIENTED_EDGE ( 'NONE', *, *, #59584, .F. ) ;
#43427=DIRECTION ( 'NONE',  ( 0.000000000000000000, -0.4539904997395351471, -0.8910065241883737830 ) ) ;
#43434=CARTESIAN_POINT ( 'NONE',  ( 50.00005079999999680, 0.000000000000000000, 0.000000000000000000 ) ) ;
#43436=DIRECTION ( 'NONE',  ( 0.000000000000000000, 0.000000000000000000, 1.000000000000000000 ) ) ;
#43437=DIRECTION ( 'NONE',  ( -1.000000000000000000, 0.000000000000000000, 0.000000000000000000 ) ) ;
#43441=FACE_OUTER_BOUND ( 'NONE', #26787, .T. ) ;
#43449=CARTESIAN_POINT ( 'NONE',  ( 4.999999999999999112, 36.13751322684449008, -21.40280677340332716 ) ) ;
#43456=CIRCLE ( 'NONE', #33819, 37.49900000000000233 ) ;
#43465=AXIS2_PLACEMENT_3D ( 'NONE', #51318, #16754, #22773 ) ;
#43474=EDGE_CURVE ( 'NONE', #63558, #26140, #1050, .T. ) ;
#43483=ORIENTED_EDGE ( 'NONE', *, *, #6206, .F. ) ;
#43490=LINE ( 'NONE', #3638, #61843 ) ;
#43497=ADVANCED_FACE ( 'NONE', ( #58308 ), #18446, .T. ) ;
#43508=AXIS2_PLACEMENT_3D ( 'NONE', #40535, #17242, #34158 ) ;
#43520=DIRECTION ( 'NONE',  ( -1.000000000000000000, -0.000000000000000000, -0.000000000000000000 ) ) ;
#43562=CIRCLE ( 'NONE', #20731, 16.00000000000000000 ) ;
#43567=DIRECTION ( 'NONE',  ( 0.000000000000000000, -0.4539904997395541320, 0.8910065241883640130 ) ) ;
#43570=ORIENTED_EDGE ( 'NONE', *, *, #66083, .T. ) ;
#43587=ORIENTED_EDGE ( 'NONE', *, *, #21142, .F. ) ;
#43625=DIRECTION ( 'NONE',  ( 0.000000000000000000, 0.000000000000000000, 1.000000000000000000 ) ) ;
#43634=DIRECTION ( 'NONE',  ( -1.000000000000000000, 0.000000000000000000, 0.000000000000000000 ) ) ;
#43645=ADVANCED_FACE ( 'NONE', ( #41854 ), #7643, .T. ) ;
#43649=FACE_OUTER_BOUND ( 'NONE', #25982, .T. ) ;
#43674=DIRECTION ( 'NONE',  ( 0.000000000000000000, 0.000000000000000000, -1.000000000000000000 ) ) ;
#43692=FACE_OUTER_BOUND ( 'NONE', #27854, .T. ) ;
#43704=CARTESIAN_POINT ( 'NONE',  ( 10.00000000000000000, 33.17418723428307459, 17.67226234102837878 ) ) ;
#43712=CARTESIAN_POINT ( 'NONE',  ( 10.00000000000000000, -32.34446384429951138, -26.79245525562750530 ) ) ;
#43722=EDGE_CURVE ( 'NONE', #35508, #48259, #47499, .T. ) ;
#43729=VERTEX_POINT ( 'NONE', #42598 ) ;
#43762=LINE ( 'NONE', #33946, #1836 ) ;
#43764=CARTESIAN_POINT ( 'NONE',  ( 5.000000000000000000, 15.48615015657637706, -39.04073710021327770 ) ) ;
#43774=AXIS2_PLACEMENT_3D ( 'NONE', #47622, #69441, #19413 ) ;
#43792=CARTESIAN_POINT ( 'NONE',  ( 10.00000000000000000, 0.000000000000000000, 0.000000000000000000 ) ) ;
#43794=AXIS2_PLACEMENT_3D ( 'NONE', #53338, #58240, #63897 ) ;
#43893=CARTESIAN_POINT ( 'NONE',  ( 0.000000000000000000, 37.58145647212453611, 16.68533520207917675 ) ) ;
#43895=DIRECTION ( 'NONE',  ( -1.000000000000000000, -0.000000000000000000, 0.000000000000000000 ) ) ;
#43904=AXIS2_PLACEMENT_3D ( 'NONE', #54989, #26047, #43371 ) ;
#43906=EDGE_CURVE ( 'NONE', #73517, #30173, #15431, .T. ) ;
#43911=FACE_OUTER_BOUND ( 'NONE', #35503, .T. ) ;
#43920=CARTESIAN_POINT ( 'NONE',  ( 0.000000000000000000, 25.88420570971400991, 27.13269053701105449 ) ) ;
#43926=DIRECTION ( 'NONE',  ( -1.000000000000000000, 0.000000000000000000, -0.000000000000000000 ) ) ;
#43934=ORIENTED_EDGE ( 'NONE', *, *, #7805, .F. ) ;
#43952=ORIENTED_EDGE ( 'NONE', *, *, #50818, .T. ) ;
#43954=EDGE_LOOP ( 'NONE', ( #30032, #4333, #67034, #34906 ) ) ;
#43958=EDGE_LOOP ( 'NONE', ( #6419, #25968, #36703, #37305 ) ) ;
#44023=VECTOR ( 'NONE', #16581, 1000.000000000000000 ) ;
#44034=VERTEX_POINT ( 'NONE', #57951 ) ;
#44035=EDGE_CURVE ( 'NONE', #72017, #47938, #57481, .T. ) ;
#44037=LINE ( 'NONE', #44410, #31256 ) ;
#44045=ORIENTED_EDGE ( 'NONE', *, *, #69450, .T. ) ;
#44053=DIRECTION ( 'NONE',  ( -1.000000000000000000, -0.000000000000000000, -0.000000000000000000 ) ) ;
#44065=DIRECTION ( 'NONE',  ( -1.000000000000000000, 0.000000000000000000, -0.000000000000000000 ) ) ;
#44073=EDGE_CURVE ( 'NONE', #10923, #26528, #35388, .T. ) ;
#44082=DIRECTION ( 'NONE',  ( 0.000000000000000000, 0.000000000000000000, -1.000000000000000000 ) ) ;
#44091=CARTESIAN_POINT ( 'NONE',  ( -10.00000000000000000, 0.000000000000000000, 0.000000000000000000 ) ) ;
#44099=VERTEX_POINT ( 'NONE', #12443 ) ;
#44100=CARTESIAN_POINT ( 'NONE',  ( 0.000000000000000000, 10.41901085202135491, -40.68715046381917944 ) ) ;
#44104=ORIENTED_EDGE ( 'NONE', *, *, #32761, .T. ) ;
#44107=CARTESIAN_POINT ( 'NONE',  ( 10.00000000000000000, 0.000000000000000000, 0.000000000000000000 ) ) ;
#44109=ORIENTED_EDGE ( 'NONE', *, *, #41492, .T. ) ;
#44112=ORIENTED_EDGE ( 'NONE', *, *, #59449, .F. ) ;
#44116=CARTESIAN_POINT ( 'NONE',  ( 10.00000000000000000, 26.79245525562714647, 32.34446384429980981 ) ) ;
#44118=ADVANCED_FACE ( 'NONE', ( #65081 ), #36858, .T. ) ;
#44120=CARTESIAN_POINT ( 'NONE',  ( 10.00000000000000000, 0.000000000000000000, 0.000000000000000000 ) ) ;
#44124=ORIENTED_EDGE ( 'NONE', *, *, #32995, .T. ) ;
#44128=VERTEX_POINT ( 'NONE', #1587 ) ;
#44133=FACE_OUTER_BOUND ( 'NONE', #35046, .T. ) ;
#44166=ADVANCED_FACE ( 'NONE', ( #35738 ), #7558, .T. ) ;
#44188=VERTEX_POINT ( 'NONE', #24837 ) ;
#44194=EDGE_CURVE ( 'NONE', #16169, #62276, #1163, .T. ) ;
#44205=EDGE_CURVE ( 'NONE', #54468, #53437, #65812, .T. ) ;
#44218=ORIENTED_EDGE ( 'NONE', *, *, #57235, .T. ) ;
#44231=VERTEX_POINT ( 'NONE', #14666 ) ;
#44273=CARTESIAN_POINT ( 'NONE',  ( 10.00000000000000000, -36.13751322684404244, -21.40280677340410165 ) ) ;
#44275=CARTESIAN_POINT ( 'NONE',  ( 0.000000000000000000, 0.000000000000000000, 0.000000000000000000 ) ) ;
#44281=DIRECTION ( 'NONE',  ( -1.000000000000000000, 0.000000000000000000, 0.000000000000000000 ) ) ;
#44286=AXIS2_PLACEMENT_3D ( 'NONE', #39088, #22164, #32678 ) ;
#44287=ORIENTED_EDGE ( 'NONE', *, *, #29371, .T. ) ;
#44301=CARTESIAN_POINT ( 'NONE',  ( 0.000000000000000000, -27.05870788708250885, 26.08949754953014022 ) ) ;
#44302=ORIENTED_EDGE ( 'NONE', *, *, #27213, .T. ) ;
#44319=ORIENTED_EDGE ( 'NONE', *, *, #13513, .T. ) ;
#44323=ORIENTED_EDGE ( 'NONE', *, *, #63814, .F. ) ;
#44332=DIRECTION ( 'NONE',  ( 0.000000000000000000, 0.000000000000000000, 1.000000000000000000 ) ) ;
#44333=DIRECTION ( 'NONE',  ( -1.000000000000000000, 0.000000000000000000, -0.000000000000000000 ) ) ;
#44344=CARTESIAN_POINT ( 'NONE',  ( 0.000000000000000000, 30.00120703465236716, -22.64427369931138756 ) ) ;
#44350=AXIS2_PLACEMENT_3D ( 'NONE', #28638, #51203, #39566 ) ;
#44351=VECTOR ( 'NONE', #30374, 1000.000000000000000 ) ;
#44353=CARTESIAN_POINT ( 'NONE',  ( 10.00000000000000000, 5.202137450156389953, 37.22597642581160216 ) ) ;
#44354=CYLINDRICAL_SURFACE ( 'NONE', #44286, 16.00000000000000000 ) ;
#44376=VERTEX_POINT ( 'NONE', #50357 ) ;
#44381=EDGE_LOOP ( 'NONE', ( #57892, #52233, #31161, #32546 ) ) ;
#44410=CARTESIAN_POINT ( 'NONE',  ( 4.999999999999999112, 2.663952781846732343, -41.91543099594814947 ) ) ;
#44420=EDGE_LOOP ( 'NONE', ( #21416, #39342, #54908, #29281 ) ) ;
#44428=AXIS2_PLACEMENT_3D ( 'NONE', #9670, #32211, #65346 ) ;
#44437=VECTOR ( 'NONE', #17751, 1000.000000000000000 ) ;
#44456=ORIENTED_EDGE ( 'NONE', *, *, #45785, .F. ) ;
#44472=EDGE_LOOP ( 'NONE', ( #36580, #25136, #15143, #53977 ) ) ;
#44475=CIRCLE ( 'NONE', #21655, 16.00000000000000000 ) ;
#44478=AXIS2_PLACEMENT_3D ( 'NONE', #27794, #68772, #4512 ) ;
#44491=DIRECTION ( 'NONE',  ( -1.000000000000000000, 0.000000000000000000, -0.000000000000000000 ) ) ;
#44492=EDGE_CURVE ( 'NONE', #56256, #20705, #23990, .T. ) ;
#44516=DIRECTION ( 'NONE',  ( -1.000000000000000000, 0.000000000000000000, -0.000000000000000000 ) ) ;
#44559=EDGE_CURVE ( 'NONE', #61302, #53203, #28813, .T. ) ;
#44561=CARTESIAN_POINT ( 'NONE',  ( 10.00000000000000000, 0.000000000000000000, 0.000000000000000000 ) ) ;
#44582=ORIENTED_EDGE ( 'NONE', *, *, #12730, .F. ) ;
#44599=DIRECTION ( 'NONE',  ( -1.000000000000000000, 0.000000000000000000, -0.000000000000000000 ) ) ;
#44657=DIRECTION ( 'NONE',  ( -1.000000000000000000, 0.000000000000000000, 0.000000000000000000 ) ) ;
#44687=EDGE_CURVE ( 'NONE', #36429, #21975, #39604, .T. ) ;
#44695=DIRECTION ( 'NONE',  ( -1.000000000000000000, -0.000000000000000000, 0.000000000000000000 ) ) ;
#44714=DIRECTION ( 'NONE',  ( 1.000000000000000000, 0.000000000000000000, 0.000000000000000000 ) ) ;
#44732=DIRECTION ( 'NONE',  ( 0.000000000000000000, 0.3090169943749410120, 0.9510565162951557516 ) ) ;
#44755=VERTEX_POINT ( 'NONE', #61568 ) ;
#44761=EDGE_CURVE ( 'NONE', #30109, #47902, #58808, .T. ) ;
#44780=VERTEX_POINT ( 'NONE', #44273 ) ;
#44800=DIRECTION ( 'NONE',  ( -1.000000000000000000, -0.000000000000000000, 0.000000000000000000 ) ) ;
#44801=ORIENTED_EDGE ( 'NONE', *, *, #34712, .F. ) ;
#44803=DIRECTION ( 'NONE',  ( 0.000000000000000000, 0.000000000000000000, 1.000000000000000000 ) ) ;
#44815=EDGE_CURVE ( 'NONE', #34136, #57179, #3331, .T. ) ;
#44817=CARTESIAN_POINT ( 'NONE',  ( 0.000000000000000000, -21.32104025579091910, -30.84782396557241313 ) ) ;
#44827=VERTEX_POINT ( 'NONE', #66466 ) ;
#44832=CARTESIAN_POINT ( 'NONE',  ( 10.00000000000000000, 0.000000000000000000, 0.000000000000000000 ) ) ;
#44883=DIRECTION ( 'NONE',  ( -1.000000000000000000, -0.000000000000000000, -0.000000000000000000 ) ) ;
#44899=DIRECTION ( 'NONE',  ( 0.000000000000000000, 0.000000000000000000, 1.000000000000000000 ) ) ;
#44903=CARTESIAN_POINT ( 'NONE',  ( 0.000000000000000000, -10.96151621346514382, 35.95386929396252640 ) ) ;
#44913=EDGE_CURVE ( 'NONE', #13679, #56468, #11952, .T. ) ;
#44918=ADVANCED_FACE ( 'NONE', ( #308 ), #69060, .F. ) ;
#44945=DIRECTION ( 'NONE',  ( -1.000000000000000000, -0.000000000000000000, -0.000000000000000000 ) ) ;
#44949=DIRECTION ( 'NONE',  ( -1.000000000000000000, -0.000000000000000000, -0.000000000000000000 ) ) ;
#44953=ORIENTED_EDGE ( 'NONE', *, *, #40427, .F. ) ;
#44961=ORIENTED_EDGE ( 'NONE', *, *, #9185, .T. ) ;
#44986=CYLINDRICAL_SURFACE ( 'NONE', #60101, 15.99999999999999645 ) ;
#45009=AXIS2_PLACEMENT_3D ( 'NONE', #39967, #69993, #46342 ) ;
#45012=DIRECTION ( 'NONE',  ( -1.000000000000000000, 0.000000000000000000, 0.000000000000000000 ) ) ;
#45014=CARTESIAN_POINT ( 'NONE',  ( 0.000000000000000000, -16.23288003029473359, -33.80338159004301701 ) ) ;
#45033=CARTESIAN_POINT ( 'NONE',  ( 10.00000000000000000, 33.00180498840046539, 17.80606268964551120 ) ) ;
#45059=CARTESIAN_POINT ( 'NONE',  ( 10.00000000000000000, 35.95386929396256903, -10.96151621346501237 ) ) ;
#45064=VERTEX_POINT ( 'NONE', #8023 ) ;
#45071=VECTOR ( 'NONE', #8, 1000.000000000000000 ) ;
#45110=CIRCLE ( 'NONE', #40319, 16.00000000000000355 ) ;
#45141=CYLINDRICAL_SURFACE ( 'NONE', #18016, 16.00000000000000355 ) ;
#45143=EDGE_CURVE ( 'NONE', #61669, #66673, #64886, .T. ) ;
#45196=EDGE_CURVE ( 'NONE', #13202, #61584, #27896, .T. ) ;
#45200=CYLINDRICAL_SURFACE ( 'NONE', #2185, 16.00000000000000000 ) ;
#45207=FACE_OUTER_BOUND ( 'NONE', #31822, .T. ) ;
#45211=DIRECTION ( 'NONE',  ( -1.000000000000000000, 0.000000000000000000, -0.000000000000000000 ) ) ;
#45217=VERTEX_POINT ( 'NONE', #67762 ) ;
#45227=VECTOR ( 'NONE', #4507, 1000.000000000000000 ) ;
#45232=ORIENTED_EDGE ( 'NONE', *, *, #72376, .T. ) ;
#45233=ORIENTED_EDGE ( 'NONE', *, *, #37165, .F. ) ;
#45248=DIRECTION ( 'NONE',  ( 0.000000000000000000, 0.000000000000000000, 1.000000000000000000 ) ) ;
#45261=DIRECTION ( 'NONE',  ( 1.000000000000000000, -0.000000000000000000, 0.000000000000000000 ) ) ;
#45269=EDGE_CURVE ( 'NONE', #37324, #4529, #70871, .T. ) ;
#45284=EDGE_CURVE ( 'NONE', #13377, #22270, #12003, .T. ) ;
#45293=CIRCLE ( 'NONE', #22464, 42.00000000000000000 ) ;
#45300=DIRECTION ( 'NONE',  ( 0.000000000000000000, -0.5877852522924624790, -0.8090169943749553338 ) ) ;
#45314=VERTEX_POINT ( 'NONE', #68510 ) ;
#45336=DIRECTION ( 'NONE',  ( 0.000000000000000000, 0.000000000000000000, 1.000000000000000000 ) ) ;
#45367=DIRECTION ( 'NONE',  ( 0.000000000000000000, 0.000000000000000000, 1.000000000000000000 ) ) ;
#45371=ORIENTED_EDGE ( 'NONE', *, *, #44559, .T. ) ;
#45395=CARTESIAN_POINT ( 'NONE',  ( -1.200000000000000030E-05, 16.95692799528845640, -2.500000000000000000 ) ) ;
#45396=CARTESIAN_POINT ( 'NONE',  ( 0.000000000000000000, -17.67226234102849958, 33.17418723428301774 ) ) ;
#45402=ADVANCED_FACE ( 'NONE', ( #45207 ), #11706, .T. ) ;
#45410=CYLINDRICAL_SURFACE ( 'NONE', #17248, 16.00000000000000000 ) ;
#45423=ORIENTED_EDGE ( 'NONE', *, *, #34441, .T. ) ;
#45428=DIRECTION ( 'NONE',  ( -1.000000000000000000, -0.000000000000000000, -0.000000000000000000 ) ) ;
#45438=DIRECTION ( 'NONE',  ( 0.000000000000000000, -0.9510565162951500895, -0.3090169943749581649 ) ) ;
#45441=CARTESIAN_POINT ( 'NONE',  ( 10.00000000000000000, 35.92658777277525672, -10.74501242461245809 ) ) ;
#45452=EDGE_CURVE ( 'NONE', #6488, #46015, #49137, .T. ) ;
#45455=ORIENTED_EDGE ( 'NONE', *, *, #33286, .T. ) ;
#45460=LINE ( 'NONE', #10861, #36944 ) ;
#45467=CIRCLE ( 'NONE', #1045, 16.00000000000000000 ) ;
#45483=EDGE_CURVE ( 'NONE', #20649, #72017, #19566, .T. ) ;
#45498=EDGE_CURVE ( 'NONE', #11957, #52503, #65459, .T. ) ;
#45500=DIRECTION ( 'NONE',  ( 1.000000000000000000, 0.000000000000000000, 0.000000000000000000 ) ) ;
#45513=AXIS2_PLACEMENT_3D ( 'NONE', #12466, #863, #23394 ) ;
#45526=ORIENTED_EDGE ( 'NONE', *, *, #48734, .F. ) ;
#45550=DIRECTION ( 'NONE',  ( -1.000000000000000000, 0.000000000000000000, 0.000000000000000000 ) ) ;
#45576=EDGE_CURVE ( 'NONE', #45217, #46805, #64347, .T. ) ;
#45589=ORIENTED_EDGE ( 'NONE', *, *, #44073, .T. ) ;
#45596=EDGE_LOOP ( 'NONE', ( #15821, #27196, #43212, #72864 ) ) ;
#45602=ORIENTED_EDGE ( 'NONE', *, *, #70971, .F. ) ;
#45619=EDGE_LOOP ( 'NONE', ( #32395, #14694, #65204, #57354 ) ) ;
#45641=LINE ( 'NONE', #73434, #15136 ) ;
#45655=CARTESIAN_POINT ( 'NONE',  ( 10.00000000000000000, 0.000000000000000000, 0.000000000000000000 ) ) ;
#45657=EDGE_LOOP ( 'NONE', ( #50934, #28542, #3993, #37274 ) ) ;
#45682=DIRECTION ( 'NONE',  ( 0.000000000000000000, 0.000000000000000000, 1.000000000000000000 ) ) ;
#45695=ORIENTED_EDGE ( 'NONE', *, *, #41310, .F. ) ;
#45697=ORIENTED_EDGE ( 'NONE', *, *, #66288, .T. ) ;
#45699=EDGE_CURVE ( 'NONE', #6579, #56950, #37982, .T. ) ;
#45730=CARTESIAN_POINT ( 'NONE',  ( 0.000000000000000000, -27.75498641678764855, 31.52238457039590358 ) ) ;
#45754=DIRECTION ( 'NONE',  ( -1.000000000000000000, -0.000000000000000000, -0.000000000000000000 ) ) ;
#45775=CARTESIAN_POINT ( 'NONE',  ( 5.000000000000000000, 26.79245525562762253, -32.34446384429941901 ) ) ;
#45783=EDGE_CURVE ( 'NONE', #53203, #22270, #21485, .T. ) ;
#45785=EDGE_CURVE ( 'NONE', #37995, #63103, #17910, .T. ) ;
#45795=ORIENTED_EDGE ( 'NONE', *, *, #61563, .F. ) ;
#45833=DIRECTION ( 'NONE',  ( 1.000000000000000000, 0.000000000000000000, 0.000000000000000000 ) ) ;
#45842=AXIS2_PLACEMENT_3D ( 'NONE', #33716, #56669, #17535 ) ;
#45848=CARTESIAN_POINT ( 'NONE',  ( 0.000000000000000000, 0.000000000000000000, 0.000000000000000000 ) ) ;
#45866=AXIS2_PLACEMENT_3D ( 'NONE', #28503, #4, #1104 ) ;
#45878=AXIS2_PLACEMENT_3D ( 'NONE', #69727, #59194, #40800 ) ;
#45918=CARTESIAN_POINT ( 'NONE',  ( 0.000000000000000000, 3.925862922256160736, 41.81611651403863306 ) ) ;
#45927=FACE_OUTER_BOUND ( 'NONE', #34298, .T. ) ;
#45930=ORIENTED_EDGE ( 'NONE', *, *, #11990, .F. ) ;
#45932=EDGE_CURVE ( 'NONE', #10439, #54468, #47903, .T. ) ;
#45958=ADVANCED_FACE ( 'NONE', ( #49835 ), #27656, .T. ) ;
#45986=DIRECTION ( 'NONE',  ( -1.000000000000000000, 0.000000000000000000, 0.000000000000000000 ) ) ;
#46003=DIRECTION ( 'NONE',  ( -1.000000000000000000, -0.000000000000000000, 0.000000000000000000 ) ) ;
#46015=VERTEX_POINT ( 'NONE', #55859 ) ;
#46090=FACE_OUTER_BOUND ( 'NONE', #58453, .T. ) ;
#46108=LINE ( 'NONE', #40096, #62560 ) ;
#46130=EDGE_CURVE ( 'NONE', #36429, #49000, #52065, .T. ) ;
#46131=CIRCLE ( 'NONE', #33992, 16.00000000000000000 ) ;
#46149=ORIENTED_EDGE ( 'NONE', *, *, #70890, .T. ) ;
#46185=VERTEX_POINT ( 'NONE', #34782 ) ;
#46187=ORIENTED_EDGE ( 'NONE', *, *, #61387, .F. ) ;
#46198=DIRECTION ( 'NONE',  ( 0.000000000000000000, 0.000000000000000000, 1.000000000000000000 ) ) ;
#46199=CARTESIAN_POINT ( 'NONE',  ( 10.00000000000000000, 4.992566952385523393, -37.16516213103272293 ) ) ;
#46232=ORIENTED_EDGE ( 'NONE', *, *, #13513, .F. ) ;
#46234=VERTEX_POINT ( 'NONE', #22775 ) ;
#46246=DIRECTION ( 'NONE',  ( 0.000000000000000000, 0.000000000000000000, 1.000000000000000000 ) ) ;
#46270=ORIENTED_EDGE ( 'NONE', *, *, #62650, .T. ) ;
#46276=CARTESIAN_POINT ( 'NONE',  ( 5.000000000000000000, -35.47612816024506088, -22.48208911017539435 ) ) ;
#46278=CYLINDRICAL_SURFACE ( 'NONE', #8509, 16.00000000000000000 ) ;
#46293=EDGE_CURVE ( 'NONE', #18771, #57844, #53929, .T. ) ;
#46294=EDGE_CURVE ( 'NONE', #8967, #67395, #19132, .T. ) ;
#46306=LINE ( 'NONE', #69603, #4164 ) ;
#46323=DIRECTION ( 'NONE',  ( -1.000000000000000000, 0.000000000000000000, 0.000000000000000000 ) ) ;
#46325=EDGE_CURVE ( 'NONE', #36437, #14549, #2395, .T. ) ;
#46338=EDGE_LOOP ( 'NONE', ( #14263, #22578, #60304, #65673 ) ) ;
#46342=DIRECTION ( 'NONE',  ( 0.000000000000000000, -0.3090169943749549453, 0.9510565162951511997 ) ) ;
#46345=DIRECTION ( 'NONE',  ( -1.000000000000000000, 0.000000000000000000, 0.000000000000000000 ) ) ;
#46398=DIRECTION ( 'NONE',  ( 1.000000000000000000, 0.000000000000000000, 0.000000000000000000 ) ) ;
#46402=VECTOR ( 'NONE', #61355, 1000.000000000000000 ) ;
#46410=ORIENTED_EDGE ( 'NONE', *, *, #50074, .F. ) ;
#46411=ORIENTED_EDGE ( 'NONE', *, *, #38041, .F. ) ;
#46423=EDGE_CURVE ( 'NONE', #18937, #3856, #24032, .T. ) ;
#46424=EDGE_LOOP ( 'NONE', ( #46918, #29482, #53248, #36819 ) ) ;
#46431=DIRECTION ( 'NONE',  ( 0.000000000000000000, 0.8090169943749445647, 0.5877852522924770229 ) ) ;
#46446=CYLINDRICAL_SURFACE ( 'NONE', #13840, 16.00000000000000000 ) ;
#46450=ORIENTED_EDGE ( 'NONE', *, *, #29348, .T. ) ;
#46478=DIRECTION ( 'NONE',  ( -1.000000000000000000, 0.000000000000000000, 0.000000000000000000 ) ) ;
#46488=COLOUR_RGB ( '', 0.72549020, 0.75294118, 0.79215686) ;
#46524=EDGE_CURVE ( 'NONE', #6569, #40304, #42062, .T. ) ;
#46532=DIRECTION ( 'NONE',  ( 0.000000000000000000, 0.000000000000000000, 1.000000000000000000 ) ) ;
#46539=ORIENTED_EDGE ( 'NONE', *, *, #16615, .F. ) ;
#46558=LINE ( 'NONE', #28147, #31306 ) ;
#46565=CARTESIAN_POINT ( 'NONE',  ( 0.000000000000000000, 0.000000000000000000, 0.000000000000000000 ) ) ;
#46572=AXIS2_PLACEMENT_3D ( 'NONE', #10728, #73868, #57979 ) ;
#46573=VECTOR ( 'NONE', #72005, 1000.000000000000000 ) ;
#46580=CYLINDRICAL_SURFACE ( 'NONE', #5865, 37.49900000000000233 ) ;
#46583=FACE_OUTER_BOUND ( 'NONE', #43954, .T. ) ;
#46621=ORIENTED_EDGE ( 'NONE', *, *, #23524, .F. ) ;
#46647=DIRECTION ( 'NONE',  ( -1.000000000000000000, 0.000000000000000000, 0.000000000000000000 ) ) ;
#46663=CIRCLE ( 'NONE', #57506, 37.49900000000000233 ) ;
#46669=DIRECTION ( 'NONE',  ( 0.000000000000000000, 1.000000000000000000, -9.787530781167598712E-16 ) ) ;
#46672=AXIS2_PLACEMENT_3D ( 'NONE', #37921, #32632, #3727 ) ;
#46713=EDGE_CURVE ( 'NONE', #20594, #13869, #4837, .T. ) ;
#46740=AXIS2_PLACEMENT_3D ( 'NONE', #43276, #31099, #7444 ) ;
#46742=ORIENTED_EDGE ( 'NONE', *, *, #15275, .F. ) ;
#46756=CARTESIAN_POINT ( 'NONE',  ( 4.999999999999999112, 16.65560815589411092, 38.55633173627015253 ) ) ;
#46770=CARTESIAN_POINT ( 'NONE',  ( 10.00000000000000000, 15.48615015657638239, -39.04073710021328480 ) ) ;
#46780=CARTESIAN_POINT ( 'NONE',  ( 4.999999999999999112, -10.41901085202107247, 40.68715046381925049 ) ) ;
#46805=VERTEX_POINT ( 'NONE', #58740 ) ;
#46812=DIRECTION ( 'NONE',  ( -1.000000000000000000, 0.000000000000000000, 0.000000000000000000 ) ) ;
#46829=CARTESIAN_POINT ( 'NONE',  ( 0.000000000000000000, -0.8828120875898013420, -37.48860685352291711 ) ) ;
#46831=ORIENTED_EDGE ( 'NONE', *, *, #17644, .F. ) ;
#46845=VECTOR ( 'NONE', #52365, 1000.000000000000000 ) ;
#46870=EDGE_CURVE ( 'NONE', #20705, #51673, #16899, .T. ) ;
#46886=CYLINDRICAL_SURFACE ( 'NONE', #29742, 16.00000000000000000 ) ;
#46902=ORIENTED_EDGE ( 'NONE', *, *, #70581, .T. ) ;
#46904=ORIENTED_EDGE ( 'NONE', *, *, #31834, .F. ) ;
#46905=CARTESIAN_POINT ( 'NONE',  ( 0.000000000000000000, 41.91543099594818500, -2.663952781846294915 ) ) ;
#46910=DIRECTION ( 'NONE',  ( -1.000000000000000000, 0.000000000000000000, 0.000000000000000000 ) ) ;
#46918=ORIENTED_EDGE ( 'NONE', *, *, #39026, .F. ) ;
#46941=CARTESIAN_POINT ( 'NONE',  ( 10.00000000000000000, 40.98264845739763018, -9.188173127306866306 ) ) ;
#46945=DIRECTION ( 'NONE',  ( -1.000000000000000000, 0.000000000000000000, -0.000000000000000000 ) ) ;
#46965=EDGE_CURVE ( 'NONE', #21754, #44827, #44037, .T. ) ;
#46973=DIRECTION ( 'NONE',  ( 0.000000000000000000, -0.9876883405951393247, 0.1564344650402204329 ) ) ;
#46977=DIRECTION ( 'NONE',  ( -1.000000000000000000, -0.000000000000000000, -0.000000000000000000 ) ) ;
#46990=DIRECTION ( 'NONE',  ( 0.000000000000000000, 0.9510565162951544194, -0.3090169943749446757 ) ) ;
#47001=VERTEX_POINT ( 'NONE', #56051 ) ;
#47009=DIRECTION ( 'NONE',  ( 0.000000000000000000, 0.000000000000000000, 1.000000000000000000 ) ) ;
#47020=EDGE_CURVE ( 'NONE', #56774, #26992, #60103, .T. ) ;
#47021=CARTESIAN_POINT ( 'NONE',  ( 10.00000000000000000, 21.40280677340421533, -36.13751322684397138 ) ) ;
#47028=DIRECTION ( 'NONE',  ( 0.000000000000000000, 0.000000000000000000, 1.000000000000000000 ) ) ;
#47034=AXIS2_PLACEMENT_3D ( 'NONE', #63663, #58750, #30161 ) ;
#47038=DIRECTION ( 'NONE',  ( 0.000000000000000000, 0.000000000000000000, 1.000000000000000000 ) ) ;
#47048=CARTESIAN_POINT ( 'NONE',  ( 10.00000000000000000, -37.48860685352291711, 0.8828120875899322373 ) ) ;
#47049=DIRECTION ( 'NONE',  ( 0.000000000000000000, -0.7071067811865389130, -0.7071067811865561215 ) ) ;
#47058=DIRECTION ( 'NONE',  ( -1.000000000000000000, -0.000000000000000000, 0.000000000000000000 ) ) ;
#47060=CYLINDRICAL_SURFACE ( 'NONE', #71566, 16.00000000000000000 ) ;
#47063=CARTESIAN_POINT ( 'NONE',  ( 10.00000000000000000, -37.16516213103280108, 4.992566952384862589 ) ) ;
#47068=LINE ( 'NONE', #17011, #47856 ) ;
#47074=EDGE_LOOP ( 'NONE', ( #59177, #48005, #8215, #52142 ) ) ;
#47114=VERTEX_POINT ( 'NONE', #16949 ) ;
#47125=DIRECTION ( 'NONE',  ( 0.000000000000000000, -0.8910065241883722287, 0.4539904997395382558 ) ) ;
#47141=DIRECTION ( 'NONE',  ( 1.000000000000000000, 0.000000000000000000, 0.000000000000000000 ) ) ;
#47154=VECTOR ( 'NONE', #61449, 1000.000000000000000 ) ;
#47173=CARTESIAN_POINT ( 'NONE',  ( 10.00000000000000000, 0.000000000000000000, 0.000000000000000000 ) ) ;
#47188=FACE_OUTER_BOUND ( 'NONE', #3007, .T. ) ;
#47189=CARTESIAN_POINT ( 'NONE',  ( 0.000000000000000000, 10.41901085202078292, 40.68715046381932865 ) ) ;
#47194=ORIENTED_EDGE ( 'NONE', *, *, #44194, .T. ) ;
#47198=EDGE_CURVE ( 'NONE', #15647, #26264, #59027, .T. ) ;
#47248=AXIS2_PLACEMENT_3D ( 'NONE', #22825, #16430, #26309 ) ;
#47249=DIRECTION ( 'NONE',  ( -1.000000000000000000, 0.000000000000000000, -0.000000000000000000 ) ) ;
#47257=CARTESIAN_POINT ( 'NONE',  ( 0.000000000000000000, -40.68715046381937128, 10.41901085202062660 ) ) ;
#47288=CYLINDRICAL_SURFACE ( 'NONE', #21596, 42.00000000000000000 ) ;
#47296=ORIENTED_EDGE ( 'NONE', *, *, #40493, .F. ) ;
#47298=CARTESIAN_POINT ( 'NONE',  ( 10.00000000000000000, 39.04073710021366139, -15.48615015657542848 ) ) ;
#47301=CARTESIAN_POINT ( 'NONE',  ( -10.00000000000000000, 0.000000000000000000, 0.000000000000000000 ) ) ;
#47309=DIRECTION ( 'NONE',  ( -1.000000000000000000, 0.000000000000000000, -0.000000000000000000 ) ) ;
#47355=FACE_OUTER_BOUND ( 'NONE', #44381, .T. ) ;
#47396=CARTESIAN_POINT ( 'NONE',  ( 0.000000000000000000, 22.48208911017551515, -35.47612816024499693 ) ) ;
#47398=DIRECTION ( 'NONE',  ( 1.000000000000000000, 0.000000000000000000, 0.000000000000000000 ) ) ;
#47423=VECTOR ( 'NONE', #6601, 1000.000000000000000 ) ;
#47436=ORIENTED_EDGE ( 'NONE', *, *, #56169, .T. ) ;
#47448=DIRECTION ( 'NONE',  ( -1.000000000000000000, 0.000000000000000000, 0.000000000000000000 ) ) ;
#47454=CARTESIAN_POINT ( 'NONE',  ( 0.000000000000000000, 0.000000000000000000, 0.000000000000000000 ) ) ;
#47458=ORIENTED_EDGE ( 'NONE', *, *, #62755, .T. ) ;
#47462=LINE ( 'NONE', #70370, #62332 ) ;
#47484=DIRECTION ( 'NONE',  ( -1.000000000000000000, 0.000000000000000000, -0.000000000000000000 ) ) ;
#47499=LINE ( 'NONE', #25672, #16621 ) ;
#47524=DIRECTION ( 'NONE',  ( 0.000000000000000000, 0.000000000000000000, -1.000000000000000000 ) ) ;
#47525=ORIENTED_EDGE ( 'NONE', *, *, #52508, .F. ) ;
#47533=ORIENTED_EDGE ( 'NONE', *, *, #70589, .F. ) ;
#47538=DIRECTION ( 'NONE',  ( -1.000000000000000000, -0.000000000000000000, 0.000000000000000000 ) ) ;
#47555=CARTESIAN_POINT ( 'NONE',  ( 0.000000000000000000, 0.000000000000000000, 0.000000000000000000 ) ) ;
#47593=ORIENTED_EDGE ( 'NONE', *, *, #14846, .F. ) ;
#47622=CARTESIAN_POINT ( 'NONE',  ( 0.000000000000000000, 27.05870788708267582, -26.08949754952995903 ) ) ;
#47636=ORIENTED_EDGE ( 'NONE', *, *, #31300, .T. ) ;
#47639=DIRECTION ( 'NONE',  ( 0.000000000000000000, 0.000000000000000000, 1.000000000000000000 ) ) ;
#47649=CARTESIAN_POINT ( 'NONE',  ( 0.000000000000000000, -32.34446384429989507, 26.79245525562703278 ) ) ;
#47651=CARTESIAN_POINT ( 'NONE',  ( -10.00000000000000000, 0.000000000000000000, 0.000000000000000000 ) ) ;
#47659=CARTESIAN_POINT ( 'NONE',  ( 10.00000000000000000, -16.23288003029521320, 33.80338159004277543 ) ) ;
#47664=DIRECTION ( 'NONE',  ( 1.000000000000000000, 0.000000000000000000, 0.000000000000000000 ) ) ;
#47685=EDGE_CURVE ( 'NONE', #30100, #18341, #10927, .T. ) ;
#47693=ORIENTED_EDGE ( 'NONE', *, *, #13143, .F. ) ;
#47696=ADVANCED_FACE ( 'NONE', ( #30620 ), #19715, .T. ) ;
#47714=VERTEX_POINT ( 'NONE', #73059 ) ;
#47743=CARTESIAN_POINT ( 'NONE',  ( 0.000000000000000000, -41.91543099594816368, -2.663952781846588014 ) ) ;
#47769=CARTESIAN_POINT ( 'NONE',  ( 0.000000000000000000, 0.000000000000000000, 0.000000000000000000 ) ) ;
#47773=EDGE_CURVE ( 'NONE', #18341, #44376, #31365, .T. ) ;
#47774=AXIS2_PLACEMENT_3D ( 'NONE', #34717, #189, #39995 ) ;
#47779=DIRECTION ( 'NONE',  ( -1.000000000000000000, 0.000000000000000000, -0.000000000000000000 ) ) ;
#47784=ORIENTED_EDGE ( 'NONE', *, *, #73019, .T. ) ;
#47801=ORIENTED_EDGE ( 'NONE', *, *, #47020, .T. ) ;
#47817=DIRECTION ( 'NONE',  ( 0.000000000000000000, 0.000000000000000000, 1.000000000000000000 ) ) ;
#47856=VECTOR ( 'NONE', #35037, 1000.000000000000000 ) ;
#47876=ORIENTED_EDGE ( 'NONE', *, *, #3514, .F. ) ;
#47880=CIRCLE ( 'NONE', #11802, 16.00000000000000000 ) ;
#47884=CIRCLE ( 'NONE', #10643, 16.00000000000000355 ) ;
#47891=VERTEX_POINT ( 'NONE', #12509 ) ;
#47897=ORIENTED_EDGE ( 'NONE', *, *, #54100, .T. ) ;
#47902=VERTEX_POINT ( 'NONE', #40724 ) ;
#47903=CIRCLE ( 'NONE', #25097, 16.00000000000000355 ) ;
#47932=FACE_OUTER_BOUND ( 'NONE', #44472, .T. ) ;
#47938=VERTEX_POINT ( 'NONE', #58756 ) ;
#47946=CARTESIAN_POINT ( 'NONE',  ( 5.000000000000000000, -27.75498641678764855, 31.52238457039590358 ) ) ;
#47968=AXIS2_PLACEMENT_3D ( 'NONE', #68727, #45428, #61970 ) ;
#47997=ORIENTED_EDGE ( 'NONE', *, *, #44913, .T. ) ;
#47998=DIRECTION ( 'NONE',  ( -1.000000000000000000, 0.000000000000000000, 0.000000000000000000 ) ) ;
#48005=ORIENTED_EDGE ( 'NONE', *, *, #51599, .F. ) ;
#48028=ORIENTED_EDGE ( 'NONE', *, *, #27922, .F. ) ;
#48031=VERTEX_POINT ( 'NONE', #29062 ) ;
#48040=ADVANCED_FACE ( 'NONE', ( #6514 ), #23435, .T. ) ;
#48048=ORIENTED_EDGE ( 'NONE', *, *, #37615, .T. ) ;
#48049=AXIS2_PLACEMENT_3D ( 'NONE', #68943, #18170, #57665 ) ;
#48060=DIRECTION ( 'NONE',  ( 0.000000000000000000, 0.000000000000000000, 1.000000000000000000 ) ) ;
#48061=VECTOR ( 'NONE', #65515, 1000.000000000000000 ) ;
#48067=VECTOR ( 'NONE', #574, 1000.000000000000000 ) ;
#48079=ORIENTED_EDGE ( 'NONE', *, *, #40057, .T. ) ;
#48080=DIRECTION ( 'NONE',  ( 0.000000000000000000, 0.5877852522924685852, 0.8090169943749508930 ) ) ;
#48081=SURFACE_STYLE_USAGE ( .BOTH. , #35324 ) ;
#48094=VERTEX_POINT ( 'NONE', #54229 ) ;
#48099=VECTOR ( 'NONE', #56660, 1000.000000000000000 ) ;
#48104=CARTESIAN_POINT ( 'NONE',  ( 10.00000000000000000, 22.74946021919133088, 29.81001611431016229 ) ) ;
#48105=DIRECTION ( 'NONE',  ( 0.000000000000000000, 0.000000000000000000, -1.000000000000000000 ) ) ;
#48124=DIRECTION ( 'NONE',  ( 0.000000000000000000, 0.000000000000000000, 1.000000000000000000 ) ) ;
#48138=DIRECTION ( 'NONE',  ( -1.000000000000000000, -0.000000000000000000, -0.000000000000000000 ) ) ;
#48150=LINE ( 'NONE', #15034, #37056 ) ;
#48182=ORIENTED_EDGE ( 'NONE', *, *, #37118, .T. ) ;
#48191=CARTESIAN_POINT ( 'NONE',  ( 0.000000000000000000, -39.04073710021356192, 15.48615015657568073 ) ) ;
#48207=EDGE_CURVE ( 'NONE', #48805, #29886, #7983, .T. ) ;
#48220=CIRCLE ( 'NONE', #52994, 16.00000000000000000 ) ;
#48248=CARTESIAN_POINT ( 'NONE',  ( 0.000000000000000000, 0.000000000000000000, 0.000000000000000000 ) ) ;
#48254=DIRECTION ( 'NONE',  ( 0.000000000000000000, 6.938893903907228378E-16, 1.000000000000000000 ) ) ;
#48259=VERTEX_POINT ( 'NONE', #66967 ) ;
#48263=EDGE_LOOP ( 'NONE', ( #68519, #28180, #57469, #13194 ) ) ;
#48280=LINE ( 'NONE', #55023, #67770 ) ;
#48296=DIRECTION ( 'NONE',  ( -1.000000000000000000, -0.000000000000000000, -0.000000000000000000 ) ) ;
#48300=DIRECTION ( 'NONE',  ( -1.000000000000000000, -0.000000000000000000, 0.000000000000000000 ) ) ;
#48314=AXIS2_PLACEMENT_3D ( 'NONE', #979, #52062, #23141 ) ;
#48320=CARTESIAN_POINT ( 'NONE',  ( 0.000000000000000000, 0.000000000000000000, 0.000000000000000000 ) ) ;
#48339=EDGE_LOOP ( 'NONE', ( #45455, #52057, #63557, #58061 ) ) ;
#48344=DIRECTION ( 'NONE',  ( -1.000000000000000000, -0.000000000000000000, -0.000000000000000000 ) ) ;
#48345=DIRECTION ( 'NONE',  ( 1.000000000000000000, -0.000000000000000000, 0.000000000000000000 ) ) ;
#48350=CYLINDRICAL_SURFACE ( 'NONE', #63385, 16.00000000000000000 ) ;
#48364=EDGE_CURVE ( 'NONE', #4011, #6866, #56067, .T. ) ;
#48396=EDGE_CURVE ( 'NONE', #30113, #62276, #28228, .T. ) ;
#48409=CARTESIAN_POINT ( 'NONE',  ( 4.999999999999999112, 40.98264845739749518, 9.188173127307448951 ) ) ;
#48424=DIRECTION ( 'NONE',  ( -1.000000000000000000, 0.000000000000000000, -0.000000000000000000 ) ) ;
#48441=VERTEX_POINT ( 'NONE', #45918 ) ;
#48446=CARTESIAN_POINT ( 'NONE',  ( 0.000000000000000000, -31.52238457039619490, 27.75498641678731104 ) ) ;
#48467=AXIS2_PLACEMENT_3D ( 'NONE', #8869, #31784, #42349 ) ;
#48470=ORIENTED_EDGE ( 'NONE', *, *, #59584, .T. ) ;
#48490=AXIS2_PLACEMENT_3D ( 'NONE', #42499, #42137, #54156 ) ;
#48510=VECTOR ( 'NONE', #27685, 1000.000000000000000 ) ;
#48522=DIRECTION ( 'NONE',  ( -1.000000000000000000, 0.000000000000000000, 0.000000000000000000 ) ) ;
#48537=FACE_OUTER_BOUND ( 'NONE', #18504, .T. ) ;
#48568=AXIS2_PLACEMENT_3D ( 'NONE', #35538, #6969, #34812 ) ;
#48575=DIRECTION ( 'NONE',  ( -1.000000000000000000, -0.000000000000000000, -0.000000000000000000 ) ) ;
#48586=DIRECTION ( 'NONE',  ( 0.000000000000000000, -0.3090169943749548342, 0.9510565162951511997 ) ) ;
#48594=ORIENTED_EDGE ( 'NONE', *, *, #44035, .F. ) ;
#48604=DIRECTION ( 'NONE',  ( -1.000000000000000000, 0.000000000000000000, 0.000000000000000000 ) ) ;
#48617=ADVANCED_FACE ( 'NONE', ( #73579 ), #10063, .T. ) ;
#48623=ORIENTED_EDGE ( 'NONE', *, *, #17470, .T. ) ;
#48627=VERTEX_POINT ( 'NONE', #45033 ) ;
#48642=VERTEX_POINT ( 'NONE', #68335 ) ;
#48643=ORIENTED_EDGE ( 'NONE', *, *, #41952, .F. ) ;
#48667=DIRECTION ( 'NONE',  ( 0.000000000000000000, 0.000000000000000000, -1.000000000000000000 ) ) ;
#48672=ORIENTED_EDGE ( 'NONE', *, *, #22530, .F. ) ;
#48678=CARTESIAN_POINT ( 'NONE',  ( 10.00000000000000000, 40.68715046381944234, -10.41901085202036192 ) ) ;
#48688=LINE ( 'NONE', #43449, #3417 ) ;
#48734=EDGE_CURVE ( 'NONE', #21818, #42186, #65146, .T. ) ;
#48735=ORIENTED_EDGE ( 'NONE', *, *, #67461, .F. ) ;
#48748=DIRECTION ( 'NONE',  ( -1.000000000000000000, 0.000000000000000000, 0.000000000000000000 ) ) ;
#48769=DIRECTION ( 'NONE',  ( -1.000000000000000000, -0.000000000000000000, -0.000000000000000000 ) ) ;
#48772=DIRECTION ( 'NONE',  ( 0.000000000000000000, 0.1564344650402242354, 0.9876883405951387696 ) ) ;
#48800=CARTESIAN_POINT ( 'NONE',  ( 10.00000000000000000, -30.84782396557233142, 21.32104025579104345 ) ) ;
#48803=CARTESIAN_POINT ( 'NONE',  ( 5.000000000000000000, 27.75498641678786527, -31.52238457039571173 ) ) ;
#48805=VERTEX_POINT ( 'NONE', #58904 ) ;
#48808=ADVANCED_FACE ( 'NONE', ( #49087 ), #19767, .T. ) ;
#48831=VECTOR ( 'NONE', #5957, 1000.000000000000000 ) ;
#48835=DIRECTION ( 'NONE',  ( 1.000000000000000000, 0.000000000000000000, 0.000000000000000000 ) ) ;
#48851=VECTOR ( 'NONE', #7834, 1000.000000000000000 ) ;
#48866=CARTESIAN_POINT ( 'NONE',  ( 4.999999999999999112, -3.925862922256468046, 41.81611651403860463 ) ) ;
#48883=DIRECTION ( 'NONE',  ( -1.000000000000000000, -0.000000000000000000, -0.000000000000000000 ) ) ;
#48887=ORIENTED_EDGE ( 'NONE', *, *, #46325, .F. ) ;
#48899=AXIS2_PLACEMENT_3D ( 'NONE', #30554, #57676, #41847 ) ;
#48907=DIRECTION ( 'NONE',  ( -1.000000000000000000, -0.000000000000000000, 0.000000000000000000 ) ) ;
#48935=ORIENTED_EDGE ( 'NONE', *, *, #18386, .T. ) ;
#48955=VECTOR ( 'NONE', #33512, 1000.000000000000000 ) ;
#48957=EDGE_CURVE ( 'NONE', #63727, #44099, #6330, .T. ) ;
#48968=AXIS2_PLACEMENT_3D ( 'NONE', #52915, #1083, #69819 ) ;
#48970=EDGE_CURVE ( 'NONE', #37974, #5960, #39919, .T. ) ;
#48983=ADVANCED_FACE ( 'NONE', ( #37779 ), #31003, .T. ) ;
#48997=EDGE_LOOP ( 'NONE', ( #47296, #9604, #47897, #14304 ) ) ;
#49000=VERTEX_POINT ( 'NONE', #20093 ) ;
#49017=ORIENTED_EDGE ( 'NONE', *, *, #18926, .F. ) ;
#49059=CIRCLE ( 'NONE', #22619, 37.49900000000001654 ) ;
#49070=ORIENTED_EDGE ( 'NONE', *, *, #65266, .F. ) ;
#49075=ORIENTED_EDGE ( 'NONE', *, *, #9417, .F. ) ;
#49077=AXIS2_PLACEMENT_3D ( 'NONE', #66285, #59907, #55355 ) ;
#49081=CIRCLE ( 'NONE', #22635, 16.00000000000000000 ) ;
#49087=FACE_OUTER_BOUND ( 'NONE', #39799, .T. ) ;
#49093=ORIENTED_EDGE ( 'NONE', *, *, #21437, .F. ) ;
#49094=DIRECTION ( 'NONE',  ( 0.000000000000000000, 0.000000000000000000, -1.000000000000000000 ) ) ;
#49102=AXIS2_PLACEMENT_3D ( 'NONE', #6141, #29772, #24520 ) ;
#49126=ADVANCED_FACE ( 'NONE', ( #54324 ), #36650, .F. ) ;
#49137=CIRCLE ( 'NONE', #58760, 42.00000000000000000 ) ;
#49143=CARTESIAN_POINT ( 'NONE',  ( 10.00000000000000000, 35.95386929396256903, -10.96151621346501237 ) ) ;
#49145=CIRCLE ( 'NONE', #32326, 42.00000000000000000 ) ;
#49169=VERTEX_POINT ( 'NONE', #72342 ) ;
#49178=CARTESIAN_POINT ( 'NONE',  ( 10.00000000000000000, 0.000000000000000000, 0.000000000000000000 ) ) ;
#49180=EDGE_LOOP ( 'NONE', ( #21597, #27520, #66500, #39123 ) ) ;
#49204=EDGE_CURVE ( 'NONE', #1611, #1093, #38509, .T. ) ;
#49214=AXIS2_PLACEMENT_3D ( 'NONE', #2826, #60323, #38486 ) ;
#49266=CARTESIAN_POINT ( 'NONE',  ( 4.999999999999999112, -9.188173127307004862, -40.98264845739759465 ) ) ;
#49281=ORIENTED_EDGE ( 'NONE', *, *, #11316, .T. ) ;
#49287=DIRECTION ( 'NONE',  ( 1.000000000000000000, 0.000000000000000000, 0.000000000000000000 ) ) ;
#49341=DIRECTION ( 'NONE',  ( 0.000000000000000000, 0.000000000000000000, 1.000000000000000000 ) ) ;
#49349=ORIENTED_EDGE ( 'NONE', *, *, #61366, .T. ) ;
#49383=DIRECTION ( 'NONE',  ( 0.000000000000000000, 0.000000000000000000, 1.000000000000000000 ) ) ;
#49412=DIRECTION ( 'NONE',  ( -1.000000000000000000, -0.000000000000000000, -0.000000000000000000 ) ) ;
#49443=DIRECTION ( 'NONE',  ( -1.000000000000000000, -0.000000000000000000, -0.000000000000000000 ) ) ;
#49485=FACE_OUTER_BOUND ( 'NONE', #43209, .T. ) ;
#49488=DIRECTION ( 'NONE',  ( 0.000000000000000000, -0.8090169943749403458, -0.5877852522924830181 ) ) ;
#49518=DIRECTION ( 'NONE',  ( -1.000000000000000000, 0.000000000000000000, -0.000000000000000000 ) ) ;
#49532=VERTEX_POINT ( 'NONE', #60529 ) ;
#49542=FACE_OUTER_BOUND ( 'NONE', #53003, .T. ) ;
#49583=CARTESIAN_POINT ( 'NONE',  ( -10.00000000000000000, 0.000000000000000000, 0.000000000000000000 ) ) ;
#49600=CARTESIAN_POINT ( 'NONE',  ( 10.00000000000000000, -37.22597642581153821, -5.202137450156795850 ) ) ;
#49624=EDGE_CURVE ( 'NONE', #58686, #60033, #73633, .T. ) ;
#49626=DIRECTION ( 'NONE',  ( -1.000000000000000000, 0.000000000000000000, 0.000000000000000000 ) ) ;
#49630=VERTEX_POINT ( 'NONE', #62389 ) ;
#49641=CIRCLE ( 'NONE', #47248, 16.00000000000000000 ) ;
#49665=DIRECTION ( 'NONE',  ( -1.000000000000000000, 0.000000000000000000, 0.000000000000000000 ) ) ;
#49693=AXIS2_PLACEMENT_3D ( 'NONE', #20768, #31309, #49341 ) ;
#49697=LINE ( 'NONE', #60278, #68214 ) ;
#49702=CIRCLE ( 'NONE', #48490, 16.00000000000000355 ) ;
#49713=ORIENTED_EDGE ( 'NONE', *, *, #67200, .T. ) ;
#49721=ORIENTED_EDGE ( 'NONE', *, *, #21023, .T. ) ;
#49724=CIRCLE ( 'NONE', #34129, 42.00000000000000000 ) ;
#49760=ADVANCED_FACE ( 'NONE', ( #58958 ), #59317, .T. ) ;
#49761=CARTESIAN_POINT ( 'NONE',  ( 10.00000000000000000, 33.79645857604513992, 16.45098606841138178 ) ) ;
#49798=EDGE_CURVE ( 'NONE', #51811, #8967, #50789, .T. ) ;
#49804=VERTEX_POINT ( 'NONE', #40547 ) ;
#49806=DIRECTION ( 'NONE',  ( 0.000000000000000000, 0.5877852522924741363, -0.8090169943749465631 ) ) ;
#49823=ORIENTED_EDGE ( 'NONE', *, *, #64451, .F. ) ;
#49824=ORIENTED_EDGE ( 'NONE', *, *, #39298, .F. ) ;
#49825=ORIENTED_EDGE ( 'NONE', *, *, #11795, .F. ) ;
#49831=FACE_OUTER_BOUND ( 'NONE', #60864, .T. ) ;
#49835=FACE_OUTER_BOUND ( 'NONE', #24244, .T. ) ;
#49848=CARTESIAN_POINT ( 'NONE',  ( 10.00000000000000000, 0.000000000000000000, 0.000000000000000000 ) ) ;
#49851=CARTESIAN_POINT ( 'NONE',  ( 10.00000000000000000, 0.000000000000000000, 0.000000000000000000 ) ) ;
#49855=VERTEX_POINT ( 'NONE', #12338 ) ;
#49894=CYLINDRICAL_SURFACE ( 'NONE', #50400, 37.49900000000000233 ) ;
#49904=DIRECTION ( 'NONE',  ( -1.000000000000000000, -0.000000000000000000, 0.000000000000000000 ) ) ;
#49911=VERTEX_POINT ( 'NONE', #61177 ) ;
#49916=EDGE_CURVE ( 'NONE', #25977, #30113, #19658, .T. ) ;
#49924=ORIENTED_EDGE ( 'NONE', *, *, #62327, .F. ) ;
#49928=AXIS2_PLACEMENT_3D ( 'NONE', #26479, #49412, #53953 ) ;
#49940=ORIENTED_EDGE ( 'NONE', *, *, #8574, .T. ) ;
#49951=CYLINDRICAL_SURFACE ( 'NONE', #38058, 16.00000000000000000 ) ;
#49964=EDGE_CURVE ( 'NONE', #21818, #49000, #61689, .T. ) ;
#49980=CARTESIAN_POINT ( 'NONE',  ( 10.00000000000000000, 0.000000000000000000, 0.000000000000000000 ) ) ;
#50021=DIRECTION ( 'NONE',  ( -1.000000000000000000, 0.000000000000000000, 0.000000000000000000 ) ) ;
#50024=ORIENTED_EDGE ( 'NONE', *, *, #1433, .T. ) ;
#50074=EDGE_CURVE ( 'NONE', #13831, #25323, #11248, .T. ) ;
#50076=DIRECTION ( 'NONE',  ( -1.000000000000000000, 0.000000000000000000, -0.000000000000000000 ) ) ;
#50084=ORIENTED_EDGE ( 'NONE', *, *, #36224, .T. ) ;
#50090=LINE ( 'NONE', #4641, #59984 ) ;
#50105=DIRECTION ( 'NONE',  ( -1.000000000000000000, -0.000000000000000000, -0.000000000000000000 ) ) ;
#50117=CARTESIAN_POINT ( 'NONE',  ( 0.000000000000000000, 37.48860685352291000, -0.8828120875901940279 ) ) ;
#50118=DIRECTION ( 'NONE',  ( -1.000000000000000000, 0.000000000000000000, 0.000000000000000000 ) ) ;
#50122=DIRECTION ( 'NONE',  ( -1.000000000000000000, 0.000000000000000000, -0.000000000000000000 ) ) ;
#50163=DIRECTION ( 'NONE',  ( 0.000000000000000000, 0.7071067811865487940, -0.7071067811865462405 ) ) ;
#50173=CIRCLE ( 'NONE', #71798, 37.49900000000001654 ) ;
#50182=ORIENTED_EDGE ( 'NONE', *, *, #29208, .T. ) ;
#50212=DIRECTION ( 'NONE',  ( -1.000000000000000000, 0.000000000000000000, 0.000000000000000000 ) ) ;
#50223=ADVANCED_FACE ( 'NONE', ( #56659 ), #5160, .T. ) ;
#50225=EDGE_CURVE ( 'NONE', #24060, #73031, #68675, .T. ) ;
#50227=DIRECTION ( 'NONE',  ( -1.000000000000000000, 0.000000000000000000, 0.000000000000000000 ) ) ;
#50245=CARTESIAN_POINT ( 'NONE',  ( 10.00000000000000000, -4.992566952384716927, -37.16516213103282951 ) ) ;
#50247=DIRECTION ( 'NONE',  ( 0.000000000000000000, 0.000000000000000000, 1.000000000000000000 ) ) ;
#50256=ADVANCED_FACE ( 'NONE', ( #11873 ), #6264, .T. ) ;
#50289=LINE ( 'NONE', #34121, #10103 ) ;
#50318=VECTOR ( 'NONE', #52232, 1000.000000000000000 ) ;
#50350=DIRECTION ( 'NONE',  ( -1.000000000000000000, 0.000000000000000000, 0.000000000000000000 ) ) ;
#50357=CARTESIAN_POINT ( 'NONE',  ( 0.000000000000000000, 12.24744871391588852, 2.500000000000003553 ) ) ;
#50371=CARTESIAN_POINT ( 'NONE',  ( 0.000000000000000000, -22.64427369931148348, -30.00120703465229965 ) ) ;
#50375=ORIENTED_EDGE ( 'NONE', *, *, #1804, .T. ) ;
#50384=CARTESIAN_POINT ( 'NONE',  ( 10.00000000000000000, 0.000000000000000000, 0.000000000000000000 ) ) ;
#50400=AXIS2_PLACEMENT_3D ( 'NONE', #73566, #10419, #61569 ) ;
#50408=VERTEX_POINT ( 'NONE', #3225 ) ;
#50420=AXIS2_PLACEMENT_3D ( 'NONE', #39084, #16894, #34538 ) ;
#50425=ORIENTED_EDGE ( 'NONE', *, *, #71604, .F. ) ;
#50426=DIRECTION ( 'NONE',  ( -1.000000000000000000, -0.000000000000000000, -0.000000000000000000 ) ) ;
#50460=DIRECTION ( 'NONE',  ( 0.000000000000000000, 0.8090169943749487835, -0.5877852522924713607 ) ) ;
#50488=VERTEX_POINT ( 'NONE', #66363 ) ;
#50496=DIRECTION ( 'NONE',  ( -1.000000000000000000, -0.000000000000000000, 0.000000000000000000 ) ) ;
#50530=AXIS2_PLACEMENT_3D ( 'NONE', #58661, #1202, #1930 ) ;
#50543=ORIENTED_EDGE ( 'NONE', *, *, #53137, .T. ) ;
#50562=CARTESIAN_POINT ( 'NONE',  ( 4.999999999999999112, 9.188173127307294408, 40.98264845739752360 ) ) ;
#50587=EDGE_LOOP ( 'NONE', ( #63743, #38161, #2349, #8494 ) ) ;
#50596=DIRECTION ( 'NONE',  ( -1.000000000000000000, 0.000000000000000000, 0.000000000000000000 ) ) ;
#50604=ADVANCED_FACE ( 'NONE', ( #56937 ), #67459, .T. ) ;
#50614=DIRECTION ( 'NONE',  ( 0.000000000000000000, -1.776356839400250465E-15, -1.000000000000000000 ) ) ;
#50618=DIRECTION ( 'NONE',  ( 0.000000000000000000, 0.000000000000000000, -1.000000000000000000 ) ) ;
#50631=CARTESIAN_POINT ( 'NONE',  ( 10.00000000000000000, -37.22597642581153821, 10.79786254984320415 ) ) ;
#50646=ORIENTED_EDGE ( 'NONE', *, *, #3327, .F. ) ;
#50677=CIRCLE ( 'NONE', #45878, 15.99999999999999822 ) ;
#50695=ORIENTED_EDGE ( 'NONE', *, *, #39539, .T. ) ;
#50725=DIRECTION ( 'NONE',  ( -1.000000000000000000, 0.000000000000000000, 0.000000000000000000 ) ) ;
#50728=DIRECTION ( 'NONE',  ( -1.000000000000000000, 0.000000000000000000, 0.000000000000000000 ) ) ;
#50738=ORIENTED_EDGE ( 'NONE', *, *, #13521, .F. ) ;
#50742=DIRECTION ( 'NONE',  ( -1.000000000000000000, -0.000000000000000000, -0.000000000000000000 ) ) ;
#50771=ORIENTED_EDGE ( 'NONE', *, *, #44815, .F. ) ;
#50774=CARTESIAN_POINT ( 'NONE',  ( 10.00000000000000000, 37.58145647212453611, 0.6853352020791767529 ) ) ;
#50782=ORIENTED_EDGE ( 'NONE', *, *, #40000, .F. ) ;
#50789=CIRCLE ( 'NONE', #18368, 42.00000000000000000 ) ;
#50805=DIRECTION ( 'NONE',  ( 0.000000000000000000, 0.000000000000000000, 1.000000000000000000 ) ) ;
#50818=EDGE_CURVE ( 'NONE', #70509, #7952, #46131, .T. ) ;
#50829=CARTESIAN_POINT ( 'NONE',  ( 0.000000000000000000, -33.00180498840060039, 17.80606268964528027 ) ) ;
#50831=VECTOR ( 'NONE', #22446, 1000.000000000000000 ) ;
#50864=CARTESIAN_POINT ( 'NONE',  ( 10.00000000000000000, 0.000000000000000000, 0.000000000000000000 ) ) ;
#50867=CARTESIAN_POINT ( 'NONE',  ( 0.000000000000000000, 0.000000000000000000, 0.000000000000000000 ) ) ;
#50882=DIRECTION ( 'NONE',  ( 1.000000000000000000, 0.000000000000000000, -0.000000000000000000 ) ) ;
#50897=FACE_OUTER_BOUND ( 'NONE', #16113, .T. ) ;
#50934=ORIENTED_EDGE ( 'NONE', *, *, #71466, .T. ) ;
#50955=CARTESIAN_POINT ( 'NONE',  ( -10.00000000000000000, 0.000000000000000000, 0.000000000000000000 ) ) ;
#50972=DIRECTION ( 'NONE',  ( -1.000000000000000000, 0.000000000000000000, -0.000000000000000000 ) ) ;
#50977=ORIENTED_EDGE ( 'NONE', *, *, #57315, .F. ) ;
#50990=ORIENTED_EDGE ( 'NONE', *, *, #42788, .F. ) ;
#50993=CARTESIAN_POINT ( 'NONE',  ( 10.00000000000000000, -25.88420570971381807, -27.13269053701123212 ) ) ;
#51014=LINE ( 'NONE', #73935, #50831 ) ;
#51024=CARTESIAN_POINT ( 'NONE',  ( 10.00000000000000000, 35.95386929396241271, 10.96151621346552751 ) ) ;
#51039=ORIENTED_EDGE ( 'NONE', *, *, #35123, .F. ) ;
#51042=CARTESIAN_POINT ( 'NONE',  ( 10.00000000000000000, 35.92658777277511462, 10.74501242461295014 ) ) ;
#51059=CYLINDRICAL_SURFACE ( 'NONE', #65425, 37.49900000000000233 ) ;
#51075=VERTEX_POINT ( 'NONE', #44817 ) ;
#51096=EDGE_CURVE ( 'NONE', #61856, #27431, #59222, .T. ) ;
#51113=VERTEX_POINT ( 'NONE', #43712 ) ;
#51119=DIRECTION ( 'NONE',  ( 0.000000000000000000, 0.000000000000000000, 1.000000000000000000 ) ) ;
#51123=ORIENTED_EDGE ( 'NONE', *, *, #67071, .F. ) ;
#51124=DIRECTION ( 'NONE',  ( 0.000000000000000000, -0.9876883405951393247, 0.1564344650402205161 ) ) ;
#51127=SURFACE_STYLE_FILL_AREA ( #11274 ) ;
#51133=ORIENTED_EDGE ( 'NONE', *, *, #18386, .F. ) ;
#51170=PLANE ( 'NONE',  #13052 ) ;
#51178=CARTESIAN_POINT ( 'NONE',  ( 10.00000000000000000, 0.6853352020790449695, 37.58145647212454321 ) ) ;
#51186=DIRECTION ( 'NONE',  ( 0.000000000000000000, -0.7071067811865536790, 0.7071067811865413555 ) ) ;
#51197=CARTESIAN_POINT ( 'NONE',  ( 10.00000000000000178, 0.000000000000000000, 0.000000000000000000 ) ) ;
#51203=DIRECTION ( 'NONE',  ( -1.000000000000000000, -0.000000000000000000, -0.000000000000000000 ) ) ;
#51223=CARTESIAN_POINT ( 'NONE',  ( 10.00000000000000000, 9.188173127307297960, 40.98264845739753071 ) ) ;
#51225=ORIENTED_EDGE ( 'NONE', *, *, #2853, .F. ) ;
#51273=CYLINDRICAL_SURFACE ( 'NONE', #28514, 16.00000000000000000 ) ;
#51292=VERTEX_POINT ( 'NONE', #65445 ) ;
#51310=VERTEX_POINT ( 'NONE', #19921 ) ;
#51314=DIRECTION ( 'NONE',  ( 0.000000000000000000, 0.000000000000000000, 1.000000000000000000 ) ) ;
#51318=CARTESIAN_POINT ( 'NONE',  ( 10.00000000000000000, 0.6853352020795618893, -37.58145647212453611 ) ) ;
#51325=ORIENTED_EDGE ( 'NONE', *, *, #33723, .F. ) ;
#51353=ORIENTED_EDGE ( 'NONE', *, *, #72032, .T. ) ;
#51363=CARTESIAN_POINT ( 'NONE',  ( 0.000000000000000000, -21.32104025579135964, 30.84782396557210760 ) ) ;
#51378=DIRECTION ( 'NONE',  ( -1.000000000000000000, -0.000000000000000000, -0.000000000000000000 ) ) ;
#51388=CIRCLE ( 'NONE', #63434, 15.99999999999999822 ) ;
#51421=CARTESIAN_POINT ( 'NONE',  ( 5.000000000000000000, 35.47612816024523852, 22.48208911017513145 ) ) ;
#51425=CARTESIAN_POINT ( 'NONE',  ( 10.00000000000000000, -40.68715046381937128, 10.41901085202062660 ) ) ;
#51436=CARTESIAN_POINT ( 'NONE',  ( 0.000000000000000000, 0.000000000000000000, 0.000000000000000000 ) ) ;
#51442=EDGE_CURVE ( 'NONE', #44231, #48627, #49641, .T. ) ;
#51443=DIRECTION ( 'NONE',  ( 0.000000000000000000, -0.9876883405951358830, -0.1564344650402421932 ) ) ;
#51448=AXIS2_PLACEMENT_3D ( 'NONE', #67500, #44949, #67871 ) ;
#51469=VECTOR ( 'NONE', #55400, 1000.000000000000000 ) ;
#51471=ORIENTED_EDGE ( 'NONE', *, *, #6066, .T. ) ;
#51497=VECTOR ( 'NONE', #36490, 1000.000000000000000 ) ;
#51516=DIRECTION ( 'NONE',  ( -1.000000000000000000, 0.000000000000000000, -0.000000000000000000 ) ) ;
#51520=VERTEX_POINT ( 'NONE', #50631 ) ;
#51521=DIRECTION ( 'NONE',  ( 0.000000000000000000, 0.000000000000000000, -1.000000000000000000 ) ) ;
#51537=CIRCLE ( 'NONE', #8276, 16.00000000000000000 ) ;
#51543=AXIS2_PLACEMENT_3D ( 'NONE', #49980, #56391, #67663 ) ;
#51548=CARTESIAN_POINT ( 'NONE',  ( 10.00000000000000000, 0.000000000000000000, 0.000000000000000000 ) ) ;
#51553=AXIS2_PLACEMENT_3D ( 'NONE', #51436, #11577, #39803 ) ;
#51563=AXIS2_PLACEMENT_3D ( 'NONE', #13189, #12810, #53053 ) ;
#51588=VERTEX_POINT ( 'NONE', #45014 ) ;
#51589=CIRCLE ( 'NONE', #59989, 16.00000000000000000 ) ;
#51599=EDGE_CURVE ( 'NONE', #4312, #24083, #51014, .T. ) ;
#51632=EDGE_CURVE ( 'NONE', #10248, #52892, #58130, .T. ) ;
#51646=ORIENTED_EDGE ( 'NONE', *, *, #61563, .T. ) ;
#51655=AXIS2_PLACEMENT_3D ( 'NONE', #60139, #62745, #39047 ) ;
#51661=CIRCLE ( 'NONE', #13224, 37.49900000000001654 ) ;
#51667=AXIS2_PLACEMENT_3D ( 'NONE', #28653, #63266, #70344 ) ;
#51671=ORIENTED_EDGE ( 'NONE', *, *, #20547, .F. ) ;
#51673=VERTEX_POINT ( 'NONE', #35197 ) ;
#51721=DIRECTION ( 'NONE',  ( 1.000000000000000000, -0.000000000000000000, -0.000000000000000000 ) ) ;
#51729=AXIS2_PLACEMENT_3D ( 'NONE', #57547, #12039, #18057 ) ;
#51732=CARTESIAN_POINT ( 'NONE',  ( 0.000000000000000000, 31.52238457039599595, 27.75498641678753842 ) ) ;
#51745=DIRECTION ( 'NONE',  ( -1.000000000000000000, -0.000000000000000000, -0.000000000000000000 ) ) ;
#51754=AXIS2_PLACEMENT_3D ( 'NONE', #32485, #43437, #21196 ) ;
#51761=CIRCLE ( 'NONE', #36135, 42.00000000000000000 ) ;
#51795=ORIENTED_EDGE ( 'NONE', *, *, #71382, .T. ) ;
#51799=EDGE_LOOP ( 'NONE', ( #23956, #13846, #19037, #31737 ) ) ;
#51811=VERTEX_POINT ( 'NONE', #42330 ) ;
#51815=ORIENTED_EDGE ( 'NONE', *, *, #16892, .T. ) ;
#51833=DIRECTION ( 'NONE',  ( 0.000000000000000000, 0.3090169943749411230, 0.9510565162951555296 ) ) ;
#51849=CARTESIAN_POINT ( 'NONE',  ( 10.00000000000000000, 0.000000000000000000, 0.000000000000000000 ) ) ;
#51866=ORIENTED_EDGE ( 'NONE', *, *, #25697, .T. ) ;
#51900=ORIENTED_EDGE ( 'NONE', *, *, #737, .T. ) ;
#51909=CARTESIAN_POINT ( 'NONE',  ( 0.000000000000000000, -33.00180498840035170, -17.80606268964575278 ) ) ;
#51914=EDGE_CURVE ( 'NONE', #19251, #35508, #19650, .T. ) ;
#51916=DIRECTION ( 'NONE',  ( -1.000000000000000000, 0.000000000000000000, 0.000000000000000000 ) ) ;
#51929=EDGE_CURVE ( 'NONE', #1611, #19251, #18469, .T. ) ;
#52016=VECTOR ( 'NONE', #48345, 1000.000000000000000 ) ;
#52022=EDGE_CURVE ( 'NONE', #68267, #26992, #71263, .T. ) ;
#52029=CARTESIAN_POINT ( 'NONE',  ( -10.00000000000000000, 0.000000000000000000, 0.000000000000000000 ) ) ;
#52043=CARTESIAN_POINT ( 'NONE',  ( 0.000000000000000000, -37.22597642581153821, -5.202137450156795850 ) ) ;
#52052=VECTOR ( 'NONE', #58780, 1000.000000000000000 ) ;
#52056=VERTEX_POINT ( 'NONE', #53143 ) ;
#52057=ORIENTED_EDGE ( 'NONE', *, *, #8159, .F. ) ;
#52061=CARTESIAN_POINT ( 'NONE',  ( 10.00000000000000000, 35.38097989696528600, -12.42422080174602605 ) ) ;
#52062=DIRECTION ( 'NONE',  ( -1.000000000000000000, -0.000000000000000000, 0.000000000000000000 ) ) ;
#52065=LINE ( 'NONE', #608, #43199 ) ;
#52071=ORIENTED_EDGE ( 'NONE', *, *, #4889, .F. ) ;
#52084=DIRECTION ( 'NONE',  ( 0.000000000000000000, -0.7071067811865389130, -0.7071067811865563435 ) ) ;
#52122=CIRCLE ( 'NONE', #34152, 37.49900000000000233 ) ;
#52126=EDGE_LOOP ( 'NONE', ( #21079, #40716, #58547, #50024 ) ) ;
#52131=CARTESIAN_POINT ( 'NONE',  ( 10.00000000000000000, 0.000000000000000000, 0.000000000000000000 ) ) ;
#52142=ORIENTED_EDGE ( 'NONE', *, *, #36078, .T. ) ;
#52143=VERTEX_POINT ( 'NONE', #66284 ) ;
#52145=EDGE_LOOP ( 'NONE', ( #29018, #778, #34131, #47194 ) ) ;
#52158=VERTEX_POINT ( 'NONE', #8760 ) ;
#52163=LINE ( 'NONE', #34885, #9372 ) ;
#52164=DIRECTION ( 'NONE',  ( -1.000000000000000000, 0.000000000000000000, 0.000000000000000000 ) ) ;
#52167=ORIENTED_EDGE ( 'NONE', *, *, #17071, .F. ) ;
#52168=CARTESIAN_POINT ( 'NONE',  ( 4.999999999999999112, -40.68715046381937128, 10.41901085202062660 ) ) ;
#52186=EDGE_CURVE ( 'NONE', #20082, #48441, #7695, .T. ) ;
#52221=EDGE_LOOP ( 'NONE', ( #55217, #8228, #70382, #52544 ) ) ;
#52224=ORIENTED_EDGE ( 'NONE', *, *, #72615, .F. ) ;
#52229=VECTOR ( 'NONE', #27841, 1000.000000000000000 ) ;
#52232=DIRECTION ( 'NONE',  ( -1.000000000000000000, 0.000000000000000000, 0.000000000000000000 ) ) ;
#52233=ORIENTED_EDGE ( 'NONE', *, *, #43294, .T. ) ;
#52237=( NAMED_UNIT ( * ) SI_UNIT ( $, .STERADIAN. ) SOLID_ANGLE_UNIT ( ) );
#52259=ORIENTED_EDGE ( 'NONE', *, *, #14935, .F. ) ;
#52260=DIRECTION ( 'NONE',  ( 1.000000000000000000, 0.000000000000000000, 0.000000000000000000 ) ) ;
#52264=VERTEX_POINT ( 'NONE', #22260 ) ;
#52278=CARTESIAN_POINT ( 'NONE',  ( 10.00000000000000000, 0.000000000000000000, 0.000000000000000000 ) ) ;
#52281=DIRECTION ( 'NONE',  ( 0.000000000000000000, 0.8090169943749486725, -0.5877852522924713607 ) ) ;
#52284=LINE ( 'NONE', #70294, #9144 ) ;
#52301=EDGE_CURVE ( 'NONE', #40680, #69529, #73741, .T. ) ;
#52354=AXIS2_PLACEMENT_3D ( 'NONE', #6433, #58660, #7163 ) ;
#52363=DIRECTION ( 'NONE',  ( 0.000000000000000000, 0.000000000000000000, 1.000000000000000000 ) ) ;
#52365=DIRECTION ( 'NONE',  ( -1.000000000000000000, 0.000000000000000000, 0.000000000000000000 ) ) ;
#52366=ORIENTED_EDGE ( 'NONE', *, *, #52982, .F. ) ;
#52397=LINE ( 'NONE', #5822, #48067 ) ;
#52420=ORIENTED_EDGE ( 'NONE', *, *, #62481, .T. ) ;
#52428=CARTESIAN_POINT ( 'NONE',  ( 10.00000000000000000, -22.74946021919153694, 29.81001611431000597 ) ) ;
#52431=ORIENTED_EDGE ( 'NONE', *, *, #8247, .T. ) ;
#52432=EDGE_CURVE ( 'NONE', #63446, #1614, #60564, .T. ) ;
#52488=AXIS2_PLACEMENT_3D ( 'NONE', #53006, #68454, #12397 ) ;
#52493=ORIENTED_EDGE ( 'NONE', *, *, #15714, .T. ) ;
#52503=VERTEX_POINT ( 'NONE', #35023 ) ;
#52508=EDGE_CURVE ( 'NONE', #44376, #24421, #6097, .T. ) ;
#52512=EDGE_CURVE ( 'NONE', #63103, #27431, #46306, .T. ) ;
#52522=ORIENTED_EDGE ( 'NONE', *, *, #42222, .F. ) ;
#52527=EDGE_LOOP ( 'NONE', ( #45423, #62905, #56459, #70787 ) ) ;
#52528=CYLINDRICAL_SURFACE ( 'NONE', #48968, 16.00000000000000000 ) ;
#52544=ORIENTED_EDGE ( 'NONE', *, *, #65343, .T. ) ;
#52560=DIRECTION ( 'NONE',  ( -1.000000000000000000, 0.000000000000000000, 0.000000000000000000 ) ) ;
#52565=LINE ( 'NONE', #1118, #26308 ) ;
#52594=AXIS2_PLACEMENT_3D ( 'NONE', #37878, #26208, #9290 ) ;
#52603=( NAMED_UNIT ( * ) PLANE_ANGLE_UNIT ( ) SI_UNIT ( $, .RADIAN. ) );
#52631=CIRCLE ( 'NONE', #3441, 16.00000000000000355 ) ;
#52643=CARTESIAN_POINT ( 'NONE',  ( 10.00000000000000000, 0.000000000000000000, 0.000000000000000000 ) ) ;
#52645=DIRECTION ( 'NONE',  ( -1.000000000000000000, 0.000000000000000000, 0.000000000000000000 ) ) ;
#52651=CARTESIAN_POINT ( 'NONE',  ( 0.000000000000000000, 37.01155633439068282, -6.555932627142014191 ) ) ;
#52679=AXIS2_PLACEMENT_3D ( 'NONE', #58706, #53070, #29380 ) ;
#52684=FACE_OUTER_BOUND ( 'NONE', #49180, .T. ) ;
#52721=AXIS2_PLACEMENT_3D ( 'NONE', #37896, #13467, #48060 ) ;
#52744=ORIENTED_EDGE ( 'NONE', *, *, #6206, .T. ) ;
#52756=DIRECTION ( 'NONE',  ( -1.000000000000000000, -0.000000000000000000, 0.000000000000000000 ) ) ;
#52757=CARTESIAN_POINT ( 'NONE',  ( 10.00000000000000000, -30.00120703465189465, -22.64427369931201639 ) ) ;
#52771=AXIS2_PLACEMENT_3D ( 'NONE', #55752, #27543, #72646 ) ;
#52787=DIRECTION ( 'NONE',  ( -1.000000000000000000, 0.000000000000000000, -0.000000000000000000 ) ) ;
#52792=AXIS2_PLACEMENT_3D ( 'NONE', #1186, #13877, #12408 ) ;
#52804=EDGE_CURVE ( 'NONE', #23577, #19685, #33060, .T. ) ;
#52815=DIRECTION ( 'NONE',  ( 0.000000000000000000, 0.000000000000000000, 1.000000000000000000 ) ) ;
#52846=ORIENTED_EDGE ( 'NONE', *, *, #73074, .F. ) ;
#52865=ORIENTED_EDGE ( 'NONE', *, *, #25951, .T. ) ;
#52875=VERTEX_POINT ( 'NONE', #10510 ) ;
#52880=CARTESIAN_POINT ( 'NONE',  ( 10.00000000000000000, 35.38097989696512968, 12.42422080174651100 ) ) ;
#52887=CARTESIAN_POINT ( 'NONE',  ( 0.000000000000000000, 0.6853352020790449695, 37.58145647212454321 ) ) ;
#52892=VERTEX_POINT ( 'NONE', #12359 ) ;
#52900=DIRECTION ( 'NONE',  ( -1.000000000000000000, 0.000000000000000000, 0.000000000000000000 ) ) ;
#52907=ORIENTED_EDGE ( 'NONE', *, *, #54428, .T. ) ;
#52915=CARTESIAN_POINT ( 'NONE',  ( 10.00000000000000000, -33.79645857604525361, 16.45098606841114730 ) ) ;
#52937=CYLINDRICAL_SURFACE ( 'NONE', #69345, 16.00000000000000000 ) ;
#52952=AXIS2_PLACEMENT_3D ( 'NONE', #55041, #3570, #42302 ) ;
#52953=CARTESIAN_POINT ( 'NONE',  ( 5.000000000000000000, 39.04073710021366139, -15.48615015657542138 ) ) ;
#52964=CARTESIAN_POINT ( 'NONE',  ( 10.00000000000000000, -15.48615015657610883, 39.04073710021339139 ) ) ;
#52980=ORIENTED_EDGE ( 'NONE', *, *, #12496, .T. ) ;
#52982=EDGE_CURVE ( 'NONE', #44827, #49630, #33008, .T. ) ;
#52994=AXIS2_PLACEMENT_3D ( 'NONE', #8536, #60053, #71291 ) ;
#53003=EDGE_LOOP ( 'NONE', ( #63818, #8045, #2363, #53569 ) ) ;
#53006=CARTESIAN_POINT ( 'NONE',  ( 10.00000000000000000, -0.6853352020793173072, 37.58145647212453611 ) ) ;
#53017=DIRECTION ( 'NONE',  ( -1.000000000000000000, 0.000000000000000000, 0.000000000000000000 ) ) ;
#53037=DIRECTION ( 'NONE',  ( 0.000000000000000000, 0.000000000000000000, -1.000000000000000000 ) ) ;
#53053=DIRECTION ( 'NONE',  ( 0.000000000000000000, 0.000000000000000000, 1.000000000000000000 ) ) ;
#53068=DIRECTION ( 'NONE',  ( -1.000000000000000000, 0.000000000000000000, 0.000000000000000000 ) ) ;
#53070=DIRECTION ( 'NONE',  ( -1.000000000000000000, 0.000000000000000000, 0.000000000000000000 ) ) ;
#53071=EDGE_LOOP ( 'NONE', ( #13315, #16532, #28692, #20529 ) ) ;
#53075=VERTEX_POINT ( 'NONE', #56645 ) ;
#53083=FACE_OUTER_BOUND ( 'NONE', #59352, .T. ) ;
#53089=DIRECTION ( 'NONE',  ( -1.000000000000000000, -0.000000000000000000, 0.000000000000000000 ) ) ;
#53097=CYLINDRICAL_SURFACE ( 'NONE', #49102, 37.49900000000000233 ) ;
#53111=CARTESIAN_POINT ( 'NONE',  ( 10.00000000000000000, 27.75498641678742473, 31.52238457039609898 ) ) ;
#53119=DIRECTION ( 'NONE',  ( -1.000000000000000000, -0.000000000000000000, -0.000000000000000000 ) ) ;
#53137=EDGE_CURVE ( 'NONE', #21499, #64024, #21669, .T. ) ;
#53143=CARTESIAN_POINT ( 'NONE',  ( 10.00000000000000000, -22.74946021919110706, -29.81001611431033282 ) ) ;
#53144=DIRECTION ( 'NONE',  ( -1.000000000000000000, -0.000000000000000000, -0.000000000000000000 ) ) ;
#53154=DIRECTION ( 'NONE',  ( -1.000000000000000000, 0.000000000000000000, 0.000000000000000000 ) ) ;
#53160=DIRECTION ( 'NONE',  ( 0.000000000000000000, -0.4539904997395352027, -0.8910065241883737830 ) ) ;
#53173=EDGE_LOOP ( 'NONE', ( #42992, #74158, #13571, #35210 ) ) ;
#53203=VERTEX_POINT ( 'NONE', #51732 ) ;
#53209=DIRECTION ( 'NONE',  ( 0.000000000000000000, 0.000000000000000000, 1.000000000000000000 ) ) ;
#53246=FACE_OUTER_BOUND ( 'NONE', #54714, .T. ) ;
#53248=ORIENTED_EDGE ( 'NONE', *, *, #71466, .F. ) ;
#53259=ORIENTED_EDGE ( 'NONE', *, *, #10890, .T. ) ;
#53300=ADVANCED_FACE ( 'NONE', ( #53246 ), #35574, .T. ) ;
#53308=FACE_OUTER_BOUND ( 'NONE', #71094, .T. ) ;
#53325=ORIENTED_EDGE ( 'NONE', *, *, #7805, .T. ) ;
#53338=CARTESIAN_POINT ( 'NONE',  ( 10.00000000000000000, 0.000000000000000000, 0.000000000000000000 ) ) ;
#53345=VERTEX_POINT ( 'NONE', #52880 ) ;
#53360=AXIS2_PLACEMENT_3D ( 'NONE', #62882, #18457, #17719 ) ;
#53367=AXIS2_PLACEMENT_3D ( 'NONE', #57860, #39460, #68025 ) ;
#53391=CIRCLE ( 'NONE', #20959, 37.49900000000000944 ) ;
#53392=EDGE_CURVE ( 'NONE', #47001, #6488, #35439, .T. ) ;
#53408=DIRECTION ( 'NONE',  ( 0.000000000000000000, 0.000000000000000000, 1.000000000000000000 ) ) ;
#53419=CARTESIAN_POINT ( 'NONE',  ( 5.000000000000000000, -32.34446384429989507, 26.79245525562703278 ) ) ;
#53437=VERTEX_POINT ( 'NONE', #6643 ) ;
#53444=ORIENTED_EDGE ( 'NONE', *, *, #64443, .T. ) ;
#53445=DIRECTION ( 'NONE',  ( -1.000000000000000000, -0.000000000000000000, -0.000000000000000000 ) ) ;
#53451=ORIENTED_EDGE ( 'NONE', *, *, #40248, .T. ) ;
#53492=LINE ( 'NONE', #18169, #26519 ) ;
#53497=VECTOR ( 'NONE', #50122, 1000.000000000000000 ) ;
#53513=CARTESIAN_POINT ( 'NONE',  ( 10.00000000000000178, 0.000000000000000000, 0.000000000000000000 ) ) ;
#53519=DIRECTION ( 'NONE',  ( 0.000000000000000000, 0.9876883405951382144, -0.1564344650402276493 ) ) ;
#53523=ORIENTED_EDGE ( 'NONE', *, *, #18997, .T. ) ;
#53526=ORIENTED_EDGE ( 'NONE', *, *, #45576, .T. ) ;
#53546=EDGE_CURVE ( 'NONE', #14214, #49169, #32792, .T. ) ;
#53549=DIRECTION ( 'NONE',  ( -1.000000000000000000, -0.000000000000000000, -0.000000000000000000 ) ) ;
#53558=ORIENTED_EDGE ( 'NONE', *, *, #60951, .F. ) ;
#53562=DIRECTION ( 'NONE',  ( 0.000000000000000000, 0.1564344650402243742, 0.9876883405951387696 ) ) ;
#53566=CARTESIAN_POINT ( 'NONE',  ( 10.00000000000000000, 37.22597642581158084, -5.202137450156524068 ) ) ;
#53569=ORIENTED_EDGE ( 'NONE', *, *, #28711, .T. ) ;
#53580=EDGE_CURVE ( 'NONE', #58797, #67105, #65688, .T. ) ;
#53581=EDGE_CURVE ( 'NONE', #37368, #67705, #21227, .T. ) ;
#53590=CARTESIAN_POINT ( 'NONE',  ( 10.00000000000000000, -27.05870788708250885, 26.08949754953014022 ) ) ;
#53593=AXIS2_PLACEMENT_3D ( 'NONE', #52278, #12423, #18430 ) ;
#53607=CARTESIAN_POINT ( 'NONE',  ( 10.00000000000000000, 27.05870788708267582, -26.08949754952995903 ) ) ;
#53609=ORIENTED_EDGE ( 'NONE', *, *, #25199, .F. ) ;
#53611=CARTESIAN_POINT ( 'NONE',  ( -1.200000000000000030E-05, 0.9569279952884557350, -2.499999999999984457 ) ) ;
#53614=DIRECTION ( 'NONE',  ( 1.000000000000000000, 0.000000000000000000, -0.000000000000000000 ) ) ;
#53618=CIRCLE ( 'NONE', #2042, 16.00000000000000000 ) ;
#53633=LINE ( 'NONE', #59280, #12520 ) ;
#53669=CARTESIAN_POINT ( 'NONE',  ( 10.00000000000000000, -5.202137450156655518, 37.22597642581156663 ) ) ;
#53671=CARTESIAN_POINT ( 'NONE',  ( 5.000000000000000000, 36.13751322684419165, 21.40280677340384585 ) ) ;
#53674=CARTESIAN_POINT ( 'NONE',  ( 10.00000000000000000, -30.80686688397025108, 21.53537804866070715 ) ) ;
#53680=CARTESIAN_POINT ( 'NONE',  ( -10.00000000000000000, 0.000000000000000000, 0.000000000000000000 ) ) ;
#53681=AXIS2_PLACEMENT_3D ( 'NONE', #67323, #27085, #15827 ) ;
#53691=EDGE_LOOP ( 'NONE', ( #37380, #43587, #70079, #72203 ) ) ;
#53701=VECTOR ( 'NONE', #14234, 1000.000000000000000 ) ;
#53714=CARTESIAN_POINT ( 'NONE',  ( 10.00000000000000000, -17.67226234102849958, 33.17418723428301774 ) ) ;
#53721=CARTESIAN_POINT ( 'NONE',  ( 10.00000000000000000, -10.74501242461308159, 35.92658777277507909 ) ) ;
#53755=DIRECTION ( 'NONE',  ( 0.000000000000000000, 0.000000000000000000, 1.000000000000000000 ) ) ;
#53763=DIRECTION ( 'NONE',  ( -1.000000000000000000, 0.000000000000000000, 0.000000000000000000 ) ) ;
#53777=CARTESIAN_POINT ( 'NONE',  ( 5.000000000000000000, -39.04073710021356192, 15.48615015657568073 ) ) ;
#53810=VERTEX_POINT ( 'NONE', #36498 ) ;
#53833=EDGE_CURVE ( 'NONE', #72774, #34470, #68099, .T. ) ;
#53836=ORIENTED_EDGE ( 'NONE', *, *, #21023, .F. ) ;
#53849=AXIS2_PLACEMENT_3D ( 'NONE', #27497, #21108, #61357 ) ;
#53864=DIRECTION ( 'NONE',  ( 0.000000000000000000, 0.000000000000000000, -1.000000000000000000 ) ) ;
#53872=CARTESIAN_POINT ( 'NONE',  ( -10.00000000000000000, 0.000000000000000000, 0.000000000000000000 ) ) ;
#53879=VERTEX_POINT ( 'NONE', #41887 ) ;
#53913=AXIS2_PLACEMENT_3D ( 'NONE', #7985, #25285, #13980 ) ;
#53915=AXIS2_PLACEMENT_3D ( 'NONE', #71759, #26275, #55598 ) ;
#53928=DIRECTION ( 'NONE',  ( -1.000000000000000000, -0.000000000000000000, 0.000000000000000000 ) ) ;
#53929=LINE ( 'NONE', #41902, #9532 ) ;
#53931=DIRECTION ( 'NONE',  ( 0.000000000000000000, 0.000000000000000000, 1.000000000000000000 ) ) ;
#53935=ADVANCED_FACE ( 'NONE', ( #64456 ), #17840, .T. ) ;
#53953=DIRECTION ( 'NONE',  ( 0.000000000000000000, 0.000000000000000000, 1.000000000000000000 ) ) ;
#53956=DIRECTION ( 'NONE',  ( -1.000000000000000000, -0.000000000000000000, -0.000000000000000000 ) ) ;
#53960=ORIENTED_EDGE ( 'NONE', *, *, #9131, .F. ) ;
#53963=CARTESIAN_POINT ( 'NONE',  ( 10.00000000000000000, 41.91543099594818500, -2.663952781846293139 ) ) ;
#53968=CIRCLE ( 'NONE', #71915, 16.00000000000000000 ) ;
#53976=AXIS2_PLACEMENT_3D ( 'NONE', #29234, #73619, #16118 ) ;
#53977=ORIENTED_EDGE ( 'NONE', *, *, #67461, .T. ) ;
#54017=AXIS2_PLACEMENT_3D ( 'NONE', #21699, #39754, #33337 ) ;
#54023=CARTESIAN_POINT ( 'NONE',  ( 10.00000000000000000, -37.58145647212455032, 0.6853352020789044152 ) ) ;
#54031=CARTESIAN_POINT ( 'NONE',  ( 10.00000000000000000, 6.555932627142952995, -37.01155633439051940 ) ) ;
#54033=CARTESIAN_POINT ( 'NONE',  ( 10.00000000000000000, 16.23288003029497162, 33.80338159004289622 ) ) ;
#54034=CIRCLE ( 'NONE', #66064, 42.00000000000000000 ) ;
#54041=AXIS2_PLACEMENT_3D ( 'NONE', #34651, #6464, #17727 ) ;
#54067=AXIS2_PLACEMENT_3D ( 'NONE', #70867, #24287, #69765 ) ;
#54100=EDGE_CURVE ( 'NONE', #24060, #63369, #29704, .T. ) ;
#54136=CYLINDRICAL_SURFACE ( 'NONE', #20128, 16.00000000000000000 ) ;
#54137=DIRECTION ( 'NONE',  ( -1.000000000000000000, 0.000000000000000000, 0.000000000000000000 ) ) ;
#54141=CARTESIAN_POINT ( 'NONE',  ( 0.000000000000000000, -30.84782396557201878, -21.32104025579148399 ) ) ;
#54142=LINE ( 'NONE', #70658, #16821 ) ;
#54153=UNCERTAINTY_MEASURE_WITH_UNIT (LENGTH_MEASURE( 1.000000000000000082E-05 ), #10159, 'distance_accuracy_value', 'NONE');
#54156=DIRECTION ( 'NONE',  ( 0.000000000000000000, -0.1564344650402170189, -0.9876883405951399908 ) ) ;
#54181=DIRECTION ( 'NONE',  ( 0.000000000000000000, -0.1564344650402382242, 0.9876883405951366601 ) ) ;
#54200=DIRECTION ( 'NONE',  ( 0.000000000000000000, -1.000000000000000000, -1.047444401652940007E-14 ) ) ;
#54212=CARTESIAN_POINT ( 'NONE',  ( 0.000000000000000000, -21.53537804866058991, -30.80686688397033635 ) ) ;
#54229=CARTESIAN_POINT ( 'NONE',  ( 10.00000000000000000, 37.48860685352291000, 0.8828120875901893649 ) ) ;
#54260=DIRECTION ( 'NONE',  ( 0.000000000000000000, 0.000000000000000000, 1.000000000000000000 ) ) ;
#54273=EDGE_CURVE ( 'NONE', #4807, #51310, #60904, .T. ) ;
#54282=VERTEX_POINT ( 'NONE', #59372 ) ;
#54290=ORIENTED_EDGE ( 'NONE', *, *, #73314, .T. ) ;
#54298=DIRECTION ( 'NONE',  ( -1.000000000000000000, -0.000000000000000000, 0.000000000000000000 ) ) ;
#54320=ADVANCED_FACE ( 'NONE', ( #19873 ), #41701, .T. ) ;
#54324=FACE_OUTER_BOUND ( 'NONE', #59938, .T. ) ;
#54356=CYLINDRICAL_SURFACE ( 'NONE', #41911, 37.49900000000000233 ) ;
#54366=DIRECTION ( 'NONE',  ( 0.000000000000000000, 0.000000000000000000, 1.000000000000000000 ) ) ;
#54367=CARTESIAN_POINT ( 'NONE',  ( 10.00000000000000000, 17.80606268964585226, -33.00180498840028775 ) ) ;
#54393=FACE_OUTER_BOUND ( 'NONE', #66301, .T. ) ;
#54409=VERTEX_POINT ( 'NONE', #37560 ) ;
#54428=EDGE_CURVE ( 'NONE', #24421, #9962, #60492, .T. ) ;
#54442=VERTEX_POINT ( 'NONE', #38666 ) ;
#54454=VERTEX_POINT ( 'NONE', #26253 ) ;
#54456=ORIENTED_EDGE ( 'NONE', *, *, #62145, .T. ) ;
#54457=DIRECTION ( 'NONE',  ( -1.000000000000000000, 0.000000000000000000, 0.000000000000000000 ) ) ;
#54468=VERTEX_POINT ( 'NONE', #37922 ) ;
#54499=CARTESIAN_POINT ( 'NONE',  ( 10.00000000000000000, -6.555932627142676772, 37.01155633439056203 ) ) ;
#54505=CARTESIAN_POINT ( 'NONE',  ( 0.000000000000000000, 36.13751322684419165, 21.40280677340384585 ) ) ;
#54530=EDGE_LOOP ( 'NONE', ( #18775, #5187, #59187, #17017 ) ) ;
#54549=ORIENTED_EDGE ( 'NONE', *, *, #56857, .T. ) ;
#54572=ORIENTED_EDGE ( 'NONE', *, *, #16751, .F. ) ;
#54589=CARTESIAN_POINT ( 'NONE',  ( 10.00000000000000000, 0.000000000000000000, 0.000000000000000000 ) ) ;
#54592=VECTOR ( 'NONE', #32628, 1000.000000000000000 ) ;
#54608=DIRECTION ( 'NONE',  ( 0.000000000000000000, 0.000000000000000000, 1.000000000000000000 ) ) ;
#54618=CYLINDRICAL_SURFACE ( 'NONE', #69388, 37.49900000000000233 ) ;
#54624=DIRECTION ( 'NONE',  ( 0.000000000000000000, -0.9876883405951358830, -0.1564344650402420822 ) ) ;
#54634=VERTEX_POINT ( 'NONE', #57076 ) ;
#54680=VERTEX_POINT ( 'NONE', #46905 ) ;
#54703=VECTOR ( 'NONE', #44516, 1000.000000000000000 ) ;
#54710=CARTESIAN_POINT ( 'NONE',  ( 10.00000000000000000, -37.01155633439063308, 6.555932627142289526 ) ) ;
#54714=EDGE_LOOP ( 'NONE', ( #19969, #24240, #71583, #35692 ) ) ;
#54718=VECTOR ( 'NONE', #3474, 1000.000000000000000 ) ;
#54737=ORIENTED_EDGE ( 'NONE', *, *, #38543, .T. ) ;
#54749=ORIENTED_EDGE ( 'NONE', *, *, #58716, .T. ) ;
#54762=CYLINDRICAL_SURFACE ( 'NONE', #121, 42.00000000000000000 ) ;
#54763=EDGE_LOOP ( 'NONE', ( #35770, #52846, #7222, #55934 ) ) ;
#54791=FACE_OUTER_BOUND ( 'NONE', #58759, .T. ) ;
#54803=DIRECTION ( 'NONE',  ( -1.000000000000000000, 0.000000000000000000, 0.000000000000000000 ) ) ;
#54805=CARTESIAN_POINT ( 'NONE',  ( 0.000000000000000000, -30.00120703465222149, 22.64427369931158296 ) ) ;
#54849=VERTEX_POINT ( 'NONE', #31806 ) ;
#54887=DIRECTION ( 'NONE',  ( 0.000000000000000000, -0.5877852522924802425, 0.8090169943749422332 ) ) ;
#54894=ADVANCED_FACE ( 'NONE', ( #43118 ), #37841, .T. ) ;
#54898=ADVANCED_FACE ( 'NONE', ( #32174 ), #71281, .T. ) ;
#54908=ORIENTED_EDGE ( 'NONE', *, *, #16892, .F. ) ;
#54913=AXIS2_PLACEMENT_3D ( 'NONE', #72960, #20370, #43329 ) ;
#54922=DIRECTION ( 'NONE',  ( -1.000000000000000000, -0.000000000000000000, 0.000000000000000000 ) ) ;
#54926=ORIENTED_EDGE ( 'NONE', *, *, #1585, .F. ) ;
#54931=ADVANCED_FACE ( 'NONE', ( #63370 ), #5861, .T. ) ;
#54942=VERTEX_POINT ( 'NONE', #33668 ) ;
#54977=DIRECTION ( 'NONE',  ( -1.000000000000000000, 0.000000000000000000, 0.000000000000000000 ) ) ;
#54989=CARTESIAN_POINT ( 'NONE',  ( 0.000000000000000000, -17.67226234102801286, -33.17418723428327354 ) ) ;
#54998=ORIENTED_EDGE ( 'NONE', *, *, #66704, .T. ) ;
#54999=ORIENTED_EDGE ( 'NONE', *, *, #14319, .F. ) ;
#55004=ADVANCED_FACE ( 'NONE', ( #73139 ), #57349, .T. ) ;
#55023=CARTESIAN_POINT ( 'NONE',  ( 5.000000000000000000, 32.34446384429971744, 26.79245525562726016 ) ) ;
#55041=CARTESIAN_POINT ( 'NONE',  ( 0.000000000000000000, 0.000000000000000000, 0.000000000000000000 ) ) ;
#55057=ADVANCED_FACE ( 'NONE', ( #27661 ), #73512, .T. ) ;
#55086=AXIS2_PLACEMENT_3D ( 'NONE', #71956, #20471, #43427 ) ;
#55144=CIRCLE ( 'NONE', #15535, 37.49900000000000944 ) ;
#55173=DIRECTION ( 'NONE',  ( -1.000000000000000000, -0.000000000000000000, -0.000000000000000000 ) ) ;
#55175=CARTESIAN_POINT ( 'NONE',  ( 10.00000000000000000, 0.000000000000000000, 0.000000000000000000 ) ) ;
#55202=CARTESIAN_POINT ( 'NONE',  ( 10.00000000000000000, 29.81001611431009479, 22.74946021919143391 ) ) ;
#55205=AXIS2_PLACEMENT_3D ( 'NONE', #68034, #40569, #63515 ) ;
#55216=FACE_OUTER_BOUND ( 'NONE', #33019, .T. ) ;
#55217=ORIENTED_EDGE ( 'NONE', *, *, #26784, .T. ) ;
#55227=ORIENTED_EDGE ( 'NONE', *, *, #57457, .T. ) ;
#55252=VECTOR ( 'NONE', #19826, 1000.000000000000000 ) ;
#55256=CYLINDRICAL_SURFACE ( 'NONE', #3523, 16.00000000000000000 ) ;
#55259=CIRCLE ( 'NONE', #20430, 37.49900000000000233 ) ;
#55355=DIRECTION ( 'NONE',  ( 0.000000000000000000, 0.000000000000000000, 1.000000000000000000 ) ) ;
#55364=DIRECTION ( 'NONE',  ( 0.000000000000000000, 0.000000000000000000, 1.000000000000000000 ) ) ;
#55365=EDGE_CURVE ( 'NONE', #17447, #60516, #3864, .T. ) ;
#55387=EDGE_LOOP ( 'NONE', ( #16631, #9736, #55418, #9726 ) ) ;
#55400=DIRECTION ( 'NONE',  ( -1.000000000000000000, 0.000000000000000000, -0.000000000000000000 ) ) ;
#55403=AXIS2_PLACEMENT_3D ( 'NONE', #5872, #11846, #18967 ) ;
#55411=CARTESIAN_POINT ( 'NONE',  ( 10.00000000000000000, 0.000000000000000000, 0.000000000000000000 ) ) ;
#55418=ORIENTED_EDGE ( 'NONE', *, *, #36078, .F. ) ;
#55455=ADVANCED_FACE ( 'NONE', ( #20747 ), #67352, .T. ) ;
#55462=VERTEX_POINT ( 'NONE', #32754 ) ;
#55494=ORIENTED_EDGE ( 'NONE', *, *, #5789, .F. ) ;
#55501=CARTESIAN_POINT ( 'NONE',  ( 10.00000000000000000, 0.000000000000000000, 0.000000000000000000 ) ) ;
#55539=DIRECTION ( 'NONE',  ( 0.000000000000000000, 0.000000000000000000, 1.000000000000000000 ) ) ;
#55554=EDGE_LOOP ( 'NONE', ( #19467, #72191, #40233, #33169 ) ) ;
#55569=CIRCLE ( 'NONE', #17205, 37.49900000000000233 ) ;
#55579=VERTEX_POINT ( 'NONE', #56829 ) ;
#55598=DIRECTION ( 'NONE',  ( 0.000000000000000000, 0.4539904997395414754, 0.8910065241883706744 ) ) ;
#55616=LINE ( 'NONE', #67644, #10431 ) ;
#55629=CIRCLE ( 'NONE', #28040, 15.99999999999999822 ) ;
#55633=CARTESIAN_POINT ( 'NONE',  ( 10.00000000000000000, 4.992566952384984269, 37.16516213103279398 ) ) ;
#55638=ORIENTED_EDGE ( 'NONE', *, *, #50818, .F. ) ;
#55641=CARTESIAN_POINT ( 'NONE',  ( 10.00000000000000000, 6.736453364084091788, -36.88895765772625879 ) ) ;
#55646=ORIENTED_EDGE ( 'NONE', *, *, #33201, .F. ) ;
#55662=EDGE_CURVE ( 'NONE', #38385, #48805, #73543, .T. ) ;
#55682=DIRECTION ( 'NONE',  ( 0.000000000000000000, 0.000000000000000000, 1.000000000000000000 ) ) ;
#55704=DIRECTION ( 'NONE',  ( 0.000000000000000000, 0.000000000000000000, 1.000000000000000000 ) ) ;
#55739=ORIENTED_EDGE ( 'NONE', *, *, #55365, .T. ) ;
#55752=CARTESIAN_POINT ( 'NONE',  ( 10.00000000000000000, -33.17418723428319538, 17.67226234102814431 ) ) ;
#55803=DIRECTION ( 'NONE',  ( -1.000000000000000000, 0.000000000000000000, 0.000000000000000000 ) ) ;
#55811=DIRECTION ( 'NONE',  ( -1.000000000000000000, -0.000000000000000000, -0.000000000000000000 ) ) ;
#55853=ORIENTED_EDGE ( 'NONE', *, *, #67467, .F. ) ;
#55859=CARTESIAN_POINT ( 'NONE',  ( 10.00000000000000000, 16.65560815589411092, 38.55633173627015964 ) ) ;
#55893=VERTEX_POINT ( 'NONE', #54505 ) ;
#55905=AXIS2_PLACEMENT_3D ( 'NONE', #58011, #17780, #24536 ) ;
#55934=ORIENTED_EDGE ( 'NONE', *, *, #71433, .T. ) ;
#55939=AXIS2_PLACEMENT_3D ( 'NONE', #44275, #8949, #12815 ) ;
#55941=CIRCLE ( 'NONE', #24757, 15.99999999999999822 ) ;
#55953=CIRCLE ( 'NONE', #53593, 42.00000000000000000 ) ;
#55962=CARTESIAN_POINT ( 'NONE',  ( 0.000000000000000000, -36.13751322684404244, -21.40280677340410165 ) ) ;
#55975=DIRECTION ( 'NONE',  ( 0.000000000000000000, 0.000000000000000000, -1.000000000000000000 ) ) ;
#56018=ORIENTED_EDGE ( 'NONE', *, *, #57221, .T. ) ;
#56041=ORIENTED_EDGE ( 'NONE', *, *, #13521, .T. ) ;
#56046=VERTEX_POINT ( 'NONE', #74013 ) ;
#56051=CARTESIAN_POINT ( 'NONE',  ( 10.00000000000000000, 12.42422080174639021, 35.38097989696516521 ) ) ;
#56067=LINE ( 'NONE', #67722, #17054 ) ;
#56070=ORIENTED_EDGE ( 'NONE', *, *, #56373, .T. ) ;
#56112=EDGE_CURVE ( 'NONE', #10248, #52143, #64011, .T. ) ;
#56115=EDGE_LOOP ( 'NONE', ( #58246, #54549, #4732, #49349 ) ) ;
#56119=CIRCLE ( 'NONE', #60946, 37.49900000000000233 ) ;
#56127=ORIENTED_EDGE ( 'NONE', *, *, #60928, .F. ) ;
#56146=ORIENTED_EDGE ( 'NONE', *, *, #2355, .T. ) ;
#56169=EDGE_CURVE ( 'NONE', #63446, #6569, #55569, .T. ) ;
#56181=DIRECTION ( 'NONE',  ( -1.000000000000000000, 0.000000000000000000, 0.000000000000000000 ) ) ;
#56206=ORIENTED_EDGE ( 'NONE', *, *, #38301, .F. ) ;
#56208=EDGE_CURVE ( 'NONE', #60292, #55893, #23175, .T. ) ;
#56240=DIRECTION ( 'NONE',  ( 0.000000000000000000, 0.000000000000000000, 1.000000000000000000 ) ) ;
#56255=DIRECTION ( 'NONE',  ( 0.000000000000000000, 0.3090169943749482839, -0.9510565162951533091 ) ) ;
#56256=VERTEX_POINT ( 'NONE', #70210 ) ;
#56260=DIRECTION ( 'NONE',  ( -1.000000000000000000, -0.000000000000000000, -0.000000000000000000 ) ) ;
#56281=CARTESIAN_POINT ( 'NONE',  ( 10.00000000000000000, 6.736453364084091788, -36.88895765772625879 ) ) ;
#56296=VECTOR ( 'NONE', #15611, 1000.000000000000000 ) ;
#56322=DIRECTION ( 'NONE',  ( -1.000000000000000000, 0.000000000000000000, 0.000000000000000000 ) ) ;
#56323=CIRCLE ( 'NONE', #51543, 42.00000000000000000 ) ;
#56343=VERTEX_POINT ( 'NONE', #43893 ) ;
#56346=AXIS2_PLACEMENT_3D ( 'NONE', #14911, #60423, #3293 ) ;
#56373=EDGE_CURVE ( 'NONE', #52503, #13202, #55629, .T. ) ;
#56391=DIRECTION ( 'NONE',  ( -1.000000000000000000, -0.000000000000000000, -0.000000000000000000 ) ) ;
#56421=DIRECTION ( 'NONE',  ( 1.000000000000000000, 0.000000000000000000, -0.000000000000000000 ) ) ;
#56444=ORIENTED_EDGE ( 'NONE', *, *, #457, .T. ) ;
#56459=ORIENTED_EDGE ( 'NONE', *, *, #70774, .T. ) ;
#56466=CARTESIAN_POINT ( 'NONE',  ( 5.000000000000000000, -39.04073710021332744, -15.48615015657624205 ) ) ;
#56468=VERTEX_POINT ( 'NONE', #51363 ) ;
#56472=DIRECTION ( 'NONE',  ( 0.000000000000000000, 0.000000000000000000, 1.000000000000000000 ) ) ;
#56473=DIRECTION ( 'NONE',  ( -1.000000000000000000, 0.000000000000000000, -0.000000000000000000 ) ) ;
#56487=VECTOR ( 'NONE', #27308, 1000.000000000000000 ) ;
#56492=DIRECTION ( 'NONE',  ( -1.000000000000000000, 0.000000000000000000, -0.000000000000000000 ) ) ;
#56503=AXIS2_PLACEMENT_3D ( 'NONE', #47454, #36165, #47817 ) ;
#56505=ORIENTED_EDGE ( 'NONE', *, *, #17315, .T. ) ;
#56515=DIRECTION ( 'NONE',  ( -1.000000000000000000, 0.000000000000000000, 0.000000000000000000 ) ) ;
#56524=CYLINDRICAL_SURFACE ( 'NONE', #614, 42.00000000000000000 ) ;
#56525=DIRECTION ( 'NONE',  ( -1.000000000000000000, -0.000000000000000000, 0.000000000000000000 ) ) ;
#56542=LINE ( 'NONE', #73805, #13864 ) ;
#56546=DIRECTION ( 'NONE',  ( -1.000000000000000000, -0.000000000000000000, -0.000000000000000000 ) ) ;
#56560=DIRECTION ( 'NONE',  ( 1.000000000000000000, 0.000000000000000000, 0.000000000000000000 ) ) ;
#56567=DIRECTION ( 'NONE',  ( 0.000000000000000000, 0.9510565162951523099, 0.3090169943749517811 ) ) ;
#56569=DIRECTION ( 'NONE',  ( 0.000000000000000000, 0.9876883405951381034, -0.1564344650402276216 ) ) ;
#56585=ORIENTED_EDGE ( 'NONE', *, *, #27333, .T. ) ;
#56593=AXIS2_PLACEMENT_3D ( 'NONE', #7266, #47484, #12149 ) ;
#56610=AXIS2_PLACEMENT_3D ( 'NONE', #69292, #29415, #52363 ) ;
#56614=CARTESIAN_POINT ( 'NONE',  ( 5.000000000000000000, 35.47612816024556537, -22.48208911017461631 ) ) ;
#56624=ORIENTED_EDGE ( 'NONE', *, *, #18297, .F. ) ;
#56631=CYLINDRICAL_SURFACE ( 'NONE', #72654, 37.49900000000000233 ) ;
#56645=CARTESIAN_POINT ( 'NONE',  ( 0.000000000000000000, -27.13269053701114331, 25.88420570971391754 ) ) ;
#56659=FACE_OUTER_BOUND ( 'NONE', #44420, .T. ) ;
#56660=DIRECTION ( 'NONE',  ( 1.000000000000000000, -0.000000000000000000, -0.000000000000000000 ) ) ;
#56668=DIRECTION ( 'NONE',  ( -1.000000000000000000, -0.000000000000000000, -0.000000000000000000 ) ) ;
#56669=DIRECTION ( 'NONE',  ( -1.000000000000000000, -0.000000000000000000, 0.000000000000000000 ) ) ;
#56673=VECTOR ( 'NONE', #30899, 1000.000000000000000 ) ;
#56703=VERTEX_POINT ( 'NONE', #68108 ) ;
#56706=EDGE_CURVE ( 'NONE', #54282, #73989, #38829, .T. ) ;
#56721=DIRECTION ( 'NONE',  ( 0.000000000000000000, 0.1564344650402311743, -0.9876883405951377704 ) ) ;
#56726=DIRECTION ( 'NONE',  ( 1.000000000000000000, -0.000000000000000000, -0.000000000000000000 ) ) ;
#56731=ORIENTED_EDGE ( 'NONE', *, *, #58716, .F. ) ;
#56774=VERTEX_POINT ( 'NONE', #61364 ) ;
#56783=SURFACE_SIDE_STYLE ('',( #51127 ) ) ;
#56793=DIRECTION ( 'NONE',  ( 0.000000000000000000, 0.000000000000000000, 1.000000000000000000 ) ) ;
#56819=DIRECTION ( 'NONE',  ( 0.000000000000000000, 0.000000000000000000, -1.000000000000000000 ) ) ;
#56826=AXIS2_PLACEMENT_3D ( 'NONE', #27788, #28900, #51833 ) ;
#56829=CARTESIAN_POINT ( 'NONE',  ( 10.00000000000000000, -41.81611651403859042, -3.925862922256606602 ) ) ;
#56857=EDGE_CURVE ( 'NONE', #60516, #57603, #16072, .T. ) ;
#56870=AXIS2_PLACEMENT_3D ( 'NONE', #64323, #25205, #71047 ) ;
#56887=EDGE_LOOP ( 'NONE', ( #254, #50646, #72129, #61891 ) ) ;
#56901=EDGE_CURVE ( 'NONE', #20649, #16746, #1739, .T. ) ;
#56922=CARTESIAN_POINT ( 'NONE',  ( 0.000000000000000000, 2.663952781846728790, -41.91543099594814947 ) ) ;
#56935=DIRECTION ( 'NONE',  ( -1.000000000000000000, 0.000000000000000000, -0.000000000000000000 ) ) ;
#56937=FACE_OUTER_BOUND ( 'NONE', #69718, .T. ) ;
#56950=VERTEX_POINT ( 'NONE', #58307 ) ;
#56957=AXIS2_PLACEMENT_3D ( 'NONE', #53872, #25308, #2041 ) ;
#56978=AXIS2_PLACEMENT_3D ( 'NONE', #23926, #7375, #9592 ) ;
#56983=CARTESIAN_POINT ( 'NONE',  ( 10.00000000000000000, 27.05870788708267582, -26.08949754952995903 ) ) ;
#56985=ORIENTED_EDGE ( 'NONE', *, *, #63237, .F. ) ;
#56990=EDGE_CURVE ( 'NONE', #19782, #54634, #40277, .T. ) ;
#57002=CARTESIAN_POINT ( 'NONE',  ( 10.00000000000000000, -5.202137450156129717, -37.22597642581163768 ) ) ;
#57006=DIRECTION ( 'NONE',  ( 0.000000000000000000, 0.000000000000000000, 1.000000000000000000 ) ) ;
#57009=CYLINDRICAL_SURFACE ( 'NONE', #27597, 16.00000000000000000 ) ;
#57036=EDGE_CURVE ( 'NONE', #2268, #15264, #69222, .T. ) ;
#57045=DIRECTION ( 'NONE',  ( -1.000000000000000000, -0.000000000000000000, 0.000000000000000000 ) ) ;
#57046=DIRECTION ( 'NONE',  ( -1.000000000000000000, 0.000000000000000000, 0.000000000000000000 ) ) ;
#57052=CARTESIAN_POINT ( 'NONE',  ( 0.000000000000000000, 26.79245525562762253, -32.34446384429942611 ) ) ;
#57068=DIRECTION ( 'NONE',  ( -1.000000000000000000, -0.000000000000000000, 0.000000000000000000 ) ) ;
#57075=EDGE_CURVE ( 'NONE', #21495, #72597, #49702, .T. ) ;
#57076=CARTESIAN_POINT ( 'NONE',  ( 0.000000000000000000, 37.22597642581158084, 10.79786254984347593 ) ) ;
#57078=ORIENTED_EDGE ( 'NONE', *, *, #18926, .T. ) ;
#57090=AXIS2_PLACEMENT_3D ( 'NONE', #21697, #8945, #61937 ) ;
#57119=DIRECTION ( 'NONE',  ( -1.000000000000000000, 0.000000000000000000, 0.000000000000000000 ) ) ;
#57133=DIRECTION ( 'NONE',  ( 0.000000000000000000, -1.000000000000000000, -1.040834085586084257E-14 ) ) ;
#57137=AXIS2_PLACEMENT_3D ( 'NONE', #57599, #74128, #63615 ) ;
#57138=ORIENTED_EDGE ( 'NONE', *, *, #66560, .F. ) ;
#57139=ORIENTED_EDGE ( 'NONE', *, *, #52186, .T. ) ;
#57177=CYLINDRICAL_SURFACE ( 'NONE', #40944, 16.00000000000000000 ) ;
#57179=VERTEX_POINT ( 'NONE', #66545 ) ;
#57182=CARTESIAN_POINT ( 'NONE',  ( 0.000000000000000000, 33.79645857604513992, -16.45098606841138178 ) ) ;
#57197=CARTESIAN_POINT ( 'NONE',  ( 10.00000000000000000, 0.000000000000000000, 0.000000000000000000 ) ) ;
#57203=ADVANCED_FACE ( 'NONE', ( #33050 ), #3774, .T. ) ;
#57206=CARTESIAN_POINT ( 'NONE',  ( 0.000000000000000000, 1.530808498934191521E-15, -12.50000000000000000 ) ) ;
#57221=EDGE_CURVE ( 'NONE', #51520, #10248, #31682, .T. ) ;
#57235=EDGE_CURVE ( 'NONE', #40253, #37974, #37715, .T. ) ;
#57237=ORIENTED_EDGE ( 'NONE', *, *, #33189, .F. ) ;
#57239=DIRECTION ( 'NONE',  ( -1.000000000000000000, 0.000000000000000000, -0.000000000000000000 ) ) ;
#57249=DIRECTION ( 'NONE',  ( 0.000000000000000000, 0.000000000000000000, 1.000000000000000000 ) ) ;
#57256=CYLINDRICAL_SURFACE ( 'NONE', #60625, 42.00000000000000000 ) ;
#57259=DIRECTION ( 'NONE',  ( -1.000000000000000000, 0.000000000000000000, 0.000000000000000000 ) ) ;
#57261=CARTESIAN_POINT ( 'NONE',  ( 10.00000000000000000, 0.000000000000000000, 0.000000000000000000 ) ) ;
#57281=DIRECTION ( 'NONE',  ( -1.000000000000000000, 0.000000000000000000, 0.000000000000000000 ) ) ;
#57294=AXIS2_PLACEMENT_3D ( 'NONE', #37673, #60607, #9086 ) ;
#57313=ORIENTED_EDGE ( 'NONE', *, *, #51914, .T. ) ;
#57315=EDGE_CURVE ( 'NONE', #64608, #24000, #34165, .T. ) ;
#57317=ORIENTED_EDGE ( 'NONE', *, *, #49798, .F. ) ;
#57324=VERTEX_POINT ( 'NONE', #34926 ) ;
#57327=ORIENTED_EDGE ( 'NONE', *, *, #45576, .F. ) ;
#57336=DIRECTION ( 'NONE',  ( 0.000000000000000000, 1.000000000000000000, -9.787530781167598712E-16 ) ) ;
#57349=CYLINDRICAL_SURFACE ( 'NONE', #20684, 37.49900000000000233 ) ;
#57354=ORIENTED_EDGE ( 'NONE', *, *, #60928, .T. ) ;
#57366=AXIS2_PLACEMENT_3D ( 'NONE', #17198, #57421, #73209 ) ;
#57376=CIRCLE ( 'NONE', #21326, 37.49900000000000944 ) ;
#57389=EDGE_CURVE ( 'NONE', #64823, #37625, #65352, .T. ) ;
#57400=ADVANCED_FACE ( 'NONE', ( #37439 ), #42695, .T. ) ;
#57402=ORIENTED_EDGE ( 'NONE', *, *, #17315, .F. ) ;
#57405=DIRECTION ( 'NONE',  ( 0.000000000000000000, 0.8090169943749445647, 0.5877852522924770229 ) ) ;
#57406=CARTESIAN_POINT ( 'NONE',  ( 0.000000000000000000, -10.74501242461307982, 35.92658777277507198 ) ) ;
#57418=VECTOR ( 'NONE', #43634, 1000.000000000000000 ) ;
#57421=DIRECTION ( 'NONE',  ( -1.000000000000000000, 0.000000000000000000, -0.000000000000000000 ) ) ;
#57423=ORIENTED_EDGE ( 'NONE', *, *, #70241, .T. ) ;
#57446=CIRCLE ( 'NONE', #36984, 37.49900000000000233 ) ;
#57457=EDGE_CURVE ( 'NONE', #24083, #61302, #13705, .T. ) ;
#57469=ORIENTED_EDGE ( 'NONE', *, *, #215, .F. ) ;
#57481=CIRCLE ( 'NONE', #25043, 16.00000000000000000 ) ;
#57492=ADVANCED_FACE ( 'NONE', ( #72716 ), #3970, .T. ) ;
#57498=DIRECTION ( 'NONE',  ( 0.000000000000000000, -0.9876883405951361050, -0.1564344650402419989 ) ) ;
#57506=AXIS2_PLACEMENT_3D ( 'NONE', #63610, #36485, #63973 ) ;
#57507=EDGE_LOOP ( 'NONE', ( #39294, #29379, #18204, #47784 ) ) ;
#57547=CARTESIAN_POINT ( 'NONE',  ( 10.00000000000000000, 0.000000000000000000, 0.000000000000000000 ) ) ;
#57585=CARTESIAN_POINT ( 'NONE',  ( -10.00000000000000000, 0.000000000000000000, 0.000000000000000000 ) ) ;
#57599=CARTESIAN_POINT ( 'NONE',  ( 10.00000000000000000, -16.45098606841102651, -33.79645857604531045 ) ) ;
#57601=DIRECTION ( 'NONE',  ( -1.000000000000000000, -0.000000000000000000, -0.000000000000000000 ) ) ;
#57603=VERTEX_POINT ( 'NONE', #28350 ) ;
#57607=EDGE_LOOP ( 'NONE', ( #2350, #54456, #67827, #53960 ) ) ;
#57612=LINE ( 'NONE', #6113, #71886 ) ;
#57628=VERTEX_POINT ( 'NONE', #4715 ) ;
#57665=DIRECTION ( 'NONE',  ( 0.000000000000000000, 0.000000000000000000, 1.000000000000000000 ) ) ;
#57676=DIRECTION ( 'NONE',  ( -1.000000000000000000, 0.000000000000000000, 0.000000000000000000 ) ) ;
#57685=ORIENTED_EDGE ( 'NONE', *, *, #26795, .F. ) ;
#57711=EDGE_CURVE ( 'NONE', #51588, #47714, #12578, .T. ) ;
#57720=DIRECTION ( 'NONE',  ( -1.000000000000000000, -0.000000000000000000, 0.000000000000000000 ) ) ;
#57727=VERTEX_POINT ( 'NONE', #13650 ) ;
#57742=CARTESIAN_POINT ( 'NONE',  ( 10.00000000000000000, 0.000000000000000000, 0.000000000000000000 ) ) ;
#57747=EDGE_CURVE ( 'NONE', #52056, #51811, #70204, .T. ) ;
#57761=CYLINDRICAL_SURFACE ( 'NONE', #180, 16.00000000000000000 ) ;
#57798=ORIENTED_EDGE ( 'NONE', *, *, #31878, .F. ) ;
#57799=ORIENTED_EDGE ( 'NONE', *, *, #45783, .T. ) ;
#57820=CARTESIAN_POINT ( 'NONE',  ( 10.00000000000000000, -36.88895765772637247, 6.736453364083436313 ) ) ;
#57843=CARTESIAN_POINT ( 'NONE',  ( 0.000000000000000000, -41.81611651403859042, -3.925862922256606602 ) ) ;
#57844=VERTEX_POINT ( 'NONE', #9122 ) ;
#57860=CARTESIAN_POINT ( 'NONE',  ( 0.000000000000000000, -30.80686688397025108, 21.53537804866070715 ) ) ;
#57875=ADVANCED_FACE ( 'NONE', ( #14014 ), #15501, .T. ) ;
#57881=FACE_OUTER_BOUND ( 'NONE', #71246, .T. ) ;
#57889=CARTESIAN_POINT ( 'NONE',  ( 5.000000000000000000, 2.663952781846149254, 41.91543099594818500 ) ) ;
#57892=ORIENTED_EDGE ( 'NONE', *, *, #42788, .T. ) ;
#57895=SHAPE_REPRESENTATION_RELATIONSHIP ( 'NONE' , 'NONE' ,  #31559, #34586 ) ;
#57930=DIRECTION ( 'NONE',  ( -1.000000000000000000, -0.000000000000000000, 0.000000000000000000 ) ) ;
#57935=CYLINDRICAL_SURFACE ( 'NONE', #11561, 42.00000000000000000 ) ;
#57938=DIRECTION ( 'NONE',  ( -1.000000000000000000, 0.000000000000000000, -0.000000000000000000 ) ) ;
#57946=DIRECTION ( 'NONE',  ( 0.000000000000000000, 0.4539904997395414754, 0.8910065241883706744 ) ) ;
#57950=ORIENTED_EDGE ( 'NONE', *, *, #4115, .F. ) ;
#57951=CARTESIAN_POINT ( 'NONE',  ( 0.000000000000000000, -26.79245525562690844, -32.34446384430000876 ) ) ;
#57965=ORIENTED_EDGE ( 'NONE', *, *, #39298, .T. ) ;
#57969=ORIENTED_EDGE ( 'NONE', *, *, #12364, .T. ) ;
#57971=VERTEX_POINT ( 'NONE', #27137 ) ;
#57979=DIRECTION ( 'NONE',  ( 0.000000000000000000, 0.000000000000000000, -1.000000000000000000 ) ) ;
#57982=PLANE ( 'NONE',  #51667 ) ;
#57992=CARTESIAN_POINT ( 'NONE',  ( -10.00000000000000000, 0.000000000000000000, 0.000000000000000000 ) ) ;
#57993=CARTESIAN_POINT ( 'NONE',  ( 10.00000000000000000, -33.17418723428294669, -17.67226234102862747 ) ) ;
#58011=CARTESIAN_POINT ( 'NONE',  ( 10.00000000000000000, 30.00120703465236716, -22.64427369931138756 ) ) ;
#58016=FACE_OUTER_BOUND ( 'NONE', #56115, .T. ) ;
#58061=ORIENTED_EDGE ( 'NONE', *, *, #68412, .T. ) ;
#58074=ORIENTED_EDGE ( 'NONE', *, *, #31733, .F. ) ;
#58098=AXIS2_PLACEMENT_3D ( 'NONE', #68599, #15598, #45300 ) ;
#58110=DIRECTION ( 'NONE',  ( -1.000000000000000000, 0.000000000000000000, 0.000000000000000000 ) ) ;
#58115=VECTOR ( 'NONE', #63277, 1000.000000000000000 ) ;
#58130=LINE ( 'NONE', #24298, #19595 ) ;
#58148=EDGE_CURVE ( 'NONE', #2581, #44188, #8580, .T. ) ;
#58152=CARTESIAN_POINT ( 'NONE',  ( 10.00000000000000000, 22.74946021919133088, 29.81001611431016229 ) ) ;
#58180=FACE_OUTER_BOUND ( 'NONE', #10412, .T. ) ;
#58194=ORIENTED_EDGE ( 'NONE', *, *, #49624, .F. ) ;
#58231=DIRECTION ( 'NONE',  ( -1.000000000000000000, -0.000000000000000000, -0.000000000000000000 ) ) ;
#58240=DIRECTION ( 'NONE',  ( -1.000000000000000000, 0.000000000000000000, 0.000000000000000000 ) ) ;
#58246=ORIENTED_EDGE ( 'NONE', *, *, #33894, .T. ) ;
#58247=DIRECTION ( 'NONE',  ( -1.000000000000000000, 0.000000000000000000, 0.000000000000000000 ) ) ;
#58249=CIRCLE ( 'NONE', #663, 16.00000000000000000 ) ;
#58261=VERTEX_POINT ( 'NONE', #1864 ) ;
#58266=ORIENTED_EDGE ( 'NONE', *, *, #70886, .T. ) ;
#58280=CARTESIAN_POINT ( 'NONE',  ( 10.00000000000000000, 0.000000000000000000, 0.000000000000000000 ) ) ;
#58307=CARTESIAN_POINT ( 'NONE',  ( 0.000000000000000000, -37.58145647212455032, 16.68533520207890319 ) ) ;
#58308=FACE_OUTER_BOUND ( 'NONE', #29119, .T. ) ;
#58317=EDGE_CURVE ( 'NONE', #46805, #59461, #58249, .T. ) ;
#58326=EDGE_CURVE ( 'NONE', #67395, #20649, #27050, .T. ) ;
#58330=DIRECTION ( 'NONE',  ( -1.000000000000000000, -0.000000000000000000, 0.000000000000000000 ) ) ;
#58347=FACE_BOUND ( 'NONE', #15504, .T. ) ;
#58370=DIRECTION ( 'NONE',  ( -1.000000000000000000, 0.000000000000000000, 0.000000000000000000 ) ) ;
#58388=DIRECTION ( 'NONE',  ( -1.000000000000000000, -0.000000000000000000, 0.000000000000000000 ) ) ;
#58393=CARTESIAN_POINT ( 'NONE',  ( -10.00000000000000000, 0.000000000000000000, 0.000000000000000000 ) ) ;
#58397=CARTESIAN_POINT ( 'NONE',  ( 0.000000000000000000, -3.925862922255855647, -41.81611651403866858 ) ) ;
#58420=LINE ( 'NONE', #64441, #27909 ) ;
#58427=DIRECTION ( 'NONE',  ( 0.000000000000000000, -0.3090169943749349057, -0.9510565162951577500 ) ) ;
#58434=ORIENTED_EDGE ( 'NONE', *, *, #1433, .F. ) ;
#58441=CARTESIAN_POINT ( 'NONE',  ( 10.00000000000000000, 37.22597642581158084, -5.202137450156524068 ) ) ;
#58453=EDGE_LOOP ( 'NONE', ( #5230, #53609, #10987, #26922 ) ) ;
#58466=VECTOR ( 'NONE', #38163, 1000.000000000000000 ) ;
#58526=AXIS2_PLACEMENT_3D ( 'NONE', #10064, #40128, #63084 ) ;
#58544=CARTESIAN_POINT ( 'NONE',  ( 10.00000000000000000, -6.555932627142676772, 37.01155633439056203 ) ) ;
#58547=ORIENTED_EDGE ( 'NONE', *, *, #3514, .T. ) ;
#58578=DIRECTION ( 'NONE',  ( 1.000000000000000000, -0.000000000000000000, -0.000000000000000000 ) ) ;
#58590=DIRECTION ( 'NONE',  ( -1.000000000000000000, 0.000000000000000000, -0.000000000000000000 ) ) ;
#58602=CARTESIAN_POINT ( 'NONE',  ( 4.999999999999999112, -41.81611651403859042, -3.925862922256606602 ) ) ;
#58626=CARTESIAN_POINT ( 'NONE',  ( 10.00000000000000000, 0.6853352020790449695, 37.58145647212454321 ) ) ;
#58630=ADVANCED_FACE ( 'NONE', ( #49831 ), #26901, .T. ) ;
#58660=DIRECTION ( 'NONE',  ( -1.000000000000000000, -0.000000000000000000, 0.000000000000000000 ) ) ;
#58661=CARTESIAN_POINT ( 'NONE',  ( 10.00000000000000000, -37.58145647212455032, 0.6853352020789044152 ) ) ;
#58673=AXIS2_PLACEMENT_3D ( 'NONE', #71510, #43351, #37698 ) ;
#58686=VERTEX_POINT ( 'NONE', #22012 ) ;
#58692=CIRCLE ( 'NONE', #23866, 16.00000000000000000 ) ;
#58698=DIRECTION ( 'NONE',  ( 0.000000000000000000, 0.000000000000000000, 1.000000000000000000 ) ) ;
#58703=ORIENTED_EDGE ( 'NONE', *, *, #19180, .F. ) ;
#58706=CARTESIAN_POINT ( 'NONE',  ( 10.00000000000000000, 0.000000000000000000, 0.000000000000000000 ) ) ;
#58716=EDGE_CURVE ( 'NONE', #44099, #45217, #23532, .T. ) ;
#58717=AXIS2_PLACEMENT_3D ( 'NONE', #34319, #28674, #67423 ) ;
#58721=ORIENTED_EDGE ( 'NONE', *, *, #68445, .T. ) ;
#58722=CARTESIAN_POINT ( 'NONE',  ( 5.000000000000000000, -16.65560815589439159, 38.55633173627004595 ) ) ;
#58740=CARTESIAN_POINT ( 'NONE',  ( 0.000000000000000000, 36.88895765772633695, 6.736453364083687667 ) ) ;
#58750=DIRECTION ( 'NONE',  ( -1.000000000000000000, -0.000000000000000000, -0.000000000000000000 ) ) ;
#58752=DIRECTION ( 'NONE',  ( 0.000000000000000000, 0.8910065241883656784, 0.4539904997395510788 ) ) ;
#58756=CARTESIAN_POINT ( 'NONE',  ( 0.000000000000000000, -31.52238457039579345, -27.75498641678775158 ) ) ;
#58759=EDGE_LOOP ( 'NONE', ( #27836, #16496, #50990, #70348 ) ) ;
#58760=AXIS2_PLACEMENT_3D ( 'NONE', #2704, #25584, #7566 ) ;
#58780=DIRECTION ( 'NONE',  ( -1.000000000000000000, 0.000000000000000000, -0.000000000000000000 ) ) ;
#58791=CIRCLE ( 'NONE', #25, 42.00000000000000000 ) ;
#58796=DIRECTION ( 'NONE',  ( 0.000000000000000000, 0.000000000000000000, 1.000000000000000000 ) ) ;
#58797=VERTEX_POINT ( 'NONE', #52061 ) ;
#58800=CARTESIAN_POINT ( 'NONE',  ( 0.000000000000000000, 37.22597642581158084, -5.202137450156524068 ) ) ;
#58808=CIRCLE ( 'NONE', #15606, 42.00000000000000000 ) ;
#58829=DIRECTION ( 'NONE',  ( -1.000000000000000000, 0.000000000000000000, 0.000000000000000000 ) ) ;
#58835=VECTOR ( 'NONE', #15171, 1000.000000000000000 ) ;
#58839=CARTESIAN_POINT ( 'NONE',  ( 10.00000000000000000, -35.53030884539094103, 12.26510123303246935 ) ) ;
#58869=CARTESIAN_POINT ( 'NONE',  ( 0.000000000000000000, -35.47612816024506088, -22.48208911017539435 ) ) ;
#58887=ORIENTED_EDGE ( 'NONE', *, *, #67297, .F. ) ;
#58904=CARTESIAN_POINT ( 'NONE',  ( 10.00000000000000000, -37.48860685352290290, -0.8828120875904512665 ) ) ;
#58909=ADVANCED_FACE ( 'NONE', ( #42641 ), #25712, .T. ) ;
#58934=DIRECTION ( 'NONE',  ( -1.000000000000000000, 0.000000000000000000, 0.000000000000000000 ) ) ;
#58958=FACE_OUTER_BOUND ( 'NONE', #9445, .T. ) ;
#58966=CIRCLE ( 'NONE', #42121, 37.49900000000000233 ) ;
#58976=DIRECTION ( 'NONE',  ( 0.000000000000000000, 0.7071067811865487940, -0.7071067811865462405 ) ) ;
#58984=EDGE_CURVE ( 'NONE', #39405, #47714, #14430, .T. ) ;
#58987=ORIENTED_EDGE ( 'NONE', *, *, #69753, .T. ) ;
#58997=AXIS2_PLACEMENT_3D ( 'NONE', #28150, #39822, #62772 ) ;
#59000=DIRECTION ( 'NONE',  ( 0.000000000000000000, 0.4539904997395477482, -0.8910065241883673437 ) ) ;
#59001=ORIENTED_EDGE ( 'NONE', *, *, #41579, .F. ) ;
#59024=AXIS2_PLACEMENT_3D ( 'NONE', #54023, #38199, #66050 ) ;
#59027=LINE ( 'NONE', #48104, #69695 ) ;
#59031=ORIENTED_EDGE ( 'NONE', *, *, #10154, .T. ) ;
#59035=ORIENTED_EDGE ( 'NONE', *, *, #12463, .F. ) ;
#59039=LINE ( 'NONE', #7527, #67472 ) ;
#59040=FACE_OUTER_BOUND ( 'NONE', #55554, .T. ) ;
#59048=CARTESIAN_POINT ( 'NONE',  ( 10.00000000000000000, -9.188173127307592836, 40.98264845739746676 ) ) ;
#59053=( GEOMETRIC_REPRESENTATION_CONTEXT ( 3 ) GLOBAL_UNCERTAINTY_ASSIGNED_CONTEXT ( ( #37605 ) ) GLOBAL_UNIT_ASSIGNED_CONTEXT ( ( #34955, #52603, #18032 ) ) REPRESENTATION_CONTEXT ( 'NONE', 'WORKASPACE' ) );
#59096=DIRECTION ( 'NONE',  ( 0.000000000000000000, 0.000000000000000000, 1.000000000000000000 ) ) ;
#59130=AXIS2_PLACEMENT_3D ( 'NONE', #14500, #37459, #2543 ) ;
#59139=FACE_OUTER_BOUND ( 'NONE', #38022, .T. ) ;
#59160=EDGE_CURVE ( 'NONE', #34558, #3167, #43762, .T. ) ;
#59166=LINE ( 'NONE', #64813, #71976 ) ;
#59171=ORIENTED_EDGE ( 'NONE', *, *, #23264, .T. ) ;
#59177=ORIENTED_EDGE ( 'NONE', *, *, #57457, .F. ) ;
#59187=ORIENTED_EDGE ( 'NONE', *, *, #47773, .T. ) ;
#59188=ORIENTED_EDGE ( 'NONE', *, *, #11438, .F. ) ;
#59194=DIRECTION ( 'NONE',  ( -1.000000000000000000, 0.000000000000000000, 0.000000000000000000 ) ) ;
#59197=DIRECTION ( 'NONE',  ( -1.000000000000000000, 0.000000000000000000, -0.000000000000000000 ) ) ;
#59215=ORIENTED_EDGE ( 'NONE', *, *, #29208, .F. ) ;
#59222=CIRCLE ( 'NONE', #63005, 42.00000000000000000 ) ;
#59227=AXIS2_PLACEMENT_3D ( 'NONE', #18713, #52560, #63494 ) ;
#59238=EDGE_CURVE ( 'NONE', #4351, #8216, #66626, .T. ) ;
#59244=ORIENTED_EDGE ( 'NONE', *, *, #17060, .F. ) ;
#59280=CARTESIAN_POINT ( 'NONE',  ( 10.00000000000000000, -37.48860685352291711, 0.8828120875899322373 ) ) ;
#59291=FACE_OUTER_BOUND ( 'NONE', #12808, .T. ) ;
#59303=VECTOR ( 'NONE', #47448, 1000.000000000000000 ) ;
#59317=CYLINDRICAL_SURFACE ( 'NONE', #59227, 16.00000000000000000 ) ;
#59323=ADVANCED_FACE ( 'NONE', ( #68546 ), #57256, .T. ) ;
#59331=CARTESIAN_POINT ( 'NONE',  ( 0.000000000000000000, 3.925862922256769583, -41.81611651403857621 ) ) ;
#59342=CARTESIAN_POINT ( 'NONE',  ( 10.00000000000000000, 30.00120703465205452, 22.64427369931179967 ) ) ;
#59352=EDGE_LOOP ( 'NONE', ( #39699, #57139, #24383, #30412, #65160, #65842, #30956, #2578, #137, #32800, #45526, #35088, #34976, #40788, #58434, #61401, #48048, #72761, #41957, #55227, #45371, #57799, #2914, #49281, #6233, #26713, #26747, #64392, #66418, #37200, #36158, #58887, #10143, #22197, #37267, #14419, #60742, #22593, #64649, #11841, #39589, #37807, #39167, #73887, #62219, #2070, #3194, #1210, #49017, #19303, #18276, #54290, #41338, #47436, #16171, #24308, #10913, #22445, #49940, #39021, #56127, #67049, #17461, #21828, #14232, #69168, #64569, #5039, #24784, #12860, #46902, #66214, #54572, #68830, #15354, #67945, #57138, #4638, #71171, #42809, #19153, #16779, #8527, #19012, #12960, #38761, #19844, #69704, #27723, #57423, #516, #35358, #31909, #41923, #41550, #7702, #44801, #8126, #58987, #9025, #45795, #48935, #39687, #17138, #26428, #30847, #26444, #34784, #28268, #48079, #70552, #32282, #63119, #6957, #4484, #17103, #64265, #11570, #4253, #70523, #13785, #72499, #39187, #5141, #31317, #74232, #17729, #64542, #50738, #32170, #57969, #71165, #9790, #18195, #22276, #8513, #11091, #59031, #7803, #16873, #64711, #36231, #70638, #17284, #73500, #63298, #13563, #47997, #114, #40242, #58074, #4165, #44045, #68987, #34941, #68265, #68527, #40034, #38874, #1534, #18053, #42962, #49824, #2646, #74054 ) ) ;
#59354=CARTESIAN_POINT ( 'NONE',  ( 10.00000000000000000, 0.000000000000000000, 0.000000000000000000 ) ) ;
#59371=CARTESIAN_POINT ( 'NONE',  ( 0.000000000000000000, -33.17418723428319538, 17.67226234102814431 ) ) ;
#59372=CARTESIAN_POINT ( 'NONE',  ( 0.000000000000000000, -6.736453364083817341, 36.88895765772630142 ) ) ;
#59384=AXIS2_PLACEMENT_3D ( 'NONE', #71992, #60001, #20505 ) ;
#59390=CIRCLE ( 'NONE', #16022, 16.00000000000000000 ) ;
#59402=DIRECTION ( 'NONE',  ( -1.000000000000000000, 0.000000000000000000, 0.000000000000000000 ) ) ;
#59415=CARTESIAN_POINT ( 'NONE',  ( -10.00000000000000000, 0.000000000000000000, 0.000000000000000000 ) ) ;
#59416=DIRECTION ( 'NONE',  ( 0.000000000000000000, 0.000000000000000000, 1.000000000000000000 ) ) ;
#59432=DIRECTION ( 'NONE',  ( -1.000000000000000000, -0.000000000000000000, 0.000000000000000000 ) ) ;
#59448=DIRECTION ( 'NONE',  ( 0.000000000000000000, -0.9510565162951565288, 0.3090169943749384029 ) ) ;
#59449=EDGE_CURVE ( 'NONE', #4529, #3167, #65398, .T. ) ;
#59461=VERTEX_POINT ( 'NONE', #20350 ) ;
#59473=CARTESIAN_POINT ( 'NONE',  ( 10.00000000000000178, 0.000000000000000000, 0.000000000000000000 ) ) ;
#59475=CYLINDRICAL_SURFACE ( 'NONE', #20856, 16.00000000000000000 ) ;
#59488=DIRECTION ( 'NONE',  ( 1.000000000000000000, 0.000000000000000000, 0.000000000000000000 ) ) ;
#59489=CARTESIAN_POINT ( 'NONE',  ( 10.00000000000000000, 0.000000000000000000, 0.000000000000000000 ) ) ;
#59495=DIRECTION ( 'NONE',  ( -1.000000000000000000, -0.000000000000000000, 0.000000000000000000 ) ) ;
#59496=EDGE_LOOP ( 'NONE', ( #13105, #50084, #9352, #57798 ) ) ;
#59499=CARTESIAN_POINT ( 'NONE',  ( 0.000000000000000000, 41.91543099594818500, 2.663952781846294915 ) ) ;
#59524=CARTESIAN_POINT ( 'NONE',  ( 10.00000000000000000, 30.84782396557248418, -21.32104025579081252 ) ) ;
#59527=CARTESIAN_POINT ( 'NONE',  ( 10.00000000000000000, 0.000000000000000000, 0.000000000000000000 ) ) ;
#59544=CARTESIAN_POINT ( 'NONE',  ( 10.00000000000000000, 0.000000000000000000, 0.000000000000000000 ) ) ;
#59578=CARTESIAN_POINT ( 'NONE',  ( 0.000000000000000000, 33.00180498840046539, 17.80606268964551120 ) ) ;
#59579=CYLINDRICAL_SURFACE ( 'NONE', #23952, 16.00000000000000000 ) ;
#59582=LINE ( 'NONE', #12956, #47423 ) ;
#59584=EDGE_CURVE ( 'NONE', #66872, #56256, #72214, .T. ) ;
#59594=DIRECTION ( 'NONE',  ( 0.000000000000000000, 0.000000000000000000, 1.000000000000000000 ) ) ;
#59600=DIRECTION ( 'NONE',  ( -1.000000000000000000, -0.000000000000000000, -0.000000000000000000 ) ) ;
#59611=DIRECTION ( 'NONE',  ( -1.000000000000000000, 0.000000000000000000, 0.000000000000000000 ) ) ;
#59623=EDGE_CURVE ( 'NONE', #61584, #11957, #61851, .T. ) ;
#59627=ORIENTED_EDGE ( 'NONE', *, *, #27213, .F. ) ;
#59630=DIRECTION ( 'NONE',  ( 0.000000000000000000, 0.000000000000000000, -1.000000000000000000 ) ) ;
#59631=ORIENTED_EDGE ( 'NONE', *, *, #12391, .T. ) ;
#59639=FACE_OUTER_BOUND ( 'NONE', #9857, .T. ) ;
#59646=DIRECTION ( 'NONE',  ( -1.000000000000000000, 0.000000000000000000, 0.000000000000000000 ) ) ;
#59676=ORIENTED_EDGE ( 'NONE', *, *, #64085, .T. ) ;
#59693=CARTESIAN_POINT ( 'NONE',  ( 0.000000000000000000, -25.88420570971381807, -27.13269053701123212 ) ) ;
#59696=CARTESIAN_POINT ( 'NONE',  ( 10.00000000000000000, 6.736453364083557105, 36.88895765772635826 ) ) ;
#59701=CIRCLE ( 'NONE', #27255, 16.00000000000000000 ) ;
#59712=CIRCLE ( 'NONE', #24872, 37.49900000000000233 ) ;
#59727=ORIENTED_EDGE ( 'NONE', *, *, #25697, .F. ) ;
#59738=LINE ( 'NONE', #55202, #54592 ) ;
#59771=VERTEX_POINT ( 'NONE', #34226 ) ;
#59785=AXIS2_PLACEMENT_3D ( 'NONE', #15112, #26022, #20755 ) ;
#59870=AXIS2_PLACEMENT_3D ( 'NONE', #20498, #4604, #27507 ) ;
#59891=CIRCLE ( 'NONE', #46672, 37.49900000000000944 ) ;
#59907=DIRECTION ( 'NONE',  ( -1.000000000000000000, -0.000000000000000000, -0.000000000000000000 ) ) ;
#59923=CIRCLE ( 'NONE', #61161, 37.49900000000001654 ) ;
#59938=EDGE_LOOP ( 'NONE', ( #34969, #42370, #23403, #55494 ) ) ;
#59967=CARTESIAN_POINT ( 'NONE',  ( 0.000000000000000000, 37.22597642581150268, 5.202137450157037435 ) ) ;
#59976=ADVANCED_FACE ( 'NONE', ( #62649 ), #56631, .T. ) ;
#59984=VECTOR ( 'NONE', #22284, 1000.000000000000000 ) ;
#59989=AXIS2_PLACEMENT_3D ( 'NONE', #52651, #15573, #39257 ) ;
#60001=DIRECTION ( 'NONE',  ( -1.000000000000000000, 0.000000000000000000, -0.000000000000000000 ) ) ;
#60013=DIRECTION ( 'NONE',  ( -1.000000000000000000, -0.000000000000000000, 0.000000000000000000 ) ) ;
#60016=FACE_OUTER_BOUND ( 'NONE', #45619, .T. ) ;
#60019=CYLINDRICAL_SURFACE ( 'NONE', #27231, 42.00000000000000000 ) ;
#60027=AXIS2_PLACEMENT_3D ( 'NONE', #55411, #67057, #15563 ) ;
#60030=AXIS2_PLACEMENT_3D ( 'NONE', #44903, #56560, #39630 ) ;
#60033=VERTEX_POINT ( 'NONE', #38957 ) ;
#60038=AXIS2_PLACEMENT_3D ( 'NONE', #6437, #61447, #44899 ) ;
#60048=EDGE_LOOP ( 'NONE', ( #18473, #68516, #24086, #46270 ) ) ;
#60053=DIRECTION ( 'NONE',  ( -1.000000000000000000, 0.000000000000000000, 0.000000000000000000 ) ) ;
#60059=CIRCLE ( 'NONE', #24031, 16.00000000000000000 ) ;
#60063=AXIS2_PLACEMENT_3D ( 'NONE', #10662, #17420, #68186 ) ;
#60077=DIRECTION ( 'NONE',  ( 0.000000000000000000, 0.000000000000000000, -1.000000000000000000 ) ) ;
#60088=EDGE_LOOP ( 'NONE', ( #11989, #48594, #63928, #64873 ) ) ;
#60091=CIRCLE ( 'NONE', #27649, 15.99999999999999822 ) ;
#60101=AXIS2_PLACEMENT_3D ( 'NONE', #11137, #50227, #68660 ) ;
#60103=CIRCLE ( 'NONE', #10886, 16.00000000000000000 ) ;
#60106=ORIENTED_EDGE ( 'NONE', *, *, #41085, .T. ) ;
#60113=VERTEX_POINT ( 'NONE', #36269 ) ;
#60139=CARTESIAN_POINT ( 'NONE',  ( 10.00000000000000000, 0.000000000000000000, 0.000000000000000000 ) ) ;
#60147=CARTESIAN_POINT ( 'NONE',  ( 4.999999999999999112, -40.98264845739755202, 9.188173127307159405 ) ) ;
#60156=DIRECTION ( 'NONE',  ( -1.000000000000000000, 0.000000000000000000, -0.000000000000000000 ) ) ;
#60194=DIRECTION ( 'NONE',  ( -1.000000000000000000, 0.000000000000000000, 0.000000000000000000 ) ) ;
#60215=ADVANCED_FACE ( 'NONE', ( #41915 ), #46446, .T. ) ;
#60265=FACE_OUTER_BOUND ( 'NONE', #8773, .T. ) ;
#60272=AXIS2_PLACEMENT_3D ( 'NONE', #59527, #24931, #29447 ) ;
#60275=CARTESIAN_POINT ( 'NONE',  ( 0.000000000000000000, -30.00120703465189465, -22.64427369931201639 ) ) ;
#60277=DIRECTION ( 'NONE',  ( -1.000000000000000000, 0.000000000000000000, 0.000000000000000000 ) ) ;
#60278=CARTESIAN_POINT ( 'NONE',  ( 10.00000000000000000, -29.81001611431024756, 22.74946021919122785 ) ) ;
#60285=ORIENTED_EDGE ( 'NONE', *, *, #39, .F. ) ;
#60290=CARTESIAN_POINT ( 'NONE',  ( 0.000000000000000000, 21.40280677340421889, -36.13751322684397138 ) ) ;
#60292=VERTEX_POINT ( 'NONE', #59578 ) ;
#60294=VECTOR ( 'NONE', #60156, 1000.000000000000000 ) ;
#60302=AXIS2_PLACEMENT_3D ( 'NONE', #42120, #54137, #53755 ) ;
#60304=ORIENTED_EDGE ( 'NONE', *, *, #38543, .F. ) ;
#60309=CARTESIAN_POINT ( 'NONE',  ( 4.999999999999999112, -40.98264845739743123, -9.188173127307734944 ) ) ;
#60313=ORIENTED_EDGE ( 'NONE', *, *, #17516, .F. ) ;
#60323=DIRECTION ( 'NONE',  ( -1.000000000000000000, 0.000000000000000000, 0.000000000000000000 ) ) ;
#60352=CARTESIAN_POINT ( 'NONE',  ( 10.00000000000000000, 21.32104025579114648, 30.84782396557224970 ) ) ;
#60353=DIRECTION ( 'NONE',  ( 0.000000000000000000, 0.000000000000000000, 1.000000000000000000 ) ) ;
#60365=VERTEX_POINT ( 'NONE', #42656 ) ;
#60370=AXIS2_PLACEMENT_3D ( 'NONE', #65607, #71216, #59594 ) ;
#60380=EDGE_CURVE ( 'NONE', #49000, #60113, #45110, .T. ) ;
#60388=CYLINDRICAL_SURFACE ( 'NONE', #48467, 16.00000000000000000 ) ;
#60393=EDGE_CURVE ( 'NONE', #14549, #35308, #68177, .T. ) ;
#60402=CYLINDRICAL_SURFACE ( 'NONE', #3046, 16.00000000000000000 ) ;
#60405=ORIENTED_EDGE ( 'NONE', *, *, #29596, .T. ) ;
#60411=AXIS2_PLACEMENT_3D ( 'NONE', #44091, #61391, #9873 ) ;
#60423=DIRECTION ( 'NONE',  ( -1.000000000000000000, 0.000000000000000000, 0.000000000000000000 ) ) ;
#60430=ORIENTED_EDGE ( 'NONE', *, *, #16810, .F. ) ;
#60469=EDGE_CURVE ( 'NONE', #48031, #36613, #45641, .T. ) ;
#60472=VERTEX_POINT ( 'NONE', #73802 ) ;
#60492=LINE ( 'NONE', #65750, #53701 ) ;
#60507=VERTEX_POINT ( 'NONE', #9552 ) ;
#60516=VERTEX_POINT ( 'NONE', #39613 ) ;
#60529=CARTESIAN_POINT ( 'NONE',  ( -3.308722450212110699E-21, 16.95692799528845640, -2.500000000000000000 ) ) ;
#60550=DIRECTION ( 'NONE',  ( -1.000000000000000000, -0.000000000000000000, 0.000000000000000000 ) ) ;
#60564=CIRCLE ( 'NONE', #53360, 16.00000000000000000 ) ;
#60572=ORIENTED_EDGE ( 'NONE', *, *, #57235, .F. ) ;
#60586=ORIENTED_EDGE ( 'NONE', *, *, #51096, .T. ) ;
#60607=DIRECTION ( 'NONE',  ( 1.000000000000000000, 0.000000000000000000, 0.000000000000000000 ) ) ;
#60625=AXIS2_PLACEMENT_3D ( 'NONE', #57992, #29766, #161 ) ;
#60647=CARTESIAN_POINT ( 'NONE',  ( -10.00000000000000000, 0.000000000000000000, 0.000000000000000000 ) ) ;
#60668=DIRECTION ( 'NONE',  ( -1.000000000000000000, -0.000000000000000000, 0.000000000000000000 ) ) ;
#60680=CARTESIAN_POINT ( 'NONE',  ( 5.000000000000000000, 27.75498641678742473, 31.52238457039609187 ) ) ;
#60681=CARTESIAN_POINT ( 'NONE',  ( 0.000000000000000000, 0.000000000000000000, 0.000000000000000000 ) ) ;
#60692=ORIENTED_EDGE ( 'NONE', *, *, #11388, .F. ) ;
#60703=CARTESIAN_POINT ( 'NONE',  ( 4.999999999999999112, -21.40280677340345505, -36.13751322684441192 ) ) ;
#60742=ORIENTED_EDGE ( 'NONE', *, *, #58317, .F. ) ;
#60778=DIRECTION ( 'NONE',  ( -1.000000000000000000, -0.000000000000000000, 0.000000000000000000 ) ) ;
#60798=EDGE_CURVE ( 'NONE', #47938, #65417, #28343, .T. ) ;
#60806=LINE ( 'NONE', #4413, #56487 ) ;
#60809=CARTESIAN_POINT ( 'NONE',  ( 10.00000000000000000, -37.01155633439053361, -6.555932627142825986 ) ) ;
#60823=CIRCLE ( 'NONE', #8010, 37.49900000000000233 ) ;
#60839=DIRECTION ( 'NONE',  ( -1.000000000000000000, 0.000000000000000000, 0.000000000000000000 ) ) ;
#60841=ORIENTED_EDGE ( 'NONE', *, *, #56857, .F. ) ;
#60864=EDGE_LOOP ( 'NONE', ( #59727, #5387, #30801, #23654 ) ) ;
#60866=ORIENTED_EDGE ( 'NONE', *, *, #12496, .F. ) ;
#60867=EDGE_CURVE ( 'NONE', #25146, #56950, #30804, .T. ) ;
#60888=CYLINDRICAL_SURFACE ( 'NONE', #32490, 16.00000000000000000 ) ;
#60904=CIRCLE ( 'NONE', #10503, 37.49900000000000233 ) ;
#60905=CARTESIAN_POINT ( 'NONE',  ( 10.00000000000000000, -17.67226234102801286, -33.17418723428327354 ) ) ;
#60928=EDGE_CURVE ( 'NONE', #43117, #23577, #53618, .T. ) ;
#60940=ORIENTED_EDGE ( 'NONE', *, *, #35828, .T. ) ;
#60946=AXIS2_PLACEMENT_3D ( 'NONE', #4354, #46323, #23033 ) ;
#60951=EDGE_CURVE ( 'NONE', #16018, #8967, #3837, .T. ) ;
#60969=ORIENTED_EDGE ( 'NONE', *, *, #48957, .T. ) ;
#60978=CARTESIAN_POINT ( 'NONE',  ( 10.00000000000000000, -30.84782396557201878, -21.32104025579148399 ) ) ;
#60982=CYLINDRICAL_SURFACE ( 'NONE', #59785, 16.00000000000000000 ) ;
#60983=CIRCLE ( 'NONE', #28555, 37.49900000000000944 ) ;
#61004=DIRECTION ( 'NONE',  ( 0.000000000000000000, 0.000000000000000000, 1.000000000000000000 ) ) ;
#61010=EDGE_CURVE ( 'NONE', #24964, #64024, #60823, .T. ) ;
#61020=ORIENTED_EDGE ( 'NONE', *, *, #69762, .F. ) ;
#61039=DIRECTION ( 'NONE',  ( 1.000000000000000000, -0.000000000000000000, 0.000000000000000000 ) ) ;
#61042=CARTESIAN_POINT ( 'NONE',  ( 0.000000000000000000, 22.64427369931212297, -30.00120703465181293 ) ) ;
#61096=VECTOR ( 'NONE', #19545, 1000.000000000000000 ) ;
#61109=AXIS2_PLACEMENT_3D ( 'NONE', #8252, #31177, #47009 ) ;
#61112=VECTOR ( 'NONE', #47058, 1000.000000000000000 ) ;
#61114=ORIENTED_EDGE ( 'NONE', *, *, #36891, .T. ) ;
#61117=AXIS2_PLACEMENT_3D ( 'NONE', #37707, #8756, #26030 ) ;
#61119=CYLINDRICAL_SURFACE ( 'NONE', #21275, 16.00000000000000000 ) ;
#61149=DIRECTION ( 'NONE',  ( 0.000000000000000000, 0.000000000000000000, 1.000000000000000000 ) ) ;
#61161=AXIS2_PLACEMENT_3D ( 'NONE', #42776, #47309, #70212 ) ;
#61177=CARTESIAN_POINT ( 'NONE',  ( 10.00000000000000000, 37.16516213103285082, -4.992566952384588141 ) ) ;
#61206=CARTESIAN_POINT ( 'NONE',  ( 10.00000000000000000, 37.22597642581158084, 10.79786254984347593 ) ) ;
#61243=ORIENTED_EDGE ( 'NONE', *, *, #11230, .F. ) ;
#61252=CARTESIAN_POINT ( 'NONE',  ( 0.000000000000000000, 0.8828120875900632436, 37.48860685352291000 ) ) ;
#61256=CARTESIAN_POINT ( 'NONE',  ( 0.000000000000000000, -21.53537804866103045, 30.80686688397002371 ) ) ;
#61265=DIRECTION ( 'NONE',  ( -1.000000000000000000, -0.000000000000000000, -0.000000000000000000 ) ) ;
#61298=ADVANCED_FACE ( 'NONE', ( #59040 ), #71765, .T. ) ;
#61302=VERTEX_POINT ( 'NONE', #43239 ) ;
#61349=CYLINDRICAL_SURFACE ( 'NONE', #64336, 42.00000000000000000 ) ;
#61355=DIRECTION ( 'NONE',  ( 1.000000000000000000, -0.000000000000000000, -0.000000000000000000 ) ) ;
#61357=DIRECTION ( 'NONE',  ( 0.000000000000000000, 1.000000000000000000, 3.491481338843133750E-15 ) ) ;
#61364=CARTESIAN_POINT ( 'NONE',  ( 0.000000000000000000, -10.74501242461258244, -35.92658777277521409 ) ) ;
#61366=EDGE_CURVE ( 'NONE', #54442, #25438, #59701, .T. ) ;
#61376=DIRECTION ( 'NONE',  ( 0.000000000000000000, -0.9510565162951565288, 0.3090169943749382364 ) ) ;
#61387=EDGE_CURVE ( 'NONE', #19308, #4312, #21241, .T. ) ;
#61391=DIRECTION ( 'NONE',  ( -1.000000000000000000, -0.000000000000000000, -0.000000000000000000 ) ) ;
#61401=ORIENTED_EDGE ( 'NONE', *, *, #11691, .T. ) ;
#61419=AXIS2_PLACEMENT_3D ( 'NONE', #70387, #12882, #63303 ) ;
#61447=DIRECTION ( 'NONE',  ( -1.000000000000000000, 0.000000000000000000, 0.000000000000000000 ) ) ;
#61449=DIRECTION ( 'NONE',  ( -1.000000000000000000, 0.000000000000000000, -0.000000000000000000 ) ) ;
#61501=VERTEX_POINT ( 'NONE', #26281 ) ;
#61508=ORIENTED_EDGE ( 'NONE', *, *, #70797, .F. ) ;
#61512=ORIENTED_EDGE ( 'NONE', *, *, #56169, .F. ) ;
#61530=ADVANCED_FACE ( 'NONE', ( #33033 ), #49951, .T. ) ;
#61541=ORIENTED_EDGE ( 'NONE', *, *, #52512, .F. ) ;
#61556=CARTESIAN_POINT ( 'NONE',  ( 0.000000000000000000, 6.555932627142418312, 37.01155633439060466 ) ) ;
#61563=EDGE_CURVE ( 'NONE', #8860, #16018, #2097, .T. ) ;
#61568=CARTESIAN_POINT ( 'NONE',  ( 0.000000000000000000, -40.68715046381921496, -10.41901085202121280 ) ) ;
#61569=DIRECTION ( 'NONE',  ( 0.000000000000000000, 0.000000000000000000, 1.000000000000000000 ) ) ;
#61572=VECTOR ( 'NONE', #18952, 1000.000000000000000 ) ;
#61575=DIRECTION ( 'NONE',  ( 1.000000000000000000, -0.000000000000000000, -0.000000000000000000 ) ) ;
#61584=VERTEX_POINT ( 'NONE', #63858 ) ;
#61595=DIRECTION ( 'NONE',  ( -1.000000000000000000, 0.000000000000000000, 0.000000000000000000 ) ) ;
#61604=EDGE_CURVE ( 'NONE', #9618, #37989, #12825, .T. ) ;
#61635=LINE ( 'NONE', #15768, #45227 ) ;
#61649=DIRECTION ( 'NONE',  ( -1.000000000000000000, 0.000000000000000000, 0.000000000000000000 ) ) ;
#61669=VERTEX_POINT ( 'NONE', #57843 ) ;
#61674=ORIENTED_EDGE ( 'NONE', *, *, #64526, .F. ) ;
#61676=ORIENTED_EDGE ( 'NONE', *, *, #25190, .T. ) ;
#61679=ORIENTED_EDGE ( 'NONE', *, *, #43474, .F. ) ;
#61689=CIRCLE ( 'NONE', #73645, 37.49900000000000233 ) ;
#61692=AXIS2_PLACEMENT_3D ( 'NONE', #44353, #16148, #4515 ) ;
#61724=DIRECTION ( 'NONE',  ( 1.000000000000000000, 0.000000000000000000, -0.000000000000000000 ) ) ;
#61755=DIRECTION ( 'NONE',  ( -1.000000000000000000, -0.000000000000000000, -0.000000000000000000 ) ) ;
#61757=ORIENTED_EDGE ( 'NONE', *, *, #70589, .T. ) ;
#61760=DIRECTION ( 'NONE',  ( 0.000000000000000000, 0.3090169943749482839, -0.9510565162951533091 ) ) ;
#61773=ORIENTED_EDGE ( 'NONE', *, *, #71180, .F. ) ;
#61782=ORIENTED_EDGE ( 'NONE', *, *, #7201, .T. ) ;
#61793=CARTESIAN_POINT ( 'NONE',  ( 0.000000000000000000, 0.000000000000000000, 0.000000000000000000 ) ) ;
#61823=DIRECTION ( 'NONE',  ( 0.000000000000000000, 0.000000000000000000, 1.000000000000000000 ) ) ;
#61826=AXIS2_PLACEMENT_3D ( 'NONE', #7786, #35982, #64564 ) ;
#61843=VECTOR ( 'NONE', #71653, 1000.000000000000000 ) ;
#61851=CIRCLE ( 'NONE', #70239, 16.00000000000000000 ) ;
#61854=VECTOR ( 'NONE', #37153, 1000.000000000000000 ) ;
#61856=VERTEX_POINT ( 'NONE', #4405 ) ;
#61885=EDGE_LOOP ( 'NONE', ( #15579, #62947, #2738, #3302 ) ) ;
#61891=ORIENTED_EDGE ( 'NONE', *, *, #15242, .T. ) ;
#61905=DIRECTION ( 'NONE',  ( 0.000000000000000000, 0.8910065241883656784, 0.4539904997395511899 ) ) ;
#61914=CARTESIAN_POINT ( 'NONE',  ( 10.00000000000000000, 0.000000000000000000, 0.000000000000000000 ) ) ;
#61935=CARTESIAN_POINT ( 'NONE',  ( 10.00000000000000000, -6.555932627142143865, -37.01155633439065440 ) ) ;
#61937=DIRECTION ( 'NONE',  ( 0.000000000000000000, -0.7071067811865535679, 0.7071067811865413555 ) ) ;
#61963=FACE_OUTER_BOUND ( 'NONE', #48263, .T. ) ;
#61969=ORIENTED_EDGE ( 'NONE', *, *, #33723, .T. ) ;
#61970=DIRECTION ( 'NONE',  ( 0.000000000000000000, 0.000000000000000000, 1.000000000000000000 ) ) ;
#62016=MANIFOLD_SOLID_BREP ( 'Cut-Extrude-Thin1', #3209 ) ;
#62027=PRODUCT ( 'small gear_ISO - Spur gear 2M 40T 20PA 10FW ---S40A75H50L20.0N', 'small gear_ISO - Spur gear 2M 40T 20PA 10FW ---S40A75H50L20.0N', '', ( #17029 ) ) ;
#62031=DIRECTION ( 'NONE',  ( 0.000000000000000000, 1.000000000000000000, -9.787530781167596740E-16 ) ) ;
#62039=DIRECTION ( 'NONE',  ( -1.000000000000000000, 0.000000000000000000, 0.000000000000000000 ) ) ;
#62058=CARTESIAN_POINT ( 'NONE',  ( 10.00000000000000000, 0.000000000000000000, 0.000000000000000000 ) ) ;
#62059=EDGE_CURVE ( 'NONE', #55579, #38385, #12927, .T. ) ;
#62061=VERTEX_POINT ( 'NONE', #13115 ) ;
#62068=VERTEX_POINT ( 'NONE', #17660 ) ;
#62085=DIRECTION ( 'NONE',  ( 1.000000000000000000, 0.000000000000000000, 0.000000000000000000 ) ) ;
#62086=AXIS2_PLACEMENT_3D ( 'NONE', #11606, #50725, #17632 ) ;
#62091=VECTOR ( 'NONE', #61575, 1000.000000000000000 ) ;
#62097=CARTESIAN_POINT ( 'NONE',  ( 10.00000000000000000, 0.000000000000000000, 0.000000000000000000 ) ) ;
#62110=STYLED_ITEM ( 'NONE', ( #67309 ), #62016 ) ;
#62114=CIRCLE ( 'NONE', #28507, 15.99999999999999822 ) ;
#62122=DIRECTION ( 'NONE',  ( -1.000000000000000000, -0.000000000000000000, -0.000000000000000000 ) ) ;
#62126=ORIENTED_EDGE ( 'NONE', *, *, #42222, .T. ) ;
#62142=ORIENTED_EDGE ( 'NONE', *, *, #4117, .F. ) ;
#62145=EDGE_CURVE ( 'NONE', #17733, #19308, #11749, .T. ) ;
#62149=ORIENTED_EDGE ( 'NONE', *, *, #29114, .T. ) ;
#62159=DIRECTION ( 'NONE',  ( 0.000000000000000000, 0.000000000000000000, -1.000000000000000000 ) ) ;
#62175=CARTESIAN_POINT ( 'NONE',  ( 4.999999999999999112, 10.41901085202135491, -40.68715046381917944 ) ) ;
#62180=ORIENTED_EDGE ( 'NONE', *, *, #51442, .F. ) ;
#62193=DIRECTION ( 'NONE',  ( 1.000000000000000000, -0.000000000000000000, -0.000000000000000000 ) ) ;
#62199=CARTESIAN_POINT ( 'NONE',  ( 10.00000000000000000, 9.188173127307898369, -40.98264845739739570 ) ) ;
#62201=AXIS2_PLACEMENT_3D ( 'NONE', #11326, #62867, #56472 ) ;
#62209=DIRECTION ( 'NONE',  ( -1.000000000000000000, -0.000000000000000000, 0.000000000000000000 ) ) ;
#62219=ORIENTED_EDGE ( 'NONE', *, *, #737, .F. ) ;
#62229=ORIENTED_EDGE ( 'NONE', *, *, #63003, .T. ) ;
#62250=CIRCLE ( 'NONE', #20204, 16.00000000000000000 ) ;
#62252=DIRECTION ( 'NONE',  ( -1.000000000000000000, 0.000000000000000000, -0.000000000000000000 ) ) ;
#62269=CYLINDRICAL_SURFACE ( 'NONE', #66640, 16.00000000000000000 ) ;
#62274=DIRECTION ( 'NONE',  ( -1.000000000000000000, 0.000000000000000000, 0.000000000000000000 ) ) ;
#62276=VERTEX_POINT ( 'NONE', #36416 ) ;
#62284=ORIENTED_EDGE ( 'NONE', *, *, #6642, .T. ) ;
#62285=AXIS2_PLACEMENT_3D ( 'NONE', #3492, #26400, #53864 ) ;
#62302=DIRECTION ( 'NONE',  ( 0.000000000000000000, 0.000000000000000000, 1.000000000000000000 ) ) ;
#62308=AXIS2_PLACEMENT_3D ( 'NONE', #44301, #61595, #4466 ) ;
#62314=EDGE_LOOP ( 'NONE', ( #65368, #12178, #72578, #62625 ) ) ;
#62327=EDGE_CURVE ( 'NONE', #63369, #50488, #16535, .T. ) ;
#62332=VECTOR ( 'NONE', #13245, 1000.000000000000000 ) ;
#62338=DIRECTION ( 'NONE',  ( -1.000000000000000000, 0.000000000000000000, 0.000000000000000000 ) ) ;
#62346=VECTOR ( 'NONE', #54803, 1000.000000000000000 ) ;
#62352=LINE ( 'NONE', #17576, #4729 ) ;
#62384=FACE_OUTER_BOUND ( 'NONE', #70551, .T. ) ;
#62389=CARTESIAN_POINT ( 'NONE',  ( 10.00000000000000000, 0.8828120875905820508, -37.48860685352290290 ) ) ;
#62400=CARTESIAN_POINT ( 'NONE',  ( 10.00000000000000000, -17.80606268964563554, 33.00180498840040855 ) ) ;
#62403=CARTESIAN_POINT ( 'NONE',  ( 4.999999999999999112, -2.663952781845850826, -41.91543099594819921 ) ) ;
#62409=CIRCLE ( 'NONE', #54017, 16.00000000000000355 ) ;
#62414=DIRECTION ( 'NONE',  ( 0.000000000000000000, 0.1564344650402244852, 0.9876883405951387696 ) ) ;
#62415=DIRECTION ( 'NONE',  ( 0.000000000000000000, 0.000000000000000000, 1.000000000000000000 ) ) ;
#62444=DIRECTION ( 'NONE',  ( 0.000000000000000000, 0.000000000000000000, 1.000000000000000000 ) ) ;
#62447=AXIS2_PLACEMENT_3D ( 'NONE', #44832, #62122, #72629 ) ;
#62481=EDGE_CURVE ( 'NONE', #41070, #56046, #72833, .T. ) ;
#62504=AXIS2_PLACEMENT_3D ( 'NONE', #38985, #45754, #5898 ) ;
#62549=VERTEX_POINT ( 'NONE', #69080 ) ;
#62560=VECTOR ( 'NONE', #4798, 1000.000000000000000 ) ;
#62561=AXIS2_PLACEMENT_3D ( 'NONE', #58839, #34794, #18238 ) ;
#62600=VERTEX_POINT ( 'NONE', #47257 ) ;
#62616=AXIS2_PLACEMENT_3D ( 'NONE', #72040, #8898, #72410 ) ;
#62625=ORIENTED_EDGE ( 'NONE', *, *, #45284, .T. ) ;
#62648=CARTESIAN_POINT ( 'NONE',  ( 10.00000000000000000, 21.32104025579114648, 30.84782396557224970 ) ) ;
#62649=FACE_OUTER_BOUND ( 'NONE', #68153, .T. ) ;
#62650=EDGE_CURVE ( 'NONE', #29886, #66673, #27419, .T. ) ;
#62686=EDGE_CURVE ( 'NONE', #68784, #14616, #73024, .T. ) ;
#62743=DIRECTION ( 'NONE',  ( -1.000000000000000000, -0.000000000000000000, 0.000000000000000000 ) ) ;
#62745=DIRECTION ( 'NONE',  ( -1.000000000000000000, 0.000000000000000000, 0.000000000000000000 ) ) ;
#62755=EDGE_CURVE ( 'NONE', #40253, #71453, #36704, .T. ) ;
#62763=CYLINDRICAL_SURFACE ( 'NONE', #43508, 16.00000000000000000 ) ;
#62772=DIRECTION ( 'NONE',  ( 0.000000000000000000, 0.000000000000000000, 1.000000000000000000 ) ) ;
#62777=LINE ( 'NONE', #68017, #38338 ) ;
#62786=FACE_OUTER_BOUND ( 'NONE', #69256, .T. ) ;
#62791=VECTOR ( 'NONE', #53614, 1000.000000000000000 ) ;
#62798=AXIS2_PLACEMENT_3D ( 'NONE', #12061, #39532, #34618 ) ;
#62862=FACE_BOUND ( 'NONE', #29566, .T. ) ;
#62867=DIRECTION ( 'NONE',  ( -1.000000000000000000, -0.000000000000000000, -0.000000000000000000 ) ) ;
#62882=CARTESIAN_POINT ( 'NONE',  ( 0.000000000000000000, 37.58145647212455032, -0.6853352020786441789 ) ) ;
#62905=ORIENTED_EDGE ( 'NONE', *, *, #2783, .T. ) ;
#62913=CARTESIAN_POINT ( 'NONE',  ( 10.00000000000000000, 30.00120703465236716, -22.64427369931138756 ) ) ;
#62947=ORIENTED_EDGE ( 'NONE', *, *, #6642, .F. ) ;
#62959=AXIS2_PLACEMENT_3D ( 'NONE', #35838, #24571, #40376 ) ;
#62973=ORIENTED_EDGE ( 'NONE', *, *, #49624, .T. ) ;
#62977=DIRECTION ( 'NONE',  ( -1.000000000000000000, -0.000000000000000000, -0.000000000000000000 ) ) ;
#62990=ADVANCED_FACE ( 'NONE', ( #23864 ), #1352, .T. ) ;
#62995=CIRCLE ( 'NONE', #26948, 37.49900000000000944 ) ;
#63003=EDGE_CURVE ( 'NONE', #34558, #49532, #68992, .T. ) ;
#63005=AXIS2_PLACEMENT_3D ( 'NONE', #15489, #27125, #50805 ) ;
#63015=VERTEX_POINT ( 'NONE', #34776 ) ;
#63019=CIRCLE ( 'NONE', #4183, 37.49900000000000233 ) ;
#63023=ORIENTED_EDGE ( 'NONE', *, *, #38523, .F. ) ;
#63029=ORIENTED_EDGE ( 'NONE', *, *, #25190, .F. ) ;
#63036=EDGE_CURVE ( 'NONE', #18829, #54942, #43069, .T. ) ;
#63079=DIRECTION ( 'NONE',  ( 0.000000000000000000, 0.7071067811865487940, -0.7071067811865462405 ) ) ;
#63084=DIRECTION ( 'NONE',  ( 0.000000000000000000, 0.000000000000000000, 1.000000000000000000 ) ) ;
#63088=ORIENTED_EDGE ( 'NONE', *, *, #8745, .F. ) ;
#63091=CARTESIAN_POINT ( 'NONE',  ( 0.000000000000000000, -33.79645857604501913, -16.45098606841161626 ) ) ;
#63092=CIRCLE ( 'NONE', #6661, 37.49900000000000944 ) ;
#63103=VERTEX_POINT ( 'NONE', #7318 ) ;
#63119=ORIENTED_EDGE ( 'NONE', *, *, #29371, .F. ) ;
#63125=CARTESIAN_POINT ( 'NONE',  ( 10.00000000000000000, 0.000000000000000000, 0.000000000000000000 ) ) ;
#63166=VECTOR ( 'NONE', #41459, 1000.000000000000000 ) ;
#63168=ORIENTED_EDGE ( 'NONE', *, *, #44815, .T. ) ;
#63178=CARTESIAN_POINT ( 'NONE',  ( 0.000000000000000000, 0.000000000000000000, 37.49900000000000233 ) ) ;
#63235=FACE_OUTER_BOUND ( 'NONE', #17040, .T. ) ;
#63237=EDGE_CURVE ( 'NONE', #47001, #49804, #10654, .T. ) ;
#63251=ORIENTED_EDGE ( 'NONE', *, *, #48957, .F. ) ;
#63266=DIRECTION ( 'NONE',  ( 1.000000000000000000, 0.000000000000000000, 0.000000000000000000 ) ) ;
#63275=SHAPE_DEFINITION_REPRESENTATION ( #38597, #31559 ) ;
#63277=DIRECTION ( 'NONE',  ( 1.000000000000000000, 0.000000000000000000, -0.000000000000000000 ) ) ;
#63297=DIRECTION ( 'NONE',  ( -1.000000000000000000, -0.000000000000000000, 0.000000000000000000 ) ) ;
#63298=ORIENTED_EDGE ( 'NONE', *, *, #46870, .T. ) ;
#63303=DIRECTION ( 'NONE',  ( 0.000000000000000000, 0.000000000000000000, 1.000000000000000000 ) ) ;
#63354=ORIENTED_EDGE ( 'NONE', *, *, #31000, .F. ) ;
#63364=DIRECTION ( 'NONE',  ( 0.000000000000000000, 0.000000000000000000, 1.000000000000000000 ) ) ;
#63369=VERTEX_POINT ( 'NONE', #35437 ) ;
#63370=FACE_OUTER_BOUND ( 'NONE', #1261, .T. ) ;
#63379=FACE_OUTER_BOUND ( 'NONE', #14673, .T. ) ;
#63385=AXIS2_PLACEMENT_3D ( 'NONE', #71264, #14124, #37075 ) ;
#63387=CIRCLE ( 'NONE', #42985, 16.00000000000000000 ) ;
#63399=CARTESIAN_POINT ( 'NONE',  ( 0.000000000000000000, -37.58145647212455032, 0.6853352020789044152 ) ) ;
#63413=EDGE_CURVE ( 'NONE', #11375, #66589, #40344, .T. ) ;
#63427=DIRECTION ( 'NONE',  ( 1.000000000000000000, -0.000000000000000000, 0.000000000000000000 ) ) ;
#63434=AXIS2_PLACEMENT_3D ( 'NONE', #18563, #41502, #53160 ) ;
#63439=CARTESIAN_POINT ( 'NONE',  ( 4.999999999999999112, -3.925862922255855647, -41.81611651403866858 ) ) ;
#63446=VERTEX_POINT ( 'NONE', #37306 ) ;
#63447=ORIENTED_EDGE ( 'NONE', *, *, #53392, .T. ) ;
#63456=ORIENTED_EDGE ( 'NONE', *, *, #35123, .T. ) ;
#63464=CARTESIAN_POINT ( 'NONE',  ( -10.00000000000000000, 0.000000000000000000, 0.000000000000000000 ) ) ;
#63480=ORIENTED_EDGE ( 'NONE', *, *, #10682, .F. ) ;
#63494=DIRECTION ( 'NONE',  ( 0.000000000000000000, 0.000000000000000000, 1.000000000000000000 ) ) ;
#63515=DIRECTION ( 'NONE',  ( 0.000000000000000000, 0.7071067811865439090, 0.7071067811865512365 ) ) ;
#63517=DIRECTION ( 'NONE',  ( -1.000000000000000000, 0.000000000000000000, 0.000000000000000000 ) ) ;
#63537=CARTESIAN_POINT ( 'NONE',  ( 10.00000000000000000, 0.000000000000000000, 0.000000000000000000 ) ) ;
#63557=ORIENTED_EDGE ( 'NONE', *, *, #53137, .F. ) ;
#63558=VERTEX_POINT ( 'NONE', #30159 ) ;
#63567=CARTESIAN_POINT ( 'NONE',  ( 10.00000000000000000, 40.68715046381928602, 10.41901085202092503 ) ) ;
#63576=AXIS2_PLACEMENT_3D ( 'NONE', #33811, #11251, #28165 ) ;
#63588=CARTESIAN_POINT ( 'NONE',  ( -10.00000000000000000, 0.000000000000000000, 0.000000000000000000 ) ) ;
#63592=EDGE_CURVE ( 'NONE', #6488, #26693, #47462, .T. ) ;
#63600=CARTESIAN_POINT ( 'NONE',  ( 10.00000000000000000, 36.13751322684449718, -21.40280677340333071 ) ) ;
#63610=CARTESIAN_POINT ( 'NONE',  ( 0.000000000000000000, 0.000000000000000000, 0.000000000000000000 ) ) ;
#63612=CARTESIAN_POINT ( 'NONE',  ( 0.000000000000000000, 2.446882695291915554E-15, 2.500000000000016431 ) ) ;
#63615=DIRECTION ( 'NONE',  ( 0.000000000000000000, 0.000000000000000000, 1.000000000000000000 ) ) ;
#63616=ORIENTED_EDGE ( 'NONE', *, *, #70886, .F. ) ;
#63663=CARTESIAN_POINT ( 'NONE',  ( 10.00000000000000000, 0.000000000000000000, 0.000000000000000000 ) ) ;
#63678=CARTESIAN_POINT ( 'NONE',  ( 10.00000000000000000, -30.80686688396994910, -21.53537804866113703 ) ) ;
#63683=CIRCLE ( 'NONE', #49214, 16.00000000000000000 ) ;
#63692=DIRECTION ( 'NONE',  ( 0.000000000000000000, -6.938893903907228378E-15, 1.000000000000000000 ) ) ;
#63706=AXIS2_PLACEMENT_3D ( 'NONE', #64286, #17298, #46990 ) ;
#63715=EDGE_LOOP ( 'NONE', ( #24965, #4123, #8034, #32243 ) ) ;
#63722=CARTESIAN_POINT ( 'NONE',  ( -10.00000000000000000, 0.000000000000000000, 0.000000000000000000 ) ) ;
#63727=VERTEX_POINT ( 'NONE', #63567 ) ;
#63739=VERTEX_POINT ( 'NONE', #68834 ) ;
#63743=ORIENTED_EDGE ( 'NONE', *, *, #71718, .T. ) ;
#63757=EDGE_LOOP ( 'NONE', ( #58703, #36085, #27352, #46410 ) ) ;
#63761=ORIENTED_EDGE ( 'NONE', *, *, #69941, .F. ) ;
#63803=DIRECTION ( 'NONE',  ( -1.000000000000000000, -0.000000000000000000, 0.000000000000000000 ) ) ;
#63805=CIRCLE ( 'NONE', #1423, 16.00000000000000000 ) ;
#63814=EDGE_CURVE ( 'NONE', #3856, #54680, #66028, .T. ) ;
#63818=ORIENTED_EDGE ( 'NONE', *, *, #19577, .T. ) ;
#63846=ORIENTED_EDGE ( 'NONE', *, *, #28711, .F. ) ;
#63858=CARTESIAN_POINT ( 'NONE',  ( 0.000000000000000000, -37.16516213103280108, 4.992566952384862589 ) ) ;
#63873=DIRECTION ( 'NONE',  ( 1.000000000000000000, 0.000000000000000000, -0.000000000000000000 ) ) ;
#63887=DIRECTION ( 'NONE',  ( -1.000000000000000000, -0.000000000000000000, 0.000000000000000000 ) ) ;
#63897=DIRECTION ( 'NONE',  ( 0.000000000000000000, 0.000000000000000000, 1.000000000000000000 ) ) ;
#63928=ORIENTED_EDGE ( 'NONE', *, *, #45483, .F. ) ;
#63934=CARTESIAN_POINT ( 'NONE',  ( 0.000000000000000000, -2.663952781846440576, 41.91543099594817789 ) ) ;
#63952=DIRECTION ( 'NONE',  ( -1.000000000000000000, -0.000000000000000000, -0.000000000000000000 ) ) ;
#63955=DIRECTION ( 'NONE',  ( 0.000000000000000000, -0.1564344650402380854, 0.9876883405951365491 ) ) ;
#63960=ORIENTED_EDGE ( 'NONE', *, *, #33189, .T. ) ;
#63973=DIRECTION ( 'NONE',  ( 0.000000000000000000, -1.000000000000000000, -1.047444401652940007E-14 ) ) ;
#63976=ORIENTED_EDGE ( 'NONE', *, *, #12230, .F. ) ;
#63979=ORIENTED_EDGE ( 'NONE', *, *, #66083, .F. ) ;
#63988=FACE_OUTER_BOUND ( 'NONE', #48997, .T. ) ;
#63995=DIRECTION ( 'NONE',  ( 0.000000000000000000, 0.000000000000000000, 1.000000000000000000 ) ) ;
#64011=CIRCLE ( 'NONE', #56826, 37.49900000000000944 ) ;
#64024=VERTEX_POINT ( 'NONE', #61252 ) ;
#64041=ADVANCED_FACE ( 'NONE', ( #25915 ), #57009, .T. ) ;
#64059=FACE_OUTER_BOUND ( 'NONE', #11134, .T. ) ;
#64068=DIRECTION ( 'NONE',  ( -1.000000000000000000, 0.000000000000000000, 0.000000000000000000 ) ) ;
#64072=DIRECTION ( 'NONE',  ( 0.000000000000000000, 0.000000000000000000, -1.000000000000000000 ) ) ;
#64085=EDGE_CURVE ( 'NONE', #6463, #34044, #22784, .T. ) ;
#64105=ADVANCED_FACE ( 'NONE', ( #37067 ), #2886, .F. ) ;
#64110=VERTEX_POINT ( 'NONE', #27151 ) ;
#64124=ADVANCED_FACE ( 'NONE', ( #60016 ), #8116, .T. ) ;
#64135=ORIENTED_EDGE ( 'NONE', *, *, #64085, .F. ) ;
#64136=CIRCLE ( 'NONE', #66543, 42.00000000000000000 ) ;
#64151=ORIENTED_EDGE ( 'NONE', *, *, #37454, .F. ) ;
#64157=ORIENTED_EDGE ( 'NONE', *, *, #71173, .F. ) ;
#64200=CARTESIAN_POINT ( 'NONE',  ( 10.00000000000000000, -35.92658777277502935, -10.74501242461320594 ) ) ;
#64204=CARTESIAN_POINT ( 'NONE',  ( 10.00000000000000000, 2.663952781846149254, 41.91543099594818500 ) ) ;
#64205=FACE_OUTER_BOUND ( 'NONE', #16551, .T. ) ;
#64207=ORIENTED_EDGE ( 'NONE', *, *, #15248, .F. ) ;
#64226=LINE ( 'NONE', #11586, #65625 ) ;
#64228=DIRECTION ( 'NONE',  ( 0.000000000000000000, 0.000000000000000000, 1.000000000000000000 ) ) ;
#64265=ORIENTED_EDGE ( 'NONE', *, *, #61366, .F. ) ;
#64268=CARTESIAN_POINT ( 'NONE',  ( 10.00000000000000000, 0.000000000000000000, 0.000000000000000000 ) ) ;
#64272=DIRECTION ( 'NONE',  ( -1.000000000000000000, -0.000000000000000000, -0.000000000000000000 ) ) ;
#64275=ORIENTED_EDGE ( 'NONE', *, *, #67071, .T. ) ;
#64282=EDGE_CURVE ( 'NONE', #57971, #37558, #42043, .T. ) ;
#64283=CARTESIAN_POINT ( 'NONE',  ( 0.000000000000000000, 0.000000000000000000, 0.000000000000000000 ) ) ;
#64286=CARTESIAN_POINT ( 'NONE',  ( 0.000000000000000000, 0.000000000000000000, 0.000000000000000000 ) ) ;
#64294=ORIENTED_EDGE ( 'NONE', *, *, #13247, .T. ) ;
#64299=CARTESIAN_POINT ( 'NONE',  ( 10.00000000000000000, 37.48860685352291000, 0.8828120875901893649 ) ) ;
#64302=CYLINDRICAL_SURFACE ( 'NONE', #52792, 42.00000000000000000 ) ;
#64309=FACE_OUTER_BOUND ( 'NONE', #32915, .T. ) ;
#64313=CARTESIAN_POINT ( 'NONE',  ( 10.00000000000000000, -33.79645857604501913, -16.45098606841161626 ) ) ;
#64323=CARTESIAN_POINT ( 'NONE',  ( 0.000000000000000000, 0.000000000000000000, 0.000000000000000000 ) ) ;
#64325=DIRECTION ( 'NONE',  ( -1.000000000000000000, 0.000000000000000000, 0.000000000000000000 ) ) ;
#64328=DIRECTION ( 'NONE',  ( -1.000000000000000000, 0.000000000000000000, 0.000000000000000000 ) ) ;
#64332=AXIS2_PLACEMENT_3D ( 'NONE', #71309, #19814, #60077 ) ;
#64336=AXIS2_PLACEMENT_3D ( 'NONE', #42571, #9457, #13979 ) ;
#64347=LINE ( 'NONE', #41768, #65950 ) ;
#64367=FACE_OUTER_BOUND ( 'NONE', #66993, .T. ) ;
#64392=ORIENTED_EDGE ( 'NONE', *, *, #16615, .T. ) ;
#64402=DIRECTION ( 'NONE',  ( -1.000000000000000000, -0.000000000000000000, 0.000000000000000000 ) ) ;
#64411=FACE_OUTER_BOUND ( 'NONE', #61885, .T. ) ;
#64415=CARTESIAN_POINT ( 'NONE',  ( 0.000000000000000000, 0.000000000000000000, 0.000000000000000000 ) ) ;
#64429=EDGE_CURVE ( 'NONE', #305, #44128, #63683, .T. ) ;
#64436=EDGE_LOOP ( 'NONE', ( #20588, #33551, #16767, #16823, #65857, #41433, #65137, #1412, #439, #60572, #72584, #52259, #18924, #10330, #29280, #61243, #36630, #56624, #41699, #66773, #8420, #33717, #56206, #15705, #7384, #49924, #8229, #4775, #5660, #74083, #65103, #63761, #33834, #17658, #66414, #69421, #17565, #49075, #57237, #17673, #64444, #42104, #20171, #55638, #5412, #713, #25274, #63846, #15509, #60841, #5392, #14895, #72672, #60692, #66661, #36702, #31704, #3926, #71082, #38009, #5916, #22489, #59627, #29109, #66235, #6409, #57317, #25694, #11555, #31144, #2718, #19300, #55853, #24311, #47693, #24683, #42744, #59188, #13880, #55646, #12930, #63029, #28251, #28652, #364, #52366, #2549, #48887, #50782, #38781, #32158, #16163, #72279, #3982, #46621, #25184, #66750, #63979, #2324, #26326, #59035, #41504, #17877, #6108, #27842, #63976, #43335, #67534, #72062, #10523, #26419, #13204, #60313, #28849, #31506, #20802, #21800, #46232, #16490, #33644, #36897, #46904, #4206, #9730, #4549, #32841, #57950, #23613, #59215, #56731, #63251, #27924, #16364, #52224, #42978, #64908, #38667, #70441, #69981, #62180, #66283, #73700, #57685, #68446, #43934, #17587, #17300, #46187, #36068, #12151, #24001, #37032, #37279, #65938, #59001, #74144, #10437, #30332, #54999, #29944, #23564, #64135, #44582, #67916, #3077 ) ) ;
#64441=CARTESIAN_POINT ( 'NONE',  ( 10.00000000000000000, 16.95692799528845640, -2.500000000000000000 ) ) ;
#64443=EDGE_CURVE ( 'NONE', #21975, #420, #16814, .T. ) ;
#64444=ORIENTED_EDGE ( 'NONE', *, *, #10421, .F. ) ;
#64445=DIRECTION ( 'NONE',  ( 0.000000000000000000, 0.3090169943749482839, -0.9510565162951533091 ) ) ;
#64451=EDGE_CURVE ( 'NONE', #17447, #44755, #43022, .T. ) ;
#64456=FACE_OUTER_BOUND ( 'NONE', #4940, .T. ) ;
#64522=MECHANICAL_DESIGN_GEOMETRIC_PRESENTATION_REPRESENTATION('',(#62110),#74118);
#64526=EDGE_CURVE ( 'NONE', #60365, #63446, #32458, .T. ) ;
#64542=ORIENTED_EDGE ( 'NONE', *, *, #37165, .T. ) ;
#64547=VECTOR ( 'NONE', #66480, 1000.000000000000000 ) ;
#64550=DIRECTION ( 'NONE',  ( 0.000000000000000000, 0.000000000000000000, 1.000000000000000000 ) ) ;
#64564=DIRECTION ( 'NONE',  ( 0.000000000000000000, -0.7071067811865535679, 0.7071067811865413555 ) ) ;
#64569=ORIENTED_EDGE ( 'NONE', *, *, #71604, .T. ) ;
#64570=EDGE_LOOP ( 'NONE', ( #37197, #17380, #8710, #18284 ) ) ;
#64576=AXIS2_PLACEMENT_3D ( 'NONE', #63537, #46977, #12014 ) ;
#64580=CIRCLE ( 'NONE', #4599, 16.00000000000000355 ) ;
#64584=AXIS2_PLACEMENT_3D ( 'NONE', #43434, #43049, #37413 ) ;
#64603=AXIS2_PLACEMENT_3D ( 'NONE', #63464, #29583, #30701 ) ;
#64608=VERTEX_POINT ( 'NONE', #33951 ) ;
#64630=CARTESIAN_POINT ( 'NONE',  ( 10.00000000000000000, 0.000000000000000000, 0.000000000000000000 ) ) ;
#64632=( LENGTH_UNIT ( ) NAMED_UNIT ( * ) SI_UNIT ( .MILLI., .METRE. ) );
#64640=CARTESIAN_POINT ( 'NONE',  ( 0.000000000000000000, 36.13751322684449008, -21.40280677340332716 ) ) ;
#64642=ORIENTED_EDGE ( 'NONE', *, *, #17425, .T. ) ;
#64649=ORIENTED_EDGE ( 'NONE', *, *, #19496, .T. ) ;
#64650=CARTESIAN_POINT ( 'NONE',  ( 10.00000000000000000, 41.81611651403867569, -3.925862922255714871 ) ) ;
#64663=EDGE_CURVE ( 'NONE', #22671, #23737, #65, .T. ) ;
#64671=DIRECTION ( 'NONE',  ( 0.000000000000000000, 0.000000000000000000, 1.000000000000000000 ) ) ;
#64672=CYLINDRICAL_SURFACE ( 'NONE', #60302, 16.00000000000000000 ) ;
#64686=EDGE_CURVE ( 'NONE', #17385, #21499, #20283, .T. ) ;
#64688=CARTESIAN_POINT ( 'NONE',  ( 10.00000000000000000, 21.53537804866081373, 30.80686688397018358 ) ) ;
#64702=DIRECTION ( 'NONE',  ( -1.000000000000000000, 0.000000000000000000, 0.000000000000000000 ) ) ;
#64705=CARTESIAN_POINT ( 'NONE',  ( 0.000000000000000000, 37.16516213103277266, 4.992566952385114831 ) ) ;
#64711=ORIENTED_EDGE ( 'NONE', *, *, #71300, .T. ) ;
#64742=CIRCLE ( 'NONE', #7275, 15.99999999999999822 ) ;
#64784=DIRECTION ( 'NONE',  ( 0.000000000000000000, 0.000000000000000000, 1.000000000000000000 ) ) ;
#64786=ADVANCED_FACE ( 'NONE', ( #35785 ), #53097, .T. ) ;
#64813=CARTESIAN_POINT ( 'NONE',  ( 10.00000000000000000, -37.22597642581153821, 10.79786254984320415 ) ) ;
#64823=VERTEX_POINT ( 'NONE', #18868 ) ;
#64826=ORIENTED_EDGE ( 'NONE', *, *, #11426, .T. ) ;
#64842=DIRECTION ( 'NONE',  ( 0.000000000000000000, -0.9510565162951500895, -0.3090169943749581649 ) ) ;
#64867=CARTESIAN_POINT ( 'NONE',  ( 0.000000000000000000, 35.92658777277525672, -10.74501242461245809 ) ) ;
#64873=ORIENTED_EDGE ( 'NONE', *, *, #56901, .T. ) ;
#64877=CIRCLE ( 'NONE', #55086, 16.00000000000000000 ) ;
#64879=DIRECTION ( 'NONE',  ( 0.000000000000000000, -0.8090169943749402348, -0.5877852522924830181 ) ) ;
#64886=CIRCLE ( 'NONE', #68481, 42.00000000000000000 ) ;
#64900=ORIENTED_EDGE ( 'NONE', *, *, #46130, .T. ) ;
#64908=ORIENTED_EDGE ( 'NONE', *, *, #51096, .F. ) ;
#64931=AXIS2_PLACEMENT_3D ( 'NONE', #48248, #70412, #54624 ) ;
#64970=FACE_OUTER_BOUND ( 'NONE', #17294, .T. ) ;
#64977=DIRECTION ( 'NONE',  ( 1.000000000000000000, 0.000000000000000000, 0.000000000000000000 ) ) ;
#64991=VERTEX_POINT ( 'NONE', #42932 ) ;
#65010=AXIS2_PLACEMENT_3D ( 'NONE', #30544, #6170, #6526 ) ;
#65015=FILL_AREA_STYLE_COLOUR ( '', #41026 ) ;
#65033=ORIENTED_EDGE ( 'NONE', *, *, #26830, .F. ) ;
#65049=EDGE_LOOP ( 'NONE', ( #61020, #51225, #73205, #53444 ) ) ;
#65053=DIRECTION ( 'NONE',  ( -1.000000000000000000, 0.000000000000000000, 0.000000000000000000 ) ) ;
#65055=CARTESIAN_POINT ( 'NONE',  ( 10.00000000000000000, 0.000000000000000000, 0.000000000000000000 ) ) ;
#65057=DIRECTION ( 'NONE',  ( 1.000000000000000000, 0.000000000000000000, 0.000000000000000000 ) ) ;
#65064=FACE_OUTER_BOUND ( 'NONE', #32760, .T. ) ;
#65067=FACE_OUTER_BOUND ( 'NONE', #21058, .T. ) ;
#65071=DIRECTION ( 'NONE',  ( 0.000000000000000000, 0.000000000000000000, 1.000000000000000000 ) ) ;
#65081=FACE_OUTER_BOUND ( 'NONE', #10105, .T. ) ;
#65098=ORIENTED_EDGE ( 'NONE', *, *, #42049, .T. ) ;
#65103=ORIENTED_EDGE ( 'NONE', *, *, #65275, .F. ) ;
#65124=CARTESIAN_POINT ( 'NONE',  ( 10.00000000000000000, -0.6853352020793173072, 37.58145647212453611 ) ) ;
#65126=DIRECTION ( 'NONE',  ( -1.000000000000000000, 0.000000000000000000, 0.000000000000000000 ) ) ;
#65133=ADVANCED_FACE ( 'NONE', ( #39136 ), #57177, .T. ) ;
#65134=ORIENTED_EDGE ( 'NONE', *, *, #41579, .T. ) ;
#65137=ORIENTED_EDGE ( 'NONE', *, *, #46713, .F. ) ;
#65146=CIRCLE ( 'NONE', #24301, 16.00000000000000000 ) ;
#65151=ORIENTED_EDGE ( 'NONE', *, *, #17730, .T. ) ;
#65160=ORIENTED_EDGE ( 'NONE', *, *, #37442, .T. ) ;
#65162=DIRECTION ( 'NONE',  ( -1.000000000000000000, 0.000000000000000000, 0.000000000000000000 ) ) ;
#65204=ORIENTED_EDGE ( 'NONE', *, *, #11990, .T. ) ;
#65231=DIRECTION ( 'NONE',  ( 0.000000000000000000, 0.000000000000000000, 1.000000000000000000 ) ) ;
#65247=VECTOR ( 'NONE', #39446, 1000.000000000000000 ) ;
#65262=ORIENTED_EDGE ( 'NONE', *, *, #63036, .F. ) ;
#65266=EDGE_CURVE ( 'NONE', #48094, #18937, #7146, .T. ) ;
#65275=EDGE_CURVE ( 'NONE', #64110, #65939, #9688, .T. ) ;
#65295=ORIENTED_EDGE ( 'NONE', *, *, #8387, .T. ) ;
#65296=DIRECTION ( 'NONE',  ( 0.000000000000000000, -6.938893903907228378E-15, 1.000000000000000000 ) ) ;
#65297=AXIS2_PLACEMENT_3D ( 'NONE', #4897, #50350, #39086 ) ;
#65300=DIRECTION ( 'NONE',  ( -1.000000000000000000, -0.000000000000000000, 0.000000000000000000 ) ) ;
#65315=CARTESIAN_POINT ( 'NONE',  ( 10.00000000000000000, -27.13269053701078448, -25.88420570971428702 ) ) ;
#65343=EDGE_CURVE ( 'NONE', #51588, #58261, #21706, .T. ) ;
#65346=DIRECTION ( 'NONE',  ( 0.000000000000000000, 0.000000000000000000, 1.000000000000000000 ) ) ;
#65352=CIRCLE ( 'NONE', #56978, 15.99999999999999822 ) ;
#65362=AXIS2_PLACEMENT_3D ( 'NONE', #34684, #46345, #41804 ) ;
#65368=ORIENTED_EDGE ( 'NONE', *, *, #17580, .T. ) ;
#65389=EDGE_CURVE ( 'NONE', #43729, #24000, #71754, .T. ) ;
#65391=CIRCLE ( 'NONE', #43774, 16.00000000000000000 ) ;
#65398=CIRCLE ( 'NONE', #32957, 12.50000000000000000 ) ;
#65401=EDGE_CURVE ( 'NONE', #66590, #54849, #3706, .T. ) ;
#65405=AXIS2_PLACEMENT_3D ( 'NONE', #36216, #70406, #18916 ) ;
#65417=VERTEX_POINT ( 'NONE', #14628 ) ;
#65422=CARTESIAN_POINT ( 'NONE',  ( 0.000000000000000000, -30.80686688396994910, -21.53537804866113703 ) ) ;
#65425=AXIS2_PLACEMENT_3D ( 'NONE', #73984, #62743, #11211 ) ;
#65445=CARTESIAN_POINT ( 'NONE',  ( 0.000000000000000000, 35.38097989696512968, 12.42422080174651100 ) ) ;
#65454=LINE ( 'NONE', #31583, #57418 ) ;
#65459=LINE ( 'NONE', #25228, #51497 ) ;
#65492=DIRECTION ( 'NONE',  ( 0.000000000000000000, 0.000000000000000000, 1.000000000000000000 ) ) ;
#65515=DIRECTION ( 'NONE',  ( -1.000000000000000000, 0.000000000000000000, 0.000000000000000000 ) ) ;
#65547=ORIENTED_EDGE ( 'NONE', *, *, #52512, .T. ) ;
#65560=AXIS2_PLACEMENT_3D ( 'NONE', #54805, #3334, #37897 ) ;
#65577=ORIENTED_EDGE ( 'NONE', *, *, #61604, .T. ) ;
#65582=LINE ( 'NONE', #60680, #19727 ) ;
#65607=CARTESIAN_POINT ( 'NONE',  ( 50.00005079999999680, 0.000000000000000000, 0.000000000000000000 ) ) ;
#65625=VECTOR ( 'NONE', #23624, 1000.000000000000000 ) ;
#65669=DIRECTION ( 'NONE',  ( 0.000000000000000000, 0.000000000000000000, 1.000000000000000000 ) ) ;
#65673=ORIENTED_EDGE ( 'NONE', *, *, #57747, .T. ) ;
#65688=CIRCLE ( 'NONE', #20049, 16.00000000000000000 ) ;
#65718=CIRCLE ( 'NONE', #57294, 16.00000000000000000 ) ;
#65749=CARTESIAN_POINT ( 'NONE',  ( 10.00000000000000000, 0.000000000000000000, 0.000000000000000000 ) ) ;
#65750=CARTESIAN_POINT ( 'NONE',  ( -1.200000000000000030E-05, 16.95692799528845995, 2.500000000000000000 ) ) ;
#65762=ORIENTED_EDGE ( 'NONE', *, *, #28533, .T. ) ;
#65763=EDGE_LOOP ( 'NONE', ( #68342, #17084, #1799, #16244 ) ) ;
#65765=CIRCLE ( 'NONE', #27325, 16.00000000000000000 ) ;
#65785=DIRECTION ( 'NONE',  ( -1.000000000000000000, -0.000000000000000000, 0.000000000000000000 ) ) ;
#65789=CIRCLE ( 'NONE', #20321, 16.00000000000000355 ) ;
#65795=DIRECTION ( 'NONE',  ( 0.000000000000000000, 0.000000000000000000, 1.000000000000000000 ) ) ;
#65810=VERTEX_POINT ( 'NONE', #47649 ) ;
#65812=LINE ( 'NONE', #55633, #70762 ) ;
#65818=AXIS2_PLACEMENT_3D ( 'NONE', #32481, #27591, #21193 ) ;
#65842=ORIENTED_EDGE ( 'NONE', *, *, #23604, .T. ) ;
#65857=ORIENTED_EDGE ( 'NONE', *, *, #71433, .F. ) ;
#65873=VECTOR ( 'NONE', #57336, 1000.000000000000000 ) ;
#65888=AXIS2_PLACEMENT_3D ( 'NONE', #68416, #50728, #62414 ) ;
#65903=DIRECTION ( 'NONE',  ( 0.000000000000000000, 0.000000000000000000, -1.000000000000000000 ) ) ;
#65912=AXIS2_PLACEMENT_3D ( 'NONE', #38541, #49443, #21229 ) ;
#65929=CIRCLE ( 'NONE', #73090, 42.00000000000000000 ) ;
#65934=AXIS2_PLACEMENT_3D ( 'NONE', #394, #63517, #7093 ) ;
#65938=ORIENTED_EDGE ( 'NONE', *, *, #44687, .F. ) ;
#65939=VERTEX_POINT ( 'NONE', #11757 ) ;
#65950=VECTOR ( 'NONE', #60194, 1000.000000000000000 ) ;
#65956=DIRECTION ( 'NONE',  ( 1.000000000000000000, -0.000000000000000000, -0.000000000000000000 ) ) ;
#65959=AXIS2_PLACEMENT_3D ( 'NONE', #49178, #43926, #26240 ) ;
#65961=CARTESIAN_POINT ( 'NONE',  ( 4.999999999999999112, -40.68715046381921496, -10.41901085202121280 ) ) ;
#66026=FACE_OUTER_BOUND ( 'NONE', #60088, .T. ) ;
#66028=CIRCLE ( 'NONE', #73196, 16.00000000000000000 ) ;
#66050=DIRECTION ( 'NONE',  ( 0.000000000000000000, 0.000000000000000000, 1.000000000000000000 ) ) ;
#66064=AXIS2_PLACEMENT_3D ( 'NONE', #72440, #36756, #2598 ) ;
#66083=EDGE_CURVE ( 'NONE', #11727, #1166, #33071, .T. ) ;
#66085=DIRECTION ( 'NONE',  ( -1.000000000000000000, -0.000000000000000000, 0.000000000000000000 ) ) ;
#66122=ORIENTED_EDGE ( 'NONE', *, *, #15592, .F. ) ;
#66151=EDGE_CURVE ( 'NONE', #51673, #54454, #70378, .T. ) ;
#66177=FACE_OUTER_BOUND ( 'NONE', #47074, .T. ) ;
#66186=ORIENTED_EDGE ( 'NONE', *, *, #59623, .T. ) ;
#66200=DIRECTION ( 'NONE',  ( 0.000000000000000000, 0.000000000000000000, 1.000000000000000000 ) ) ;
#66207=EDGE_CURVE ( 'NONE', #729, #9618, #18699, .T. ) ;
#66214=ORIENTED_EDGE ( 'NONE', *, *, #6378, .T. ) ;
#66218=DIRECTION ( 'NONE',  ( 0.000000000000000000, 0.9876883405951381034, -0.1564344650402276216 ) ) ;
#66232=EDGE_LOOP ( 'NONE', ( #18559, #44302, #22690, #32257 ) ) ;
#66235=ORIENTED_EDGE ( 'NONE', *, *, #58326, .F. ) ;
#66249=STYLED_ITEM ( 'NONE', ( #40973 ), #34586 ) ;
#66283=ORIENTED_EDGE ( 'NONE', *, *, #8854, .F. ) ;
#66284=CARTESIAN_POINT ( 'NONE',  ( 10.00000000000000000, -35.38097989696520074, 12.42422080174625520 ) ) ;
#66285=CARTESIAN_POINT ( 'NONE',  ( -10.00000000000000000, 0.000000000000000000, 0.000000000000000000 ) ) ;
#66288=EDGE_CURVE ( 'NONE', #37558, #5960, #38034, .T. ) ;
#66301=EDGE_LOOP ( 'NONE', ( #31599, #44124, #63023, #52071 ) ) ;
#66302=EDGE_LOOP ( 'NONE', ( #63456, #65262, #54926, #4267 ) ) ;
#66308=EDGE_CURVE ( 'NONE', #53075, #25170, #30716, .T. ) ;
#66334=ORIENTED_EDGE ( 'NONE', *, *, #27157, .T. ) ;
#66344=ADVANCED_FACE ( 'NONE', ( #43692 ), #61349, .T. ) ;
#66361=DIRECTION ( 'NONE',  ( -1.000000000000000000, 0.000000000000000000, -0.000000000000000000 ) ) ;
#66363=CARTESIAN_POINT ( 'NONE',  ( 10.00000000000000000, -32.34446384429989507, 26.79245525562703278 ) ) ;
#66387=CARTESIAN_POINT ( 'NONE',  ( 10.00000000000000000, -33.00180498840060039, 17.80606268964528027 ) ) ;
#66391=ORIENTED_EDGE ( 'NONE', *, *, #17580, .F. ) ;
#66414=ORIENTED_EDGE ( 'NONE', *, *, #68791, .F. ) ;
#66418=ORIENTED_EDGE ( 'NONE', *, *, #35465, .T. ) ;
#66433=ORIENTED_EDGE ( 'NONE', *, *, #9075, .T. ) ;
#66466=CARTESIAN_POINT ( 'NONE',  ( 10.00000000000000000, 2.663952781846733675, -41.91543099594814947 ) ) ;
#66469=AXIS2_PLACEMENT_3D ( 'NONE', #1392, #646, #24286 ) ;
#66479=CARTESIAN_POINT ( 'NONE',  ( 0.000000000000000000, -40.98264845739755202, 9.188173127307159405 ) ) ;
#66480=DIRECTION ( 'NONE',  ( -1.000000000000000000, 0.000000000000000000, -0.000000000000000000 ) ) ;
#66482=AXIS2_PLACEMENT_3D ( 'NONE', #65124, #7599, #19970 ) ;
#66500=ORIENTED_EDGE ( 'NONE', *, *, #2438, .T. ) ;
#66534=DIRECTION ( 'NONE',  ( 0.000000000000000000, 0.3090169943749482839, -0.9510565162951533091 ) ) ;
#66543=AXIS2_PLACEMENT_3D ( 'NONE', #50864, #50105, #9901 ) ;
#66545=CARTESIAN_POINT ( 'NONE',  ( 0.000000000000000000, -0.8828120875903202602, 37.48860685352291000 ) ) ;
#66560=EDGE_CURVE ( 'NONE', #63739, #25323, #27117, .T. ) ;
#66565=AXIS2_PLACEMENT_3D ( 'NONE', #32626, #15335, #31887 ) ;
#66585=AXIS2_PLACEMENT_3D ( 'NONE', #50371, #45500, #21805 ) ;
#66589=VERTEX_POINT ( 'NONE', #51909 ) ;
#66590=VERTEX_POINT ( 'NONE', #6786 ) ;
#66600=EDGE_CURVE ( 'NONE', #4011, #44188, #55953, .T. ) ;
#66626=CIRCLE ( 'NONE', #45009, 37.49900000000000233 ) ;
#66633=FACE_OUTER_BOUND ( 'NONE', #63757, .T. ) ;
#66640=AXIS2_PLACEMENT_3D ( 'NONE', #11847, #50596, #67525 ) ;
#66642=CARTESIAN_POINT ( 'NONE',  ( 10.00000000000000000, -21.40280677340345505, -36.13751322684441902 ) ) ;
#66652=FACE_OUTER_BOUND ( 'NONE', #15153, .T. ) ;
#66661=ORIENTED_EDGE ( 'NONE', *, *, #28342, .F. ) ;
#66673=VERTEX_POINT ( 'NONE', #47743 ) ;
#66684=CARTESIAN_POINT ( 'NONE',  ( 0.000000000000000000, 22.74946021919133088, 29.81001611431016229 ) ) ;
#66693=VERTEX_POINT ( 'NONE', #12785 ) ;
#66700=DIRECTION ( 'NONE',  ( 1.000000000000000000, 0.000000000000000000, 0.000000000000000000 ) ) ;
#66701=DIRECTION ( 'NONE',  ( 0.000000000000000000, -8.881784197001252323E-16, -1.000000000000000000 ) ) ;
#66704=EDGE_CURVE ( 'NONE', #44128, #9413, #70657, .T. ) ;
#66707=EDGE_CURVE ( 'NONE', #72132, #58797, #10332, .T. ) ;
#66750=ORIENTED_EDGE ( 'NONE', *, *, #35543, .F. ) ;
#66773=ORIENTED_EDGE ( 'NONE', *, *, #67729, .F. ) ;
#66789=ORIENTED_EDGE ( 'NONE', *, *, #48207, .F. ) ;
#66793=DIRECTION ( 'NONE',  ( 0.000000000000000000, 0.000000000000000000, 1.000000000000000000 ) ) ;
#66804=ADVANCED_FACE ( 'NONE', ( #8643 ), #30809, .T. ) ;
#66824=CARTESIAN_POINT ( 'NONE',  ( 10.00000000000000000, -21.32104025579135964, 30.84782396557210760 ) ) ;
#66849=CARTESIAN_POINT ( 'NONE',  ( 10.00000000000000000, 10.74501242461333028, -35.92658777277499382 ) ) ;
#66872=VERTEX_POINT ( 'NONE', #68007 ) ;
#66886=DIRECTION ( 'NONE',  ( 0.000000000000000000, 0.000000000000000000, 1.000000000000000000 ) ) ;
#66893=EDGE_CURVE ( 'NONE', #6463, #16864, #38695, .T. ) ;
#66912=ORIENTED_EDGE ( 'NONE', *, *, #31670, .F. ) ;
#66922=CIRCLE ( 'NONE', #5781, 16.00000000000000000 ) ;
#66925=ORIENTED_EDGE ( 'NONE', *, *, #388, .F. ) ;
#66927=ORIENTED_EDGE ( 'NONE', *, *, #38897, .T. ) ;
#66928=AXIS2_PLACEMENT_3D ( 'NONE', #36647, #8823, #2114 ) ;
#66964=CARTESIAN_POINT ( 'NONE',  ( 5.000000000000000000, -27.75498641678720446, -31.52238457039628727 ) ) ;
#66967=CARTESIAN_POINT ( 'NONE',  ( 0.000000000000000000, 32.34446384430010113, -26.79245525562679831 ) ) ;
#66982=DIRECTION ( 'NONE',  ( 1.000000000000000000, 0.000000000000000000, 0.000000000000000000 ) ) ;
#66983=AXIS2_PLACEMENT_3D ( 'NONE', #34821, #38982, #40092 ) ;
#66984=CIRCLE ( 'NONE', #67161, 42.00000000000000000 ) ;
#66985=CARTESIAN_POINT ( 'NONE',  ( 0.000000000000000000, 0.000000000000000000, 0.000000000000000000 ) ) ;
#66993=EDGE_LOOP ( 'NONE', ( #51325, #60969, #72216, #35587 ) ) ;
#67001=AXIS2_PLACEMENT_3D ( 'NONE', #34090, #51378, #73938 ) ;
#67011=CARTESIAN_POINT ( 'NONE',  ( 0.000000000000000000, -3.925862922256468046, 41.81611651403860463 ) ) ;
#67034=ORIENTED_EDGE ( 'NONE', *, *, #23276, .F. ) ;
#67043=AXIS2_PLACEMENT_3D ( 'NONE', #25673, #31675, #61376 ) ;
#67049=ORIENTED_EDGE ( 'NONE', *, *, #36597, .T. ) ;
#67052=EDGE_LOOP ( 'NONE', ( #68278, #66433, #24037, #13025 ) ) ;
#67057=DIRECTION ( 'NONE',  ( -1.000000000000000000, 0.000000000000000000, -0.000000000000000000 ) ) ;
#67060=CIRCLE ( 'NONE', #11818, 12.50000000000000000 ) ;
#67071=EDGE_CURVE ( 'NONE', #23893, #51310, #64226, .T. ) ;
#67073=CARTESIAN_POINT ( 'NONE',  ( 10.00000000000000178, 12.24744871391589029, 2.500000000000004441 ) ) ;
#67076=CARTESIAN_POINT ( 'NONE',  ( 10.00000000000000000, -10.96151621346461447, -35.95386929396268272 ) ) ;
#67105=VERTEX_POINT ( 'NONE', #47298 ) ;
#67106=LINE ( 'NONE', #32518, #48851 ) ;
#67161=AXIS2_PLACEMENT_3D ( 'NONE', #28435, #51745, #23186 ) ;
#67200=EDGE_CURVE ( 'NONE', #57844, #49855, #30603, .T. ) ;
#67212=CYLINDRICAL_SURFACE ( 'NONE', #23710, 16.00000000000000000 ) ;
#67214=CIRCLE ( 'NONE', #68420, 16.00000000000000355 ) ;
#67279=CIRCLE ( 'NONE', #93, 16.00000000000000000 ) ;
#67297=EDGE_CURVE ( 'NONE', #51292, #63103, #36677, .T. ) ;
#67307=DIRECTION ( 'NONE',  ( 0.000000000000000000, 0.000000000000000000, 1.000000000000000000 ) ) ;
#67309=PRESENTATION_STYLE_ASSIGNMENT (( #68052 ) ) ;
#67319=DIRECTION ( 'NONE',  ( -1.000000000000000000, -0.000000000000000000, 0.000000000000000000 ) ) ;
#67323=CARTESIAN_POINT ( 'NONE',  ( 10.00000000000000000, 0.000000000000000000, 0.000000000000000000 ) ) ;
#67351=CYLINDRICAL_SURFACE ( 'NONE', #16832, 42.00000000000000000 ) ;
#67352=CYLINDRICAL_SURFACE ( 'NONE', #14730, 16.00000000000000000 ) ;
#67360=VECTOR ( 'NONE', #14060, 1000.000000000000000 ) ;
#67395=VERTEX_POINT ( 'NONE', #50993 ) ;
#67423=DIRECTION ( 'NONE',  ( 0.000000000000000000, 1.000000000000000000, 3.491481338843133750E-15 ) ) ;
#67441=AXIS2_PLACEMENT_3D ( 'NONE', #21645, #44599, #68644 ) ;
#67459=CYLINDRICAL_SURFACE ( 'NONE', #2960, 16.00000000000000000 ) ;
#67461=EDGE_CURVE ( 'NONE', #34558, #30100, #72667, .T. ) ;
#67467=EDGE_CURVE ( 'NONE', #30173, #39405, #4289, .T. ) ;
#67472=VECTOR ( 'NONE', #65053, 1000.000000000000000 ) ;
#67483=AXIS2_PLACEMENT_3D ( 'NONE', #28762, #249, #23142 ) ;
#67500=CARTESIAN_POINT ( 'NONE',  ( 10.00000000000000000, 0.000000000000000000, 0.000000000000000000 ) ) ;
#67516=CARTESIAN_POINT ( 'NONE',  ( 10.00000000000000000, 0.000000000000000000, 0.000000000000000000 ) ) ;
#67525=DIRECTION ( 'NONE',  ( 0.000000000000000000, 0.000000000000000000, 1.000000000000000000 ) ) ;
#67528=ORIENTED_EDGE ( 'NONE', *, *, #30702, .F. ) ;
#67534=ORIENTED_EDGE ( 'NONE', *, *, #51914, .F. ) ;
#67539=CARTESIAN_POINT ( 'NONE',  ( 10.00000000000000000, 0.000000000000000000, 0.000000000000000000 ) ) ;
#67552=CARTESIAN_POINT ( 'NONE',  ( 5.000000000000000000, -31.52238457039619490, 27.75498641678731104 ) ) ;
#67609=ORIENTED_EDGE ( 'NONE', *, *, #57075, .F. ) ;
#67630=CARTESIAN_POINT ( 'NONE',  ( 10.00000000000000000, 12.26510123303259725, 35.53030884539089840 ) ) ;
#67644=CARTESIAN_POINT ( 'NONE',  ( 10.00000000000000000, 35.38097989696512968, 12.42422080174651100 ) ) ;
#67651=ADVANCED_FACE ( 'NONE', ( #43441 ), #43057, .T. ) ;
#67655=CIRCLE ( 'NONE', #18432, 16.00000000000000000 ) ;
#67663=DIRECTION ( 'NONE',  ( 0.000000000000000000, 0.000000000000000000, 1.000000000000000000 ) ) ;
#67675=DIRECTION ( 'NONE',  ( 0.000000000000000000, 0.1564344650402311743, -0.9876883405951377704 ) ) ;
#67698=VECTOR ( 'NONE', #27307, 1000.000000000000000 ) ;
#67703=CARTESIAN_POINT ( 'NONE',  ( 10.00000000000000000, -25.88420570971419821, 27.13269053701087330 ) ) ;
#67705=VERTEX_POINT ( 'NONE', #53963 ) ;
#67722=CARTESIAN_POINT ( 'NONE',  ( 4.999999999999999112, -36.13751322684434797, 21.40280677340357940 ) ) ;
#67729=EDGE_CURVE ( 'NONE', #54454, #57324, #55941, .T. ) ;
#67747=EDGE_LOOP ( 'NONE', ( #814, #14260, #42884, #33902 ) ) ;
#67762=CARTESIAN_POINT ( 'NONE',  ( 10.00000000000000000, 36.88895765772633695, 6.736453364083687667 ) ) ;
#67770=VECTOR ( 'NONE', #65956, 1000.000000000000000 ) ;
#67794=LINE ( 'NONE', #33195, #36520 ) ;
#67803=ORIENTED_EDGE ( 'NONE', *, *, #48364, .T. ) ;
#67816=ORIENTED_EDGE ( 'NONE', *, *, #40892, .F. ) ;
#67819=DIRECTION ( 'NONE',  ( 0.000000000000000000, 0.9876883405951372152, 0.1564344650402346160 ) ) ;
#67827=ORIENTED_EDGE ( 'NONE', *, *, #17676, .F. ) ;
#67829=AXIS2_PLACEMENT_3D ( 'NONE', #58544, #58934, #71292 ) ;
#67871=DIRECTION ( 'NONE',  ( 0.000000000000000000, 0.000000000000000000, 1.000000000000000000 ) ) ;
#67907=CARTESIAN_POINT ( 'NONE',  ( 10.00000000000000000, 10.74501242461333028, -35.92658777277499382 ) ) ;
#67908=CIRCLE ( 'NONE', #27037, 37.49900000000000233 ) ;
#67916=ORIENTED_EDGE ( 'NONE', *, *, #45932, .F. ) ;
#67928=AXIS2_PLACEMENT_3D ( 'NONE', #9658, #72786, #50614 ) ;
#67939=DIRECTION ( 'NONE',  ( 0.000000000000000000, -0.8090169943749531134, 0.5877852522924653655 ) ) ;
#67940=ORIENTED_EDGE ( 'NONE', *, *, #3664, .T. ) ;
#67945=ORIENTED_EDGE ( 'NONE', *, *, #50074, .T. ) ;
#67974=ADVANCED_FACE ( 'NONE', ( #10311 ), #11417, .T. ) ;
#68007=CARTESIAN_POINT ( 'NONE',  ( 10.00000000000000000, -25.88420570971419821, 27.13269053701087330 ) ) ;
#68017=CARTESIAN_POINT ( 'NONE',  ( 4.999999999999999112, -10.41901085202050581, -40.68715046381939970 ) ) ;
#68024=DIRECTION ( 'NONE',  ( -1.000000000000000000, -0.000000000000000000, -0.000000000000000000 ) ) ;
#68025=DIRECTION ( 'NONE',  ( 0.000000000000000000, 0.1564344650402244852, 0.9876883405951387696 ) ) ;
#68034=CARTESIAN_POINT ( 'NONE',  ( 0.000000000000000000, -12.26510123303284594, 35.53030884539080603 ) ) ;
#68052=SURFACE_STYLE_USAGE ( .BOTH. , #56783 ) ;
#68062=FACE_OUTER_BOUND ( 'NONE', #41151, .T. ) ;
#68099=CIRCLE ( 'NONE', #2072, 15.99999999999999822 ) ;
#68108=CARTESIAN_POINT ( 'NONE',  ( 0.000000000000000000, 35.47612816024556537, -22.48208911017461631 ) ) ;
#68127=DIRECTION ( 'NONE',  ( 0.000000000000000000, 0.000000000000000000, 1.000000000000000000 ) ) ;
#68147=AXIS2_PLACEMENT_3D ( 'NONE', #62913, #11371, #57249 ) ;
#68153=EDGE_LOOP ( 'NONE', ( #40510, #33099, #13485, #28996 ) ) ;
#68156=ORIENTED_EDGE ( 'NONE', *, *, #17644, .T. ) ;
#68177=LINE ( 'NONE', #21180, #54703 ) ;
#68182=CARTESIAN_POINT ( 'NONE',  ( 0.000000000000000000, 0.000000000000000000, 0.000000000000000000 ) ) ;
#68186=DIRECTION ( 'NONE',  ( 0.000000000000000000, 0.8910065241883688980, -0.4539904997395447506 ) ) ;
#68214=VECTOR ( 'NONE', #54977, 1000.000000000000000 ) ;
#68226=ORIENTED_EDGE ( 'NONE', *, *, #66288, .F. ) ;
#68249=EDGE_LOOP ( 'NONE', ( #20833, #11574, #39190, #18383 ) ) ;
#68256=FACE_OUTER_BOUND ( 'NONE', #68364, .T. ) ;
#68265=ORIENTED_EDGE ( 'NONE', *, *, #29521, .T. ) ;
#68267=VERTEX_POINT ( 'NONE', #11244 ) ;
#68278=ORIENTED_EDGE ( 'NONE', *, *, #59160, .T. ) ;
#68321=CARTESIAN_POINT ( 'NONE',  ( 0.000000000000000000, 0.000000000000000000, 0.000000000000000000 ) ) ;
#68328=ORIENTED_EDGE ( 'NONE', *, *, #70774, .F. ) ;
#68335=CARTESIAN_POINT ( 'NONE',  ( 0.000000000000000000, -17.80606268964563554, 33.00180498840040855 ) ) ;
#68337=FACE_OUTER_BOUND ( 'NONE', #18220, .T. ) ;
#68342=ORIENTED_EDGE ( 'NONE', *, *, #57711, .F. ) ;
#68364=EDGE_LOOP ( 'NONE', ( #41687, #41284, #882, #19147 ) ) ;
#68385=CARTESIAN_POINT ( 'NONE',  ( 0.000000000000000000, 33.80338159004283938, 16.23288003029508886 ) ) ;
#68391=CYLINDRICAL_SURFACE ( 'NONE', #42967, 16.00000000000000000 ) ;
#68412=EDGE_CURVE ( 'NONE', #21499, #20440, #3227, .T. ) ;
#68416=CARTESIAN_POINT ( 'NONE',  ( 10.00000000000000000, -30.80686688397025108, 21.53537804866070715 ) ) ;
#68420=AXIS2_PLACEMENT_3D ( 'NONE', #41634, #40914, #70937 ) ;
#68430=DIRECTION ( 'NONE',  ( -1.000000000000000000, 0.000000000000000000, -0.000000000000000000 ) ) ;
#68442=EDGE_CURVE ( 'NONE', #31431, #54454, #15212, .T. ) ;
#68445=EDGE_CURVE ( 'NONE', #42999, #34136, #31996, .T. ) ;
#68446=ORIENTED_EDGE ( 'NONE', *, *, #28844, .F. ) ;
#68453=ORIENTED_EDGE ( 'NONE', *, *, #16810, .T. ) ;
#68454=DIRECTION ( 'NONE',  ( -1.000000000000000000, 0.000000000000000000, 0.000000000000000000 ) ) ;
#68463=ORIENTED_EDGE ( 'NONE', *, *, #65275, .T. ) ;
#68478=CIRCLE ( 'NONE', #60063, 37.49900000000000233 ) ;
#68481=AXIS2_PLACEMENT_3D ( 'NONE', #32421, #61755, #55364 ) ;
#68483=LINE ( 'NONE', #27869, #46402 ) ;
#68510=CARTESIAN_POINT ( 'NONE',  ( 10.00000000000000000, 16.23288003029497162, 33.80338159004289622 ) ) ;
#68514=CARTESIAN_POINT ( 'NONE',  ( 10.00000000000000000, 0.000000000000000000, 0.000000000000000000 ) ) ;
#68516=ORIENTED_EDGE ( 'NONE', *, *, #55662, .T. ) ;
#68519=ORIENTED_EDGE ( 'NONE', *, *, #64451, .T. ) ;
#68527=ORIENTED_EDGE ( 'NONE', *, *, #42626, .T. ) ;
#68529=ORIENTED_EDGE ( 'NONE', *, *, #4790, .T. ) ;
#68546=FACE_OUTER_BOUND ( 'NONE', #59496, .T. ) ;
#68547=FACE_OUTER_BOUND ( 'NONE', #9976, .T. ) ;
#68599=CARTESIAN_POINT ( 'NONE',  ( 10.00000000000000000, 17.67226234102874116, -33.17418723428288274 ) ) ;
#68610=ORIENTED_EDGE ( 'NONE', *, *, #61387, .T. ) ;
#68623=FACE_OUTER_BOUND ( 'NONE', #27262, .T. ) ;
#68629=ORIENTED_EDGE ( 'NONE', *, *, #11797, .T. ) ;
#68644=DIRECTION ( 'NONE',  ( 0.000000000000000000, 0.000000000000000000, 1.000000000000000000 ) ) ;
#68655=CARTESIAN_POINT ( 'NONE',  ( 10.00000000000000000, 12.26510123303308752, -35.53030884539072787 ) ) ;
#68660=DIRECTION ( 'NONE',  ( 0.000000000000000000, 0.000000000000000000, 1.000000000000000000 ) ) ;
#68666=( GEOMETRIC_REPRESENTATION_CONTEXT ( 3 ) GLOBAL_UNCERTAINTY_ASSIGNED_CONTEXT ( ( #42873 ) ) GLOBAL_UNIT_ASSIGNED_CONTEXT ( ( #64632, #70993, #52237 ) ) REPRESENTATION_CONTEXT ( 'NONE', 'WORKASPACE' ) );
#68672=VECTOR ( 'NONE', #57938, 1000.000000000000000 ) ;
#68675=LINE ( 'NONE', #32584, #67698 ) ;
#68697=DIRECTION ( 'NONE',  ( 0.000000000000000000, 1.000000000000000000, -6.938893903907229364E-16 ) ) ;
#68727=CARTESIAN_POINT ( 'NONE',  ( 0.000000000000000000, 0.000000000000000000, 0.000000000000000000 ) ) ;
#68745=EDGE_LOOP ( 'NONE', ( #35564, #4299, #65134, #64900 ) ) ;
#68755=DIRECTION ( 'NONE',  ( 0.000000000000000000, 0.000000000000000000, -1.000000000000000000 ) ) ;
#68756=DIRECTION ( 'NONE',  ( -1.000000000000000000, 0.000000000000000000, 0.000000000000000000 ) ) ;
#68772=DIRECTION ( 'NONE',  ( -1.000000000000000000, 0.000000000000000000, 0.000000000000000000 ) ) ;
#68777=AXIS2_PLACEMENT_3D ( 'NONE', #37746, #54298, #71188 ) ;
#68778=ADVANCED_FACE ( 'NONE', ( #983 ), #13688, .T. ) ;
#68784=VERTEX_POINT ( 'NONE', #18957 ) ;
#68791=EDGE_CURVE ( 'NONE', #52143, #10923, #2112, .T. ) ;
#68826=EDGE_CURVE ( 'NONE', #57324, #13679, #8055, .T. ) ;
#68830=ORIENTED_EDGE ( 'NONE', *, *, #26050, .T. ) ;
#68834=CARTESIAN_POINT ( 'NONE',  ( 0.000000000000000000, 6.736453364084091788, -36.88895765772625879 ) ) ;
#68850=CARTESIAN_POINT ( 'NONE',  ( 10.00000000000000000, -37.58145647212453611, -0.6853352020794456489 ) ) ;
#68871=CARTESIAN_POINT ( 'NONE',  ( 10.00000000000000000, 17.80606268964540462, 33.00180498840053644 ) ) ;
#68879=ORIENTED_EDGE ( 'NONE', *, *, #3857, .F. ) ;
#68890=DIRECTION ( 'NONE',  ( 0.000000000000000000, 0.000000000000000000, 1.000000000000000000 ) ) ;
#68892=CARTESIAN_POINT ( 'NONE',  ( 10.00000000000000000, 22.64427369931212297, -30.00120703465181293 ) ) ;
#68908=CARTESIAN_POINT ( 'NONE',  ( 5.000000000000000000, -32.34446384429951138, -26.79245525562750530 ) ) ;
#68943=CARTESIAN_POINT ( 'NONE',  ( 0.000000000000000000, 0.000000000000000000, 0.000000000000000000 ) ) ;
#68973=VERTEX_POINT ( 'NONE', #18261 ) ;
#68987=ORIENTED_EDGE ( 'NONE', *, *, #4889, .T. ) ;
#68992=LINE ( 'NONE', #11464, #65873 ) ;
#68997=CYLINDRICAL_SURFACE ( 'NONE', #43465, 16.00000000000000000 ) ;
#69044=CARTESIAN_POINT ( 'NONE',  ( 0.000000000000000000, -36.13751322684434797, 21.40280677340357940 ) ) ;
#69060=PLANE ( 'NONE',  #73183 ) ;
#69080=CARTESIAN_POINT ( 'NONE',  ( 10.00000000000000000, -38.55633173626998911, -16.65560815589452304 ) ) ;
#69103=CARTESIAN_POINT ( 'NONE',  ( 10.00000000000000000, 0.000000000000000000, 0.000000000000000000 ) ) ;
#69107=ORIENTED_EDGE ( 'NONE', *, *, #70158, .F. ) ;
#69124=EDGE_CURVE ( 'NONE', #65810, #25170, #17682, .T. ) ;
#69142=FACE_OUTER_BOUND ( 'NONE', #53691, .T. ) ;
#69162=AXIS2_PLACEMENT_3D ( 'NONE', #42122, #65057, #41014 ) ;
#69168=ORIENTED_EDGE ( 'NONE', *, *, #54273, .T. ) ;
#69201=DIRECTION ( 'NONE',  ( -1.000000000000000000, 0.000000000000000000, 0.000000000000000000 ) ) ;
#69204=DIRECTION ( 'NONE',  ( 0.000000000000000000, 0.9876883405951372152, 0.1564344650402346160 ) ) ;
#69222=LINE ( 'NONE', #48866, #10055 ) ;
#69232=CARTESIAN_POINT ( 'NONE',  ( 10.00000000000000000, 41.81611651403861885, 3.925862922256313503 ) ) ;
#69238=CARTESIAN_POINT ( 'NONE',  ( 0.000000000000000000, 33.17418723428307459, 17.67226234102837878 ) ) ;
#69252=ADVANCED_FACE ( 'NONE', ( #74208 ), #51273, .T. ) ;
#69253=DIRECTION ( 'NONE',  ( -1.000000000000000000, 0.000000000000000000, 0.000000000000000000 ) ) ;
#69256=EDGE_LOOP ( 'NONE', ( #31809, #17392, #32967, #64826 ) ) ;
#69292=CARTESIAN_POINT ( 'NONE',  ( 10.00000000000000000, -27.05870788708213226, -26.08949754953053102 ) ) ;
#69301=CARTESIAN_POINT ( 'NONE',  ( 10.00000000000000000, 33.00180498840072829, -17.80606268964504935 ) ) ;
#69345=AXIS2_PLACEMENT_3D ( 'NONE', #6705, #19454, #29610 ) ;
#69354=FACE_OUTER_BOUND ( 'NONE', #5542, .T. ) ;
#69355=CARTESIAN_POINT ( 'NONE',  ( 10.00000000000000000, -40.68715046381921496, -10.41901085202121457 ) ) ;
#69373=CARTESIAN_POINT ( 'NONE',  ( 10.00000000000000000, 27.05870788708231700, 26.08949754953034272 ) ) ;
#69384=DIRECTION ( 'NONE',  ( -1.000000000000000000, 0.000000000000000000, 0.000000000000000000 ) ) ;
#69388=AXIS2_PLACEMENT_3D ( 'NONE', #26767, #20021, #54260 ) ;
#69398=DIRECTION ( 'NONE',  ( -1.000000000000000000, -0.000000000000000000, 0.000000000000000000 ) ) ;
#69418=DIRECTION ( 'NONE',  ( -1.000000000000000000, 0.000000000000000000, -0.000000000000000000 ) ) ;
#69421=ORIENTED_EDGE ( 'NONE', *, *, #56112, .F. ) ;
#69424=CIRCLE ( 'NONE', #22638, 16.00000000000000000 ) ;
#69426=FACE_OUTER_BOUND ( 'NONE', #53071, .T. ) ;
#69441=DIRECTION ( 'NONE',  ( -1.000000000000000000, -0.000000000000000000, 0.000000000000000000 ) ) ;
#69450=EDGE_CURVE ( 'NONE', #22476, #24772, #6898, .T. ) ;
#69467=AXIS2_PLACEMENT_3D ( 'NONE', #51548, #12064, #12430 ) ;
#69487=LINE ( 'NONE', #46199, #28987 ) ;
#69520=LINE ( 'NONE', #58602, #10125 ) ;
#69529=VERTEX_POINT ( 'NONE', #58397 ) ;
#69575=FACE_OUTER_BOUND ( 'NONE', #41241, .T. ) ;
#69594=VECTOR ( 'NONE', #60668, 1000.000000000000000 ) ;
#69603=CARTESIAN_POINT ( 'NONE',  ( 5.000000000000000000, 39.04073710021344112, 15.48615015657596850 ) ) ;
#69618=ORIENTED_EDGE ( 'NONE', *, *, #9417, .T. ) ;
#69695=VECTOR ( 'NONE', #18413, 1000.000000000000000 ) ;
#69704=ORIENTED_EDGE ( 'NONE', *, *, #52022, .T. ) ;
#69718=EDGE_LOOP ( 'NONE', ( #45697, #22876, #7781, #68529 ) ) ;
#69727=CARTESIAN_POINT ( 'NONE',  ( 10.00000000000000000, -37.58145647212453611, -0.6853352020794456489 ) ) ;
#69728=DIRECTION ( 'NONE',  ( -1.000000000000000000, 0.000000000000000000, -0.000000000000000000 ) ) ;
#69747=ORIENTED_EDGE ( 'NONE', *, *, #19184, .T. ) ;
#69748=VECTOR ( 'NONE', #40247, 1000.000000000000000 ) ;
#69753=EDGE_CURVE ( 'NONE', #14449, #44034, #65765, .T. ) ;
#69762=EDGE_CURVE ( 'NONE', #31095, #420, #4606, .T. ) ;
#69765=DIRECTION ( 'NONE',  ( 0.000000000000000000, 0.5877852522924685852, 0.8090169943749508930 ) ) ;
#69774=EDGE_LOOP ( 'NONE', ( #41539, #35069, #41974, #16085 ) ) ;
#69818=VERTEX_POINT ( 'NONE', #73733 ) ;
#69819=DIRECTION ( 'NONE',  ( 0.000000000000000000, 0.000000000000000000, 1.000000000000000000 ) ) ;
#69842=ADVANCED_FACE ( 'NONE', ( #18448 ), #35730, .T. ) ;
#69849=VECTOR ( 'NONE', #17446, 1000.000000000000000 ) ;
#69905=VERTEX_POINT ( 'NONE', #1581 ) ;
#69939=ADVANCED_FACE ( 'NONE', ( #34633 ), #35381, .T. ) ;
#69941=EDGE_CURVE ( 'NONE', #6579, #64110, #20129, .T. ) ;
#69962=CARTESIAN_POINT ( 'NONE',  ( 10.00000000000000000, 16.45098606841173705, -33.79645857604496229 ) ) ;
#69981=ORIENTED_EDGE ( 'NONE', *, *, #27333, .F. ) ;
#69982=CARTESIAN_POINT ( 'NONE',  ( -10.00000000000000000, 0.000000000000000000, 0.000000000000000000 ) ) ;
#69985=ORIENTED_EDGE ( 'NONE', *, *, #22323, .T. ) ;
#69993=DIRECTION ( 'NONE',  ( -1.000000000000000000, 0.000000000000000000, 0.000000000000000000 ) ) ;
#70024=APPLICATION_CONTEXT ( 'automotive_design' ) ;
#70079=ORIENTED_EDGE ( 'NONE', *, *, #11426, .F. ) ;
#70084=DIRECTION ( 'NONE',  ( 0.000000000000000000, -0.4539904997395351471, -0.8910065241883737830 ) ) ;
#70142=CIRCLE ( 'NONE', #66565, 16.00000000000000000 ) ;
#70156=DIRECTION ( 'NONE',  ( 0.000000000000000000, 0.000000000000000000, 1.000000000000000000 ) ) ;
#70158=EDGE_CURVE ( 'NONE', #48627, #60292, #294, .T. ) ;
#70165=EDGE_CURVE ( 'NONE', #28591, #20602, #22626, .T. ) ;
#70175=EDGE_LOOP ( 'NONE', ( #67803, #15729, #65033, #72292 ) ) ;
#70204=CIRCLE ( 'NONE', #65405, 16.00000000000000000 ) ;
#70208=DIRECTION ( 'NONE',  ( 0.000000000000000000, 0.000000000000000000, 1.000000000000000000 ) ) ;
#70210=CARTESIAN_POINT ( 'NONE',  ( 0.000000000000000000, -25.88420570971419821, 27.13269053701087330 ) ) ;
#70212=DIRECTION ( 'NONE',  ( 0.000000000000000000, 0.1564344650402312298, -0.9876883405951375483 ) ) ;
#70229=ORIENTED_EDGE ( 'NONE', *, *, #68826, .F. ) ;
#70239=AXIS2_PLACEMENT_3D ( 'NONE', #14706, #49287, #43674 ) ;
#70241=EDGE_CURVE ( 'NONE', #56774, #72774, #30974, .T. ) ;
#70268=EDGE_LOOP ( 'NONE', ( #33186, #70229, #52865, #4756 ) ) ;
#70294=CARTESIAN_POINT ( 'NONE',  ( 50.00005079999999680, 0.000000000000000000, 12.50000000000000000 ) ) ;
#70340=ORIENTED_EDGE ( 'NONE', *, *, #32053, .F. ) ;
#70341=CYLINDRICAL_SURFACE ( 'NONE', #14196, 42.00000000000000000 ) ;
#70344=DIRECTION ( 'NONE',  ( 0.000000000000000000, 0.000000000000000000, -1.000000000000000000 ) ) ;
#70348=ORIENTED_EDGE ( 'NONE', *, *, #8663, .F. ) ;
#70351=CARTESIAN_POINT ( 'NONE',  ( 10.00000000000000000, -16.23288003029473359, -33.80338159004301701 ) ) ;
#70365=EDGE_CURVE ( 'NONE', #41070, #729, #38232, .T. ) ;
#70370=CARTESIAN_POINT ( 'NONE',  ( 5.000000000000000000, 15.48615015657581750, 39.04073710021349797 ) ) ;
#70378=LINE ( 'NONE', #18517, #63166 ) ;
#70382=ORIENTED_EDGE ( 'NONE', *, *, #7128, .T. ) ;
#70387=CARTESIAN_POINT ( 'NONE',  ( 10.00000000000000000, -22.64427369931191336, 30.00120703465197280 ) ) ;
#70399=DIRECTION ( 'NONE',  ( -1.000000000000000000, 0.000000000000000000, -0.000000000000000000 ) ) ;
#70400=ADVANCED_FACE ( 'NONE', ( #14008 ), #36954, .T. ) ;
#70406=DIRECTION ( 'NONE',  ( -1.000000000000000000, 0.000000000000000000, 0.000000000000000000 ) ) ;
#70412=DIRECTION ( 'NONE',  ( -1.000000000000000000, -0.000000000000000000, 0.000000000000000000 ) ) ;
#70422=DIRECTION ( 'NONE',  ( -1.000000000000000000, 0.000000000000000000, -0.000000000000000000 ) ) ;
#70431=ORIENTED_EDGE ( 'NONE', *, *, #48970, .T. ) ;
#70441=ORIENTED_EDGE ( 'NONE', *, *, #35828, .F. ) ;
#70504=VERTEX_POINT ( 'NONE', #41042 ) ;
#70509=VERTEX_POINT ( 'NONE', #47048 ) ;
#70523=ORIENTED_EDGE ( 'NONE', *, *, #45143, .T. ) ;
#70536=VERTEX_POINT ( 'NONE', #69232 ) ;
#70551=EDGE_LOOP ( 'NONE', ( #26711, #790, #70815, #9059 ) ) ;
#70552=ORIENTED_EDGE ( 'NONE', *, *, #38041, .T. ) ;
#70562=VECTOR ( 'NONE', #59611, 1000.000000000000000 ) ;
#70581=EDGE_CURVE ( 'NONE', #54849, #60507, #43082, .T. ) ;
#70588=CIRCLE ( 'NONE', #42990, 42.00000000000000000 ) ;
#70589=EDGE_CURVE ( 'NONE', #50488, #65810, #23377, .T. ) ;
#70599=ORIENTED_EDGE ( 'NONE', *, *, #23505, .F. ) ;
#70600=EDGE_CURVE ( 'NONE', #38085, #18829, #46663, .T. ) ;
#70609=VECTOR ( 'NONE', #25007, 1000.000000000000000 ) ;
#70638=ORIENTED_EDGE ( 'NONE', *, *, #66308, .F. ) ;
#70646=CARTESIAN_POINT ( 'NONE',  ( 10.00000000000000000, 3.925862922256160736, 41.81611651403863306 ) ) ;
#70652=CARTESIAN_POINT ( 'NONE',  ( 10.00000000000000178, 1.530808498934191521E-15, -12.50000000000000000 ) ) ;
#70657=LINE ( 'NONE', #46276, #772 ) ;
#70658=CARTESIAN_POINT ( 'NONE',  ( 5.000000000000000000, 26.79245525562714292, 32.34446384429980981 ) ) ;
#70666=DIRECTION ( 'NONE',  ( -1.000000000000000000, 0.000000000000000000, -0.000000000000000000 ) ) ;
#70671=CIRCLE ( 'NONE', #62285, 16.00000000000000000 ) ;
#70676=AXIS2_PLACEMENT_3D ( 'NONE', #25561, #12795, #42864 ) ;
#70683=DIRECTION ( 'NONE',  ( -1.000000000000000000, 0.000000000000000000, 0.000000000000000000 ) ) ;
#70691=CIRCLE ( 'NONE', #15491, 37.49900000000000944 ) ;
#70725=CIRCLE ( 'NONE', #14334, 37.49900000000000944 ) ;
#70735=FACE_OUTER_BOUND ( 'NONE', #7859, .T. ) ;
#70762=VECTOR ( 'NONE', #20679, 1000.000000000000000 ) ;
#70774=EDGE_CURVE ( 'NONE', #61501, #51075, #71796, .T. ) ;
#70787=ORIENTED_EDGE ( 'NONE', *, *, #34712, .T. ) ;
#70792=CIRCLE ( 'NONE', #35966, 15.99999999999999822 ) ;
#70797=EDGE_CURVE ( 'NONE', #37666, #14575, #48150, .T. ) ;
#70806=VECTOR ( 'NONE', #57119, 1000.000000000000000 ) ;
#70815=ORIENTED_EDGE ( 'NONE', *, *, #58984, .F. ) ;
#70842=EDGE_CURVE ( 'NONE', #60472, #43729, #19067, .T. ) ;
#70846=DIRECTION ( 'NONE',  ( -1.000000000000000000, 0.000000000000000000, 0.000000000000000000 ) ) ;
#70854=CYLINDRICAL_SURFACE ( 'NONE', #64584, 12.50000000000000000 ) ;
#70867=CARTESIAN_POINT ( 'NONE',  ( 10.00000000000000000, -37.01155633439063308, 6.555932627142289526 ) ) ;
#70871=CIRCLE ( 'NONE', #30024, 12.50000000000000000 ) ;
#70873=CARTESIAN_POINT ( 'NONE',  ( 0.000000000000000000, 0.000000000000000000, 0.000000000000000000 ) ) ;
#70886=EDGE_CURVE ( 'NONE', #71645, #9962, #5270, .T. ) ;
#70890=EDGE_CURVE ( 'NONE', #67705, #14575, #56323, .T. ) ;
#70899=CARTESIAN_POINT ( 'NONE',  ( 4.999999999999999112, 9.188173127307898369, -40.98264845739739570 ) ) ;
#70902=LINE ( 'NONE', #54367, #27336 ) ;
#70916=DIRECTION ( 'NONE',  ( -1.000000000000000000, 0.000000000000000000, -0.000000000000000000 ) ) ;
#70937=DIRECTION ( 'NONE',  ( 0.000000000000000000, -0.1564344650402170189, -0.9876883405951399908 ) ) ;
#70947=AXIS2_PLACEMENT_3D ( 'NONE', #45655, #55803, #9930 ) ;
#70967=EDGE_CURVE ( 'NONE', #9139, #61669, #73161, .T. ) ;
#70971=EDGE_CURVE ( 'NONE', #53879, #35308, #53968, .T. ) ;
#70986=VECTOR ( 'NONE', #35074, 1000.000000000000000 ) ;
#70991=ORIENTED_EDGE ( 'NONE', *, *, #52432, .T. ) ;
#70993=( NAMED_UNIT ( * ) PLANE_ANGLE_UNIT ( ) SI_UNIT ( $, .RADIAN. ) );
#71013=AXIS2_PLACEMENT_3D ( 'NONE', #68182, #56546, #66701 ) ;
#71031=ORIENTED_EDGE ( 'NONE', *, *, #42049, .F. ) ;
#71034=FACE_OUTER_BOUND ( 'NONE', #19472, .T. ) ;
#71047=DIRECTION ( 'NONE',  ( 0.000000000000000000, 0.000000000000000000, 1.000000000000000000 ) ) ;
#71082=ORIENTED_EDGE ( 'NONE', *, *, #39739, .F. ) ;
#71094=EDGE_LOOP ( 'NONE', ( #28043, #50977, #36492, #36076 ) ) ;
#71112=ORIENTED_EDGE ( 'NONE', *, *, #36711, .F. ) ;
#71127=CARTESIAN_POINT ( 'NONE',  ( 10.00000000000000000, -4.992566952385247170, 37.16516213103275845 ) ) ;
#71129=ADVANCED_FACE ( 'NONE', ( #7833 ), #42790, .T. ) ;
#71147=DIRECTION ( 'NONE',  ( -1.000000000000000000, -0.000000000000000000, 0.000000000000000000 ) ) ;
#71165=ORIENTED_EDGE ( 'NONE', *, *, #40427, .T. ) ;
#71171=ORIENTED_EDGE ( 'NONE', *, *, #70971, .T. ) ;
#71173=EDGE_CURVE ( 'NONE', #64110, #25146, #25492, .T. ) ;
#71180=EDGE_CURVE ( 'NONE', #37092, #55893, #32314, .T. ) ;
#71188=DIRECTION ( 'NONE',  ( 0.000000000000000000, -0.7071067811865389130, -0.7071067811865561215 ) ) ;
#71216=DIRECTION ( 'NONE',  ( -1.000000000000000000, 0.000000000000000000, 0.000000000000000000 ) ) ;
#71232=DIRECTION ( 'NONE',  ( 0.000000000000000000, 0.000000000000000000, 1.000000000000000000 ) ) ;
#71233=FACE_OUTER_BOUND ( 'NONE', #31236, .T. ) ;
#71245=DIRECTION ( 'NONE',  ( -1.000000000000000000, 0.000000000000000000, -0.000000000000000000 ) ) ;
#71246=EDGE_LOOP ( 'NONE', ( #72586, #47876, #39938, #26615 ) ) ;
#71262=CARTESIAN_POINT ( 'NONE',  ( -10.00000000000000000, 0.000000000000000000, 0.000000000000000000 ) ) ;
#71263=CIRCLE ( 'NONE', #62959, 42.00000000000000000 ) ;
#71264=CARTESIAN_POINT ( 'NONE',  ( 10.00000000000000000, 10.96151621346540317, -35.95386929396244113 ) ) ;
#71267=ADVANCED_FACE ( 'NONE', ( #43911 ), #49894, .T. ) ;
#71281=CYLINDRICAL_SURFACE ( 'NONE', #15811, 37.49900000000000233 ) ;
#71282=EDGE_CURVE ( 'NONE', #14214, #52264, #62409, .T. ) ;
#71291=DIRECTION ( 'NONE',  ( 0.000000000000000000, -0.4539904997395542430, 0.8910065241883641241 ) ) ;
#71292=DIRECTION ( 'NONE',  ( 0.000000000000000000, 0.8090169943749447867, 0.5877852522924769119 ) ) ;
#71297=ORIENTED_EDGE ( 'NONE', *, *, #60380, .F. ) ;
#71300=EDGE_CURVE ( 'NONE', #73482, #65810, #1204, .T. ) ;
#71309=CARTESIAN_POINT ( 'NONE',  ( 0.000000000000000000, 27.05870788708231700, 26.08949754953034272 ) ) ;
#71330=CIRCLE ( 'NONE', #66585, 15.99999999999999645 ) ;
#71332=CARTESIAN_POINT ( 'NONE',  ( 5.000000000000000000, -35.47612816024539484, 22.48208911017487921 ) ) ;
#71382=EDGE_CURVE ( 'NONE', #51520, #21663, #59166, .T. ) ;
#71383=ORIENTED_EDGE ( 'NONE', *, *, #24841, .F. ) ;
#71391=FACE_OUTER_BOUND ( 'NONE', #45596, .T. ) ;
#71433=EDGE_CURVE ( 'NONE', #2268, #42999, #58791, .T. ) ;
#71452=CYLINDRICAL_SURFACE ( 'NONE', #31671, 37.49900000000000233 ) ;
#71453=VERTEX_POINT ( 'NONE', #57406 ) ;
#71465=LINE ( 'NONE', #35778, #59303 ) ;
#71466=EDGE_CURVE ( 'NONE', #38459, #53810, #22832, .T. ) ;
#71510=CARTESIAN_POINT ( 'NONE',  ( 10.00000000000000000, 0.000000000000000000, 0.000000000000000000 ) ) ;
#71525=DIRECTION ( 'NONE',  ( 0.000000000000000000, 0.000000000000000000, 1.000000000000000000 ) ) ;
#71548=ADVANCED_FACE ( 'NONE', ( #824 ), #73448, .T. ) ;
#71566=AXIS2_PLACEMENT_3D ( 'NONE', #69962, #47779, #58698 ) ;
#71578=LINE ( 'NONE', #25726, #67360 ) ;
#71579=DIRECTION ( 'NONE',  ( -1.000000000000000000, 0.000000000000000000, -0.000000000000000000 ) ) ;
#71583=ORIENTED_EDGE ( 'NONE', *, *, #33536, .T. ) ;
#71587=ORIENTED_EDGE ( 'NONE', *, *, #3824, .F. ) ;
#71604=EDGE_CURVE ( 'NONE', #51310, #22671, #70792, .T. ) ;
#71633=EDGE_CURVE ( 'NONE', #1093, #56703, #51589, .T. ) ;
#71645=VERTEX_POINT ( 'NONE', #67073 ) ;
#71653=DIRECTION ( 'NONE',  ( -1.000000000000000000, -0.000000000000000000, 0.000000000000000000 ) ) ;
#71665=CIRCLE ( 'NONE', #62086, 37.49900000000001654 ) ;
#71718=EDGE_CURVE ( 'NONE', #17733, #5742, #54142, .T. ) ;
#71754=LINE ( 'NONE', #60147, #72093 ) ;
#71759=CARTESIAN_POINT ( 'NONE',  ( 0.000000000000000000, -22.64427369931191336, 30.00120703465197280 ) ) ;
#71760=ORIENTED_EDGE ( 'NONE', *, *, #13392, .T. ) ;
#71765=CYLINDRICAL_SURFACE ( 'NONE', #16436, 16.00000000000000000 ) ;
#71796=LINE ( 'NONE', #43271, #2320 ) ;
#71798=AXIS2_PLACEMENT_3D ( 'NONE', #40367, #56935, #56569 ) ;
#71811=ORIENTED_EDGE ( 'NONE', *, *, #41534, .T. ) ;
#71838=DIRECTION ( 'NONE',  ( 0.000000000000000000, 8.881784197001252323E-16, 1.000000000000000000 ) ) ;
#71876=DIRECTION ( 'NONE',  ( -1.000000000000000000, 0.000000000000000000, -0.000000000000000000 ) ) ;
#71886=VECTOR ( 'NONE', #30122, 1000.000000000000000 ) ;
#71896=CYLINDRICAL_SURFACE ( 'NONE', #49077, 42.00000000000000000 ) ;
#71901=EDGE_LOOP ( 'NONE', ( #12036, #22254, #72094, #20305 ) ) ;
#71908=AXIS2_PLACEMENT_3D ( 'NONE', #52043, #23852, #47524 ) ;
#71915=AXIS2_PLACEMENT_3D ( 'NONE', #29637, #24750, #57498 ) ;
#71917=ORIENTED_EDGE ( 'NONE', *, *, #48364, .F. ) ;
#71929=CARTESIAN_POINT ( 'NONE',  ( 0.000000000000000000, -16.45098606841102651, -33.79645857604531045 ) ) ;
#71956=CARTESIAN_POINT ( 'NONE',  ( 10.00000000000000000, 37.58145647212455032, -0.6853352020786441789 ) ) ;
#71976=VECTOR ( 'NONE', #53154, 1000.000000000000000 ) ;
#71978=DIRECTION ( 'NONE',  ( -1.000000000000000000, 0.000000000000000000, 0.000000000000000000 ) ) ;
#71992=CARTESIAN_POINT ( 'NONE',  ( 10.00000000000000000, 6.555932627142952995, -37.01155633439051940 ) ) ;
#72005=DIRECTION ( 'NONE',  ( -1.000000000000000000, 0.000000000000000000, -0.000000000000000000 ) ) ;
#72017=VERTEX_POINT ( 'NONE', #42462 ) ;
#72031=CARTESIAN_POINT ( 'NONE',  ( 10.00000000000000000, 0.000000000000000000, 0.000000000000000000 ) ) ;
#72032=EDGE_CURVE ( 'NONE', #3104, #64823, #37272, .T. ) ;
#72037=DIRECTION ( 'NONE',  ( 0.000000000000000000, -0.3090169943749548342, 0.9510565162951511997 ) ) ;
#72040=CARTESIAN_POINT ( 'NONE',  ( 10.00000000000000000, -22.64427369931148348, -30.00120703465229965 ) ) ;
#72062=ORIENTED_EDGE ( 'NONE', *, *, #51929, .F. ) ;
#72093=VECTOR ( 'NONE', #24798, 1000.000000000000000 ) ;
#72094=ORIENTED_EDGE ( 'NONE', *, *, #30013, .F. ) ;
#72129=ORIENTED_EDGE ( 'NONE', *, *, #4530, .F. ) ;
#72132=VERTEX_POINT ( 'NONE', #45441 ) ;
#72151=CARTESIAN_POINT ( 'NONE',  ( 0.000000000000000000, -41.81611651403864727, 3.925862922256025289 ) ) ;
#72155=DIRECTION ( 'NONE',  ( -1.000000000000000000, 0.000000000000000000, -0.000000000000000000 ) ) ;
#72157=DIRECTION ( 'NONE',  ( -1.000000000000000000, 0.000000000000000000, 0.000000000000000000 ) ) ;
#72176=CIRCLE ( 'NONE', #35009, 42.00000000000000000 ) ;
#72191=ORIENTED_EDGE ( 'NONE', *, *, #53833, .F. ) ;
#72197=VERTEX_POINT ( 'NONE', #41627 ) ;
#72203=ORIENTED_EDGE ( 'NONE', *, *, #2897, .T. ) ;
#72214=LINE ( 'NONE', #67703, #52229 ) ;
#72216=ORIENTED_EDGE ( 'NONE', *, *, #1341, .F. ) ;
#72247=DIRECTION ( 'NONE',  ( -1.000000000000000000, -0.000000000000000000, -0.000000000000000000 ) ) ;
#72252=VECTOR ( 'NONE', #22606, 1000.000000000000000 ) ;
#72278=CARTESIAN_POINT ( 'NONE',  ( 0.000000000000000000, 37.22597642581158084, -5.202137450156524068 ) ) ;
#72279=ORIENTED_EDGE ( 'NONE', *, *, #2933, .F. ) ;
#72292=ORIENTED_EDGE ( 'NONE', *, *, #42860, .T. ) ;
#72301=CYLINDRICAL_SURFACE ( 'NONE', #21547, 16.00000000000000000 ) ;
#72313=FACE_OUTER_BOUND ( 'NONE', #68249, .T. ) ;
#72342=CARTESIAN_POINT ( 'NONE',  ( 0.000000000000000000, 30.84782396557217865, 21.32104025579125306 ) ) ;
#72376=EDGE_CURVE ( 'NONE', #23893, #4586, #64742, .T. ) ;
#72408=CYLINDRICAL_SURFACE ( 'NONE', #3439, 37.49900000000000233 ) ;
#72410=DIRECTION ( 'NONE',  ( 0.000000000000000000, 0.000000000000000000, 1.000000000000000000 ) ) ;
#72421=ORIENTED_EDGE ( 'NONE', *, *, #15248, .T. ) ;
#72440=CARTESIAN_POINT ( 'NONE',  ( 0.000000000000000000, 0.000000000000000000, 0.000000000000000000 ) ) ;
#72459=ADVANCED_FACE ( 'NONE', ( #54393 ), #54762, .T. ) ;
#72468=DIRECTION ( 'NONE',  ( -1.000000000000000000, -0.000000000000000000, 0.000000000000000000 ) ) ;
#72499=ORIENTED_EDGE ( 'NONE', *, *, #4043, .T. ) ;
#72519=DIRECTION ( 'NONE',  ( -1.000000000000000000, -0.000000000000000000, 0.000000000000000000 ) ) ;
#72529=DIRECTION ( 'NONE',  ( -1.000000000000000000, -0.000000000000000000, 0.000000000000000000 ) ) ;
#72566=CARTESIAN_POINT ( 'NONE',  ( 10.00000000000000000, -31.52238457039619490, 27.75498641678731104 ) ) ;
#72578=ORIENTED_EDGE ( 'NONE', *, *, #25199, .T. ) ;
#72584=ORIENTED_EDGE ( 'NONE', *, *, #2355, .F. ) ;
#72586=ORIENTED_EDGE ( 'NONE', *, *, #11691, .F. ) ;
#72589=DIRECTION ( 'NONE',  ( 0.000000000000000000, 1.000000000000000000, 3.491481338843133750E-15 ) ) ;
#72597=VERTEX_POINT ( 'NONE', #10378 ) ;
#72615=EDGE_CURVE ( 'NONE', #53345, #37277, #33541, .T. ) ;
#72629=DIRECTION ( 'NONE',  ( 0.000000000000000000, 0.000000000000000000, 1.000000000000000000 ) ) ;
#72630=ORIENTED_EDGE ( 'NONE', *, *, #73314, .F. ) ;
#72631=CARTESIAN_POINT ( 'NONE',  ( 10.00000000000000000, -37.16516213103280108, 4.992566952384862589 ) ) ;
#72637=ADVANCED_FACE ( 'NONE', ( #38589 ), #34052, .T. ) ;
#72646=DIRECTION ( 'NONE',  ( 0.000000000000000000, 0.000000000000000000, 1.000000000000000000 ) ) ;
#72654=AXIS2_PLACEMENT_3D ( 'NONE', #49848, #50972, #73521 ) ;
#72667=CIRCLE ( 'NONE', #67928, 12.50000000000000000 ) ;
#72669=DIRECTION ( 'NONE',  ( -1.000000000000000000, -0.000000000000000000, -0.000000000000000000 ) ) ;
#72672=ORIENTED_EDGE ( 'NONE', *, *, #28192, .F. ) ;
#72683=LINE ( 'NONE', #60703, #73219 ) ;
#72716=FACE_OUTER_BOUND ( 'NONE', #11919, .T. ) ;
#72754=DIRECTION ( 'NONE',  ( 0.000000000000000000, 0.000000000000000000, 1.000000000000000000 ) ) ;
#72761=ORIENTED_EDGE ( 'NONE', *, *, #9131, .T. ) ;
#72774=VERTEX_POINT ( 'NONE', #12864 ) ;
#72786=DIRECTION ( 'NONE',  ( -1.000000000000000000, -0.000000000000000000, -0.000000000000000000 ) ) ;
#72821=EDGE_LOOP ( 'NONE', ( #61512, #61674, #31860, #73563 ) ) ;
#72833=LINE ( 'NONE', #66849, #14111 ) ;
#72834=CIRCLE ( 'NONE', #5698, 16.00000000000000355 ) ;
#72851=CARTESIAN_POINT ( 'NONE',  ( 10.00000000000000000, 37.58145647212453611, 0.6853352020791767529 ) ) ;
#72864=ORIENTED_EDGE ( 'NONE', *, *, #23604, .F. ) ;
#72868=DIRECTION ( 'NONE',  ( -1.000000000000000000, 0.000000000000000000, 0.000000000000000000 ) ) ;
#72869=LINE ( 'NONE', #21374, #39911 ) ;
#72907=CARTESIAN_POINT ( 'NONE',  ( 0.000000000000000000, 0.000000000000000000, 0.000000000000000000 ) ) ;
#72913=VERTEX_POINT ( 'NONE', #48678 ) ;
#72938=ORIENTED_EDGE ( 'NONE', *, *, #62686, .F. ) ;
#72960=CARTESIAN_POINT ( 'NONE',  ( 10.00000000000000000, 0.000000000000000000, 0.000000000000000000 ) ) ;
#73019=EDGE_CURVE ( 'NONE', #53437, #48441, #68, .T. ) ;
#73020=VERTEX_POINT ( 'NONE', #21197 ) ;
#73024=CIRCLE ( 'NONE', #5827, 16.00000000000000000 ) ;
#73031=VERTEX_POINT ( 'NONE', #10676 ) ;
#73036=DIRECTION ( 'NONE',  ( -1.000000000000000000, -0.000000000000000000, -0.000000000000000000 ) ) ;
#73056=ADVANCED_FACE ( 'NONE', ( #50897 ), #15943, .T. ) ;
#73057=AXIS2_PLACEMENT_3D ( 'NONE', #25316, #53144, #23832 ) ;
#73059=CARTESIAN_POINT ( 'NONE',  ( 0.000000000000000000, -17.80606268964516659, -33.00180498840066434 ) ) ;
#73074=EDGE_CURVE ( 'NONE', #15264, #10428, #31188, .T. ) ;
#73090=AXIS2_PLACEMENT_3D ( 'NONE', #68514, #33914, #12459 ) ;
#73139=FACE_OUTER_BOUND ( 'NONE', #11222, .T. ) ;
#73159=ORIENTED_EDGE ( 'NONE', *, *, #19664, .F. ) ;
#73161=CIRCLE ( 'NONE', #65934, 16.00000000000000000 ) ;
#73183=AXIS2_PLACEMENT_3D ( 'NONE', #45395, #68697, #5551 ) ;
#73184=DIRECTION ( 'NONE',  ( -1.000000000000000000, 0.000000000000000000, -0.000000000000000000 ) ) ;
#73196=AXIS2_PLACEMENT_3D ( 'NONE', #57182, #11664, #34604 ) ;
#73202=DIRECTION ( 'NONE',  ( 0.000000000000000000, 0.000000000000000000, 1.000000000000000000 ) ) ;
#73205=ORIENTED_EDGE ( 'NONE', *, *, #4631, .F. ) ;
#73209=DIRECTION ( 'NONE',  ( 0.000000000000000000, 0.000000000000000000, 1.000000000000000000 ) ) ;
#73219=VECTOR ( 'NONE', #48300, 1000.000000000000000 ) ;
#73222=CIRCLE ( 'NONE', #27622, 42.00000000000000000 ) ;
#73261=EDGE_CURVE ( 'NONE', #39405, #36301, #3630, .T. ) ;
#73294=ORIENTED_EDGE ( 'NONE', *, *, #64663, .F. ) ;
#73301=AXIS2_PLACEMENT_3D ( 'NONE', #550, #24546, #64784 ) ;
#73311=CARTESIAN_POINT ( 'NONE',  ( 0.000000000000000000, 0.000000000000000000, 0.000000000000000000 ) ) ;
#73312=VERTEX_POINT ( 'NONE', #18893 ) ;
#73314=EDGE_CURVE ( 'NONE', #15341, #1614, #4819, .T. ) ;
#73360=CIRCLE ( 'NONE', #40970, 42.00000000000000000 ) ;
#73363=CARTESIAN_POINT ( 'NONE',  ( 0.000000000000000000, -37.48860685352290290, -0.8828120875904512665 ) ) ;
#73372=DIRECTION ( 'NONE',  ( 0.000000000000000000, 0.000000000000000000, 1.000000000000000000 ) ) ;
#73434=CARTESIAN_POINT ( 'NONE',  ( 10.00000000000000000, 37.16516213103277977, 4.992566952385115719 ) ) ;
#73435=CARTESIAN_POINT ( 'NONE',  ( 10.00000000000000000, 0.000000000000000000, 0.000000000000000000 ) ) ;
#73448=CYLINDRICAL_SURFACE ( 'NONE', #60038, 16.00000000000000000 ) ;
#73482=VERTEX_POINT ( 'NONE', #11591 ) ;
#73490=DIRECTION ( 'NONE',  ( -1.000000000000000000, 0.000000000000000000, 0.000000000000000000 ) ) ;
#73491=ORIENTED_EDGE ( 'NONE', *, *, #9075, .F. ) ;
#73500=ORIENTED_EDGE ( 'NONE', *, *, #44492, .T. ) ;
#73512=CYLINDRICAL_SURFACE ( 'NONE', #24302, 42.00000000000000000 ) ;
#73517=VERTEX_POINT ( 'NONE', #28517 ) ;
#73521=DIRECTION ( 'NONE',  ( 0.000000000000000000, 0.000000000000000000, 1.000000000000000000 ) ) ;
#73523=DIRECTION ( 'NONE',  ( -1.000000000000000000, 0.000000000000000000, 0.000000000000000000 ) ) ;
#73543=CIRCLE ( 'NONE', #62798, 16.00000000000000000 ) ;
#73563=ORIENTED_EDGE ( 'NONE', *, *, #23283, .T. ) ;
#73566=CARTESIAN_POINT ( 'NONE',  ( 10.00000000000000000, 0.000000000000000000, 0.000000000000000000 ) ) ;
#73579=FACE_OUTER_BOUND ( 'NONE', #17230, .T. ) ;
#73598=CARTESIAN_POINT ( 'NONE',  ( 0.000000000000000000, -4.992566952384716927, -37.16516213103282951 ) ) ;
#73619=DIRECTION ( 'NONE',  ( -1.000000000000000000, 0.000000000000000000, 0.000000000000000000 ) ) ;
#73633=LINE ( 'NONE', #16504, #65247 ) ;
#73634=DIRECTION ( 'NONE',  ( -1.000000000000000000, 0.000000000000000000, -0.000000000000000000 ) ) ;
#73638=LINE ( 'NONE', #40935, #19116 ) ;
#73645=AXIS2_PLACEMENT_3D ( 'NONE', #25837, #26577, #13805 ) ;
#73649=FACE_OUTER_BOUND ( 'NONE', #24905, .T. ) ;
#73673=CARTESIAN_POINT ( 'NONE',  ( 10.00000000000000000, 0.000000000000000000, 0.000000000000000000 ) ) ;
#73700=ORIENTED_EDGE ( 'NONE', *, *, #71282, .F. ) ;
#73733=CARTESIAN_POINT ( 'NONE',  ( 10.00000000000000000, 29.81001611431009479, 22.74946021919143391 ) ) ;
#73741=CIRCLE ( 'NONE', #38929, 16.00000000000000000 ) ;
#73760=ORIENTED_EDGE ( 'NONE', *, *, #51442, .T. ) ;
#73761=AXIS2_PLACEMENT_3D ( 'NONE', #8339, #19240, #7961 ) ;
#73770=ORIENTED_EDGE ( 'NONE', *, *, #45483, .T. ) ;
#73784=CIRCLE ( 'NONE', #25768, 16.00000000000000355 ) ;
#73802=CARTESIAN_POINT ( 'NONE',  ( 10.00000000000000000, -36.88895765772637247, 6.736453364083436313 ) ) ;
#73805=CARTESIAN_POINT ( 'NONE',  ( 4.999999999999999112, 38.55633173627034438, -16.65560815589369881 ) ) ;
#73849=ORIENTED_EDGE ( 'NONE', *, *, #14935, .T. ) ;
#73868=DIRECTION ( 'NONE',  ( 1.000000000000000000, 0.000000000000000000, 0.000000000000000000 ) ) ;
#73871=ORIENTED_EDGE ( 'NONE', *, *, #44205, .F. ) ;
#73878=AXIS2_PLACEMENT_3D ( 'NONE', #12157, #23091, #56567 ) ;
#73886=CARTESIAN_POINT ( 'NONE',  ( -10.00000000000000000, 0.000000000000000000, 0.000000000000000000 ) ) ;
#73887=ORIENTED_EDGE ( 'NONE', *, *, #11058, .T. ) ;
#73898=EDGE_LOOP ( 'NONE', ( #11573, #42064, #34588, #20123 ) ) ;
#73903=ORIENTED_EDGE ( 'NONE', *, *, #70158, .T. ) ;
#73908=CARTESIAN_POINT ( 'NONE',  ( 10.00000000000000000, -30.00120703465222149, 22.64427369931158296 ) ) ;
#73935=CARTESIAN_POINT ( 'NONE',  ( 10.00000000000000000, 25.88420570971400991, 27.13269053701105449 ) ) ;
#73938=DIRECTION ( 'NONE',  ( 0.000000000000000000, 0.000000000000000000, 1.000000000000000000 ) ) ;
#73941=EDGE_LOOP ( 'NONE', ( #10098, #21566, #32426, #35116 ) ) ;
#73943=EDGE_CURVE ( 'NONE', #23737, #11727, #46108, .T. ) ;
#73955=DIRECTION ( 'NONE',  ( 0.000000000000000000, 0.000000000000000000, 1.000000000000000000 ) ) ;
#73984=CARTESIAN_POINT ( 'NONE',  ( 10.00000000000000000, 0.000000000000000000, 0.000000000000000000 ) ) ;
#73989=VERTEX_POINT ( 'NONE', #5899 ) ;
#74013=CARTESIAN_POINT ( 'NONE',  ( 0.000000000000000000, 10.74501242461333028, -35.92658777277499382 ) ) ;
#74032=VERTEX_POINT ( 'NONE', #50245 ) ;
#74040=ORIENTED_EDGE ( 'NONE', *, *, #64429, .T. ) ;
#74054=ORIENTED_EDGE ( 'NONE', *, *, #61010, .T. ) ;
#74064=ADVANCED_FACE ( 'NONE', ( #10781 ), #57761, .T. ) ;
#74075=AXIS2_PLACEMENT_3D ( 'NONE', #6588, #58829, #12213 ) ;
#74083=ORIENTED_EDGE ( 'NONE', *, *, #42860, .F. ) ;
#74090=CARTESIAN_POINT ( 'NONE',  ( 50.00005079999999680, 1.530808498934191521E-15, -12.50000000000000000 ) ) ;
#74099=CARTESIAN_POINT ( 'NONE',  ( 10.00000000000000000, -37.16516213103273714, -4.992566952385376844 ) ) ;
#74101=LINE ( 'NONE', #22613, #61096 ) ;
#74109=CARTESIAN_POINT ( 'NONE',  ( 10.00000000000000000, 37.22597642581158084, 10.79786254984347593 ) ) ;
#74118=( GEOMETRIC_REPRESENTATION_CONTEXT ( 3 ) GLOBAL_UNCERTAINTY_ASSIGNED_CONTEXT ( ( #54153 ) ) GLOBAL_UNIT_ASSIGNED_CONTEXT ( ( #10159, #33082, #17288 ) ) REPRESENTATION_CONTEXT ( 'NONE', 'WORKASPACE' ) );
#74128=DIRECTION ( 'NONE',  ( -1.000000000000000000, 0.000000000000000000, -0.000000000000000000 ) ) ;
#74139=ORIENTED_EDGE ( 'NONE', *, *, #70797, .T. ) ;
#74144=ORIENTED_EDGE ( 'NONE', *, *, #43294, .F. ) ;
#74158=ORIENTED_EDGE ( 'NONE', *, *, #39539, .F. ) ;
#74176=DIRECTION ( 'NONE',  ( -1.000000000000000000, -0.000000000000000000, 0.000000000000000000 ) ) ;
#74203=DIRECTION ( 'NONE',  ( -1.000000000000000000, -0.000000000000000000, -0.000000000000000000 ) ) ;
#74208=FACE_OUTER_BOUND ( 'NONE', #48339, .T. ) ;
#74209=DIRECTION ( 'NONE',  ( 0.000000000000000000, 0.000000000000000000, 1.000000000000000000 ) ) ;
#74232=ORIENTED_EDGE ( 'NONE', *, *, #31000, .T. ) ;
#74275=DIRECTION ( 'NONE',  ( 0.000000000000000000, 0.000000000000000000, 1.000000000000000000 ) ) ;
#74279=DIRECTION ( 'NONE',  ( -1.000000000000000000, 0.000000000000000000, -0.000000000000000000 ) ) ;
#74283=AXIS2_PLACEMENT_3D ( 'NONE', #15894, #6116, #68890 ) ;
#74314=CIRCLE ( 'NONE', #62308, 15.99999999999999822 ) ;
#74336=CYLINDRICAL_SURFACE ( 'NONE', #58526, 16.00000000000000000 ) ;
#74338=AXIS2_PLACEMENT_3D ( 'NONE', #25234, #48522, #54181 ) ;
ENDSEC;
END-ISO-10303-21;
